ISO-10303-21;
HEADER;
/* Generated by software containing ST-Developer
 * from STEP Tools, Inc. (www.steptools.com) 
 */

FILE_DESCRIPTION(
/* description */ (''),
/* implementation_level */ '2;1');

FILE_NAME(
/* name */ 'ISO 1207 - M3 x 6 - 4.8.step',
/* time_stamp */ '2026-10-14T18:40:07-07:00',
/* author */ (''),
/* organization */ (''),
/* preprocessor_version */ 'ST-DEVELOPER v20.2',
/* originating_system */ 'Autodesk Translation Framework v15.15.0.0',
/* authorisation */ '');

FILE_SCHEMA (('AUTOMOTIVE_DESIGN { 1 0 10303 214 3 1 1 }'));
ENDSEC;

DATA;
#10=MECHANICAL_DESIGN_GEOMETRIC_PRESENTATION_REPRESENTATION('',(#840),#81040);
#356=(
BOUNDED_CURVE()
B_SPLINE_CURVE(2,(#80918,#80919,#80920),.UNSPECIFIED.,.F.,.F.)
B_SPLINE_CURVE_WITH_KNOTS((3,3),(0.,0.0569264978342637),.UNSPECIFIED.)
CURVE()
GEOMETRIC_REPRESENTATION_ITEM()
RATIONAL_B_SPLINE_CURVE((1.,1.00316883460161,1.))
REPRESENTATION_ITEM('')
);
#357=(
BOUNDED_CURVE()
B_SPLINE_CURVE(2,(#80923,#80924,#80925),.UNSPECIFIED.,.F.,.F.)
B_SPLINE_CURVE_WITH_KNOTS((3,3),(0.,0.0569264978342636),.UNSPECIFIED.)
CURVE()
GEOMETRIC_REPRESENTATION_ITEM()
RATIONAL_B_SPLINE_CURVE((1.,1.00316883454694,1.))
REPRESENTATION_ITEM('')
);
#358=(
BOUNDED_CURVE()
B_SPLINE_CURVE(2,(#80930,#80931,#80932),.UNSPECIFIED.,.F.,.F.)
B_SPLINE_CURVE_WITH_KNOTS((3,3),(0.,0.0569264978342637),.UNSPECIFIED.)
CURVE()
GEOMETRIC_REPRESENTATION_ITEM()
RATIONAL_B_SPLINE_CURVE((1.,1.00316883459387,1.))
REPRESENTATION_ITEM('')
);
#359=(
BOUNDED_CURVE()
B_SPLINE_CURVE(2,(#80936,#80937,#80938),.UNSPECIFIED.,.F.,.F.)
B_SPLINE_CURVE_WITH_KNOTS((3,3),(0.,0.0569264978342637),.UNSPECIFIED.)
CURVE()
GEOMETRIC_REPRESENTATION_ITEM()
RATIONAL_B_SPLINE_CURVE((1.,1.00316883460998,1.))
REPRESENTATION_ITEM('')
);
#363=TOROIDAL_SURFACE('',#16535,1.5635,0.1);
#370=B_SPLINE_SURFACE_WITH_KNOTS('',3,3,((#80001,#80002,#80003,#80004,#80005,
#80006,#80007,#80008,#80009,#80010,#80011,#80012,#80013,#80014,#80015,#80016,
#80017,#80018,#80019,#80020,#80021,#80022,#80023,#80024,#80025,#80026,#80027,
#80028,#80029,#80030,#80031,#80032,#80033,#80034,#80035,#80036,#80037,#80038,
#80039,#80040,#80041,#80042,#80043,#80044,#80045,#80046,#80047,#80048,#80049,
#80050,#80051,#80052,#80053,#80054,#80055,#80056,#80057,#80058,#80059,#80060,
#80061,#80062,#80063,#80064,#80065,#80066,#80067,#80068,#80069,#80070,#80071,
#80072,#80073,#80074,#80075,#80076,#80077,#80078,#80079,#80080,#80081,#80082,
#80083,#80084),(#80085,#80086,#80087,#80088,#80089,#80090,#80091,#80092,
#80093,#80094,#80095,#80096,#80097,#80098,#80099,#80100,#80101,#80102,#80103,
#80104,#80105,#80106,#80107,#80108,#80109,#80110,#80111,#80112,#80113,#80114,
#80115,#80116,#80117,#80118,#80119,#80120,#80121,#80122,#80123,#80124,#80125,
#80126,#80127,#80128,#80129,#80130,#80131,#80132,#80133,#80134,#80135,#80136,
#80137,#80138,#80139,#80140,#80141,#80142,#80143,#80144,#80145,#80146,#80147,
#80148,#80149,#80150,#80151,#80152,#80153,#80154,#80155,#80156,#80157,#80158,
#80159,#80160,#80161,#80162,#80163,#80164,#80165,#80166,#80167,#80168),
(#80169,#80170,#80171,#80172,#80173,#80174,#80175,#80176,#80177,#80178,
#80179,#80180,#80181,#80182,#80183,#80184,#80185,#80186,#80187,#80188,#80189,
#80190,#80191,#80192,#80193,#80194,#80195,#80196,#80197,#80198,#80199,#80200,
#80201,#80202,#80203,#80204,#80205,#80206,#80207,#80208,#80209,#80210,#80211,
#80212,#80213,#80214,#80215,#80216,#80217,#80218,#80219,#80220,#80221,#80222,
#80223,#80224,#80225,#80226,#80227,#80228,#80229,#80230,#80231,#80232,#80233,
#80234,#80235,#80236,#80237,#80238,#80239,#80240,#80241,#80242,#80243,#80244,
#80245,#80246,#80247,#80248,#80249,#80250,#80251,#80252),(#80253,#80254,
#80255,#80256,#80257,#80258,#80259,#80260,#80261,#80262,#80263,#80264,#80265,
#80266,#80267,#80268,#80269,#80270,#80271,#80272,#80273,#80274,#80275,#80276,
#80277,#80278,#80279,#80280,#80281,#80282,#80283,#80284,#80285,#80286,#80287,
#80288,#80289,#80290,#80291,#80292,#80293,#80294,#80295,#80296,#80297,#80298,
#80299,#80300,#80301,#80302,#80303,#80304,#80305,#80306,#80307,#80308,#80309,
#80310,#80311,#80312,#80313,#80314,#80315,#80316,#80317,#80318,#80319,#80320,
#80321,#80322,#80323,#80324,#80325,#80326,#80327,#80328,#80329,#80330,#80331,
#80332,#80333,#80334,#80335,#80336)),.UNSPECIFIED.,.F.,.F.,.F.,(4,4),(4,
1,1,1,1,1,1,1,1,1,1,1,1,1,1,1,1,1,1,1,1,1,1,1,1,1,1,1,1,1,1,1,1,1,1,1,1,
1,1,1,1,1,1,1,1,1,1,1,1,1,1,1,1,1,1,1,1,1,1,1,1,1,1,1,1,1,1,1,1,1,1,1,1,
1,1,1,1,1,1,1,1,4),(-0.000243720225400152,0.0332111771674427),(8.30203615430888,
9.29159561709456,10.2811550798802,11.2707145426659,12.2602740054516,13.2498334682373,
14.2393929310229,15.2289523938086,16.2185118565943,17.20807131938,18.1976307821657,
19.1871902449513,20.176749707737,21.1663091705227,22.1558686333084,23.145428096094,
24.1349875588797,25.1245470216654,26.1141064844511,27.1036659472367,28.0932254100224,
29.0827848728081,30.0723443355938,31.0619037983795,32.0514632611651,33.0410227239508,
34.0305821867365,35.0201416495222,36.0097011123078,36.9992605750935,37.9888200378792,
38.9783795006649,39.9679389634505,40.9574984262362,41.9470578890219,42.9366173518076,
43.9261768145933,44.9157362773789,45.9052957401646,46.8948552029503,47.884414665736,
48.8739741285216,49.8635335913073,50.853093054093,51.8426525168787,52.8322119796644,
53.82177144245,54.8113309052357,55.8008903680214,56.7904498308071,57.7800092935927,
58.7695687563784,59.7591282191641,60.7486876819498,61.7382471447354,62.7278066075211,
63.7173660703068,64.7069255330925,65.6964849958782,66.6860444586638,67.6756039214495,
68.6651633842352,69.6547228470209,70.6442823098065,71.6338417725922,72.6234012353779,
73.6129606981636,74.6025201609492,75.5920796237349,76.5816390865206,77.5711985493063,
78.560758012092,79.5503174748776,80.5398769376633,81.529436400449,82.5189958632347,
83.5085553260203,84.498114788806,85.4876742515917,86.4772337143774,87.466793177163,
88.4565963601741),.UNSPECIFIED.);
#371=B_SPLINE_SURFACE_WITH_KNOTS('',3,3,((#80552,#80553,#80554,#80555,#80556,
#80557,#80558,#80559,#80560,#80561,#80562,#80563,#80564,#80565,#80566,#80567,
#80568,#80569,#80570,#80571,#80572,#80573,#80574,#80575,#80576,#80577,#80578,
#80579,#80580,#80581,#80582,#80583,#80584,#80585,#80586,#80587,#80588,#80589,
#80590,#80591,#80592,#80593,#80594,#80595,#80596,#80597,#80598,#80599,#80600,
#80601,#80602,#80603,#80604,#80605,#80606,#80607,#80608,#80609,#80610,#80611,
#80612,#80613,#80614,#80615,#80616,#80617,#80618,#80619,#80620,#80621,#80622,
#80623,#80624,#80625,#80626,#80627,#80628,#80629,#80630,#80631,#80632,#80633),
(#80634,#80635,#80636,#80637,#80638,#80639,#80640,#80641,#80642,#80643,
#80644,#80645,#80646,#80647,#80648,#80649,#80650,#80651,#80652,#80653,#80654,
#80655,#80656,#80657,#80658,#80659,#80660,#80661,#80662,#80663,#80664,#80665,
#80666,#80667,#80668,#80669,#80670,#80671,#80672,#80673,#80674,#80675,#80676,
#80677,#80678,#80679,#80680,#80681,#80682,#80683,#80684,#80685,#80686,#80687,
#80688,#80689,#80690,#80691,#80692,#80693,#80694,#80695,#80696,#80697,#80698,
#80699,#80700,#80701,#80702,#80703,#80704,#80705,#80706,#80707,#80708,#80709,
#80710,#80711,#80712,#80713,#80714,#80715),(#80716,#80717,#80718,#80719,
#80720,#80721,#80722,#80723,#80724,#80725,#80726,#80727,#80728,#80729,#80730,
#80731,#80732,#80733,#80734,#80735,#80736,#80737,#80738,#80739,#80740,#80741,
#80742,#80743,#80744,#80745,#80746,#80747,#80748,#80749,#80750,#80751,#80752,
#80753,#80754,#80755,#80756,#80757,#80758,#80759,#80760,#80761,#80762,#80763,
#80764,#80765,#80766,#80767,#80768,#80769,#80770,#80771,#80772,#80773,#80774,
#80775,#80776,#80777,#80778,#80779,#80780,#80781,#80782,#80783,#80784,#80785,
#80786,#80787,#80788,#80789,#80790,#80791,#80792,#80793,#80794,#80795,#80796,
#80797),(#80798,#80799,#80800,#80801,#80802,#80803,#80804,#80805,#80806,
#80807,#80808,#80809,#80810,#80811,#80812,#80813,#80814,#80815,#80816,#80817,
#80818,#80819,#80820,#80821,#80822,#80823,#80824,#80825,#80826,#80827,#80828,
#80829,#80830,#80831,#80832,#80833,#80834,#80835,#80836,#80837,#80838,#80839,
#80840,#80841,#80842,#80843,#80844,#80845,#80846,#80847,#80848,#80849,#80850,
#80851,#80852,#80853,#80854,#80855,#80856,#80857,#80858,#80859,#80860,#80861,
#80862,#80863,#80864,#80865,#80866,#80867,#80868,#80869,#80870,#80871,#80872,
#80873,#80874,#80875,#80876,#80877,#80878,#80879)),.UNSPECIFIED.,.F.,.F.,
 .F.,(4,4),(4,1,1,1,1,1,1,1,1,1,1,1,1,1,1,1,1,1,1,1,1,1,1,1,1,1,1,1,1,1,
1,1,1,1,1,1,1,1,1,1,1,1,1,1,1,1,1,1,1,1,1,1,1,1,1,1,1,1,1,1,1,1,1,1,1,1,
1,1,1,1,1,1,1,1,1,1,1,1,1,4),(-0.000214583729420464,0.0331596015900255),
(13.6891124208198,14.6774813298366,15.6658502388533,16.65421914787,17.6425880568867,
18.6309569659034,19.6193258749201,20.6076947839369,21.5960636929536,22.5844326019703,
23.572801510987,24.5611704200037,25.5495393290204,26.5379082380372,27.5262771470539,
28.5146460560706,29.5030149650873,30.491383874104,31.4797527831207,32.4681216921375,
33.4564906011542,34.4448595101709,35.4332284191876,36.4215973282043,37.409966237221,
38.3983351462378,39.3867040552545,40.3750729642712,41.3634418732879,42.3518107823046,
43.3401796913213,44.3285486003381,45.3169175093548,46.3052864183715,47.2936553273882,
48.2820242364049,49.2703931454216,50.2587620544383,51.2471309634551,52.2354998724718,
53.2238687814885,54.2122376905052,55.2006065995219,56.1889755085386,57.1773444175554,
58.1657133265721,59.1540822355888,60.1424511446055,61.1308200536222,62.119188962639,
63.1075578716557,64.0959267806724,65.0842956896891,66.0726645987058,67.0610335077225,
68.0494024167392,69.037771325756,70.0261402347727,71.0145091437894,72.0028780528061,
72.9912469618228,73.9796158708395,74.9679847798563,75.956353688873,76.9447225978897,
77.9330915069064,78.9214604159231,79.9098293249398,80.8981982339565,81.8865671429733,
82.87493605199,83.8633049610067,84.8516738700234,85.8400427790401,86.8284116880568,
87.8167805970736,88.8051495060903,89.793518415107,90.7818873241237,91.7702562331404),
 .UNSPECIFIED.);
#736=B_SPLINE_CURVE_WITH_KNOTS('',3,(#71464,#71465,#71466,#71467,#71468,
#71469,#71470,#71471,#71472,#71473,#71474,#71475,#71476,#71477,#71478,#71479,
#71480,#71481,#71482,#71483,#71484,#71485,#71486,#71487,#71488,#71489,#71490,
#71491,#71492,#71493,#71494,#71495,#71496,#71497,#71498,#71499,#71500,#71501,
#71502,#71503,#71504,#71505,#71506,#71507,#71508,#71509,#71510,#71511,#71512,
#71513),.UNSPECIFIED.,.F.,.F.,(4,2,2,2,2,2,2,2,2,2,2,2,2,2,2,2,2,2,2,2,
2,2,2,2,4),(-0.122423255841805,-0.0999829706431865,-0.0946734372657195,
-0.0915496508705648,-0.0890650675485836,-0.0885992594482396,-0.0883573289906038,
-0.0882095118206766,-0.0881118884764039,-0.0880444119263917,-0.0877866006987234,
-0.087536118637217,-0.0872881890861582,-0.0870385562324885,-0.0823894050783034,
-0.0766946381380574,-0.0645769068426376,-0.0442003190552192,-0.0363184547158113,
-0.0337638212259385,-0.0322886353240006,-0.0306601413305012,-0.028154169115766,
-0.0251639879571378,-1.64669222008241E-5),.UNSPECIFIED.);
#737=B_SPLINE_CURVE_WITH_KNOTS('',3,(#71519,#71520,#71521,#71522,#71523,
#71524,#71525,#71526,#71527,#71528,#71529,#71530,#71531,#71532,#71533,#71534,
#71535,#71536,#71537,#71538,#71539,#71540,#71541,#71542,#71543,#71544,#71545,
#71546,#71547,#71548,#71549,#71550,#71551,#71552,#71553,#71554,#71555,#71556,
#71557,#71558,#71559,#71560,#71561,#71562,#71563,#71564,#71565,#71566,#71567,
#71568,#71569,#71570,#71571,#71572,#71573,#71574,#71575,#71576,#71577,#71578,
#71579,#71580,#71581,#71582,#71583,#71584,#71585,#71586,#71587,#71588,#71589,
#71590,#71591,#71592,#71593,#71594,#71595,#71596,#71597,#71598,#71599,#71600,
#71601,#71602,#71603,#71604,#71605,#71606,#71607,#71608,#71609,#71610,#71611,
#71612,#71613,#71614,#71615,#71616,#71617,#71618,#71619,#71620,#71621,#71622,
#71623,#71624,#71625,#71626,#71627,#71628,#71629,#71630,#71631,#71632,#71633,
#71634,#71635,#71636,#71637,#71638,#71639,#71640,#71641,#71642,#71643,#71644,
#71645,#71646,#71647,#71648,#71649,#71650,#71651,#71652,#71653,#71654,#71655,
#71656,#71657,#71658,#71659,#71660,#71661,#71662,#71663,#71664,#71665,#71666,
#71667,#71668,#71669,#71670,#71671,#71672,#71673,#71674,#71675,#71676,#71677,
#71678,#71679,#71680,#71681,#71682,#71683,#71684,#71685,#71686,#71687,#71688,
#71689,#71690,#71691,#71692,#71693,#71694,#71695,#71696,#71697,#71698,#71699,
#71700,#71701,#71702,#71703,#71704,#71705,#71706,#71707,#71708,#71709,#71710,
#71711,#71712),.UNSPECIFIED.,.F.,.F.,(4,2,2,2,2,2,2,2,2,2,2,2,2,2,2,2,2,
2,2,2,2,2,2,2,2,2,2,2,2,2,2,2,2,2,2,2,2,2,2,2,2,2,2,2,2,2,2,2,2,2,2,2,2,
2,2,2,2,2,2,2,2,2,2,2,2,2,2,2,2,2,2,2,2,2,2,2,2,2,2,2,2,2,2,2,2,2,2,2,2,
2,2,2,2,2,2,2,4),(-0.864476967535523,-0.863889634574054,-0.854675797726696,
-0.851995417487591,-0.850332462543021,-0.848693725647681,-0.846126694304765,
-0.837342669241336,-0.817949626733269,-0.799856452191916,-0.795213179187172,
-0.792256402525947,-0.78944606020123,-0.785566598692449,-0.775646096380797,
-0.759356663236241,-0.739509218581221,-0.73591332044633,-0.734035765386652,
-0.732479759907595,-0.730418678303376,-0.725701864215524,-0.718740184720392,
-0.689763722041757,-0.681111783649308,-0.677684159242237,-0.67486735084454,
-0.671971200872892,-0.667628387988473,-0.65335413729465,-0.639005936404083,
-0.621515501088468,-0.618529978947483,-0.616801368435175,-0.615206389194971,
-0.612861067751976,-0.606175308750074,-0.594406778078637,-0.567202520344681,
-0.561989034076196,-0.558914841376038,-0.556146221350687,-0.552552000476236,
-0.544551840079185,-0.532961386299957,-0.51022384185869,-0.503511592953835,
-0.50109781664782,-0.499506041170944,-0.497806124230549,-0.494954209620038,
-0.481789387126653,-0.45255284874405,-0.446110537707706,-0.442751740029425,
-0.440002483373519,-0.436769946478657,-0.430772981453676,-0.42304054345816,
-0.401718761825549,-0.38765749554838,-0.384728284700792,-0.383011709734159,
-0.38141001687277,-0.379029680187536,-0.372057204892285,-0.35944246953021,
-0.333798244484927,-0.328467102130281,-0.325339129525335,-0.322855780507222,
-0.319491609711317,-0.31280977049461,-0.295705363046698,-0.273692192348844,
-0.268952640071077,-0.266909685660323,-0.265352735250808,-0.263489349530779,
-0.259848259621297,-0.245637777556396,-0.218799199836102,-0.212365474480367,
-0.209009532762126,-0.206261938931301,-0.203030665317132,-0.197034248549036,
-0.189301661782186,-0.167974324458412,-0.153915929666823,-0.150987715178024,
-0.149271939936827,-0.147670744624839,-0.145291645111244,-0.138328368373508,
-0.125743539426254,-0.122423255841805),.UNSPECIFIED.);
#738=B_SPLINE_CURVE_WITH_KNOTS('',3,(#71716,#71717,#71718,#71719,#71720,
#71721,#71722,#71723,#71724,#71725,#71726,#71727,#71728,#71729,#71730,#71731),
 .UNSPECIFIED.,.F.,.F.,(4,3,3,3,3,4),(15.2092144196076,15.3360303631197,
15.4631229098697,15.5906899826816,15.6658502388533,15.707963267949),
 .UNSPECIFIED.);
#739=B_SPLINE_CURVE_WITH_KNOTS('',3,(#71732,#71733,#71734,#71735,#71736,
#71737,#71738,#71739,#71740,#71741,#71742,#71743,#71744,#71745,#71746,#71747,
#71748,#71749,#71750,#71751,#71752,#71753,#71754,#71755,#71756,#71757,#71758,
#71759,#71760,#71761,#71762,#71763,#71764,#71765,#71766,#71767,#71768,#71769,
#71770,#71771,#71772,#71773,#71774,#71775,#71776,#71777,#71778,#71779,#71780,
#71781,#71782,#71783,#71784,#71785,#71786,#71787,#71788,#71789,#71790,#71791,
#71792,#71793,#71794,#71795,#71796,#71797,#71798,#71799,#71800,#71801,#71802,
#71803,#71804,#71805,#71806,#71807,#71808,#71809,#71810,#71811,#71812,#71813,
#71814,#71815,#71816,#71817,#71818,#71819,#71820,#71821,#71822,#71823,#71824,
#71825,#71826,#71827,#71828,#71829,#71830,#71831,#71832,#71833,#71834,#71835,
#71836,#71837,#71838,#71839,#71840,#71841,#71842,#71843,#71844,#71845,#71846,
#71847,#71848,#71849,#71850,#71851,#71852,#71853,#71854,#71855,#71856,#71857,
#71858,#71859,#71860,#71861,#71862,#71863,#71864,#71865,#71866,#71867,#71868,
#71869,#71870,#71871,#71872,#71873,#71874,#71875,#71876,#71877,#71878,#71879,
#71880,#71881,#71882),.UNSPECIFIED.,.F.,.F.,(4,3,3,3,3,3,3,3,3,3,3,3,3,
3,3,3,3,3,3,3,3,3,3,3,3,3,3,3,3,3,3,3,3,3,3,3,3,3,3,3,3,3,3,3,3,3,3,3,3,
3,4),(15.7079642759245,15.8269893519292,15.9458440195906,16.0645825459371,
16.1832590062766,16.3020151623243,16.4208033607179,16.5398240072109,16.65421914787,
16.7777652614971,16.8976025282206,17.0173252415981,17.1369855788367,17.2566356083551,
17.376407960716,17.4962551100189,17.6163141716932,17.6425880568867,17.7661341705138,
17.8856871273224,18.0051210589497,18.124488751243,18.2438428753474,18.3633167375596,
18.4828635828783,18.6026226744951,18.6309569659034,18.7545030795305,18.8741702459772,
18.9937195103916,19.113203420604,19.2326744112691,19.3522652237597,19.4719291891606,
19.5918044907923,19.6193258749201,19.7428719885472,19.8625446199524,19.9820997791249,
20.1015900018609,20.2210677113655,20.3406657945147,20.4603373617903,20.5802206731859,
20.6076947839369,20.7275367997089,20.8471946066813,20.9667304809259,21.0861923026828,
21.2056842522114,21.2859961957582),.UNSPECIFIED.);
#740=B_SPLINE_CURVE_WITH_KNOTS('',3,(#71887,#71888,#71889,#71890,#71891,
#71892,#71893,#71894,#71895,#71896,#71897,#71898,#71899,#71900,#71901,#71902,
#71903,#71904,#71905,#71906,#71907,#71908,#71909,#71910,#71911,#71912,#71913,
#71914,#71915,#71916,#71917,#71918,#71919,#71920,#71921,#71922,#71923,#71924,
#71925,#71926,#71927,#71928,#71929,#71930,#71931,#71932,#71933,#71934,#71935,
#71936,#71937,#71938,#71939,#71940,#71941,#71942,#71943,#71944,#71945,#71946,
#71947,#71948,#71949,#71950,#71951,#71952,#71953,#71954,#71955,#71956,#71957,
#71958,#71959,#71960,#71961,#71962,#71963,#71964,#71965,#71966,#71967,#71968,
#71969,#71970,#71971,#71972,#71973,#71974,#71975,#71976,#71977,#71978,#71979,
#71980,#71981,#71982,#71983,#71984,#71985,#71986,#71987,#71988,#71989,#71990,
#71991,#71992,#71993,#71994,#71995,#71996,#71997,#71998,#71999,#72000,#72001,
#72002,#72003,#72004,#72005,#72006,#72007,#72008,#72009,#72010,#72011,#72012,
#72013,#72014,#72015,#72016,#72017,#72018,#72019,#72020,#72021,#72022,#72023,
#72024,#72025,#72026,#72027,#72028,#72029,#72030,#72031,#72032,#72033,#72034,
#72035,#72036,#72037,#72038,#72039,#72040,#72041,#72042,#72043,#72044,#72045,
#72046,#72047,#72048,#72049,#72050,#72051,#72052,#72053,#72054,#72055,#72056,
#72057,#72058,#72059,#72060,#72061,#72062,#72063,#72064,#72065,#72066,#72067,
#72068,#72069,#72070,#72071,#72072,#72073,#72074),.UNSPECIFIED.,.F.,.F.,
(4,2,2,2,2,2,2,2,2,2,2,2,2,2,2,2,2,2,2,2,2,2,2,2,2,2,2,2,2,2,2,2,2,2,2,
2,2,2,2,2,2,2,2,2,2,2,2,2,2,2,2,2,2,2,2,2,2,2,2,2,2,2,2,2,2,2,2,2,2,2,2,
2,2,2,2,2,2,2,2,2,2,2,2,2,2,2,2,2,2,2,2,2,2,4),(-1.60658442102956,-1.60224560786445,
-1.58703238171082,-1.5734536786702,-1.55779363519776,-1.55404776376174,
-1.55216286224401,-1.55060743210901,-1.54855577362445,-1.54389533409889,
-1.5370509807898,-1.50958833980546,-1.49965316887026,-1.49566917207978,
-1.49286872478607,-1.48994894568779,-1.48548876262572,-1.46964021552359,
-1.46491862458907,-1.44377072705897,-1.43814235132304,-1.43588239170092,
-1.43430177257987,-1.43253826107621,-1.42938893998371,-1.4115371691861,
-1.38556738688697,-1.38026768918793,-1.37714661872821,-1.37438643815279,
-1.37087330911222,-1.36335832702959,-1.35278004079731,-1.34822560070426,
-1.32739842198097,-1.32139715254891,-1.31907787404184,-1.3175030806732,
-1.31577003692568,-1.31276400765762,-1.29344874239736,-1.26892156514752,
-1.26349525637699,-1.26034708690077,-1.25761709893635,-1.25416009797896,
-1.24696597825883,-1.23702677495449,-1.22302998282919,-1.20717547508139,
-1.20341685256838,-1.20152961580493,-1.19998948005837,-1.19795050560538,
-1.19336344955988,-1.1674264216449,-1.15039868698494,-1.14578342053174,
-1.14283242100576,-1.14001913252266,-1.1361217811602,-1.12606630931722,
-1.10939123146061,-1.09016198578807,-1.08653429012839,-1.08465013995714,
-1.08309486788521,-1.08104281701865,-1.0763790917414,-1.06952757044592,
-1.04196987920764,-1.03211911150126,-1.0281480061105,-1.02535007697864,
-1.02242733268321,-1.0179511079645,-1.00185202779994,-0.996794935981721,
-0.9745544455494,-0.97005663100529,-0.968054434720027,-0.966500232781827,
-0.964603936085443,-0.960798565106953,-0.955619183957662,-0.94093791664804,
-0.918459327905157,-0.912954086788694,-0.909789115755706,-0.907034914308456,
-0.903589053834301,-0.896457126838998,-0.886639159095262,-0.864476967535523),
 .UNSPECIFIED.);
#741=B_SPLINE_CURVE_WITH_KNOTS('',3,(#72076,#72077,#72078,#72079,#72080,
#72081,#72082,#72083,#72084,#72085,#72086,#72087,#72088,#72089,#72090,#72091,
#72092,#72093,#72094),.UNSPECIFIED.,.F.,.F.,(4,3,3,3,3,3,4),(21.2859961957582,
21.4056047705331,21.525437818082,21.5960636929536,21.7289761291196,21.8610704963778,
21.9911485745023),.UNSPECIFIED.);
#742=B_SPLINE_CURVE_WITH_KNOTS('',3,(#72095,#72096,#72097,#72098,#72099,
#72100,#72101,#72102,#72103,#72104,#72105,#72106,#72107,#72108,#72109,#72110,
#72111,#72112,#72113,#72114,#72115,#72116,#72117,#72118,#72119,#72120,#72121,
#72122,#72123,#72124,#72125,#72126,#72127,#72128,#72129,#72130,#72131,#72132,
#72133,#72134,#72135,#72136,#72137,#72138,#72139,#72140,#72141,#72142,#72143,
#72144,#72145,#72146,#72147,#72148,#72149,#72150,#72151,#72152,#72153,#72154,
#72155,#72156,#72157,#72158,#72159,#72160,#72161,#72162,#72163,#72164,#72165,
#72166,#72167,#72168,#72169,#72170,#72171,#72172,#72173,#72174,#72175,#72176,
#72177,#72178,#72179,#72180,#72181,#72182,#72183,#72184,#72185,#72186,#72187,
#72188,#72189,#72190,#72191,#72192,#72193,#72194,#72195,#72196,#72197,#72198,
#72199,#72200,#72201,#72202,#72203,#72204,#72205,#72206,#72207,#72208,#72209,
#72210,#72211,#72212,#72213,#72214,#72215,#72216,#72217,#72218,#72219,#72220,
#72221,#72222,#72223,#72224,#72225,#72226,#72227,#72228,#72229,#72230,#72231,
#72232,#72233,#72234,#72235,#72236,#72237,#72238,#72239,#72240,#72241,#72242,
#72243,#72244,#72245,#72246,#72247,#72248),.UNSPECIFIED.,.F.,.F.,(4,3,3,
3,3,3,3,3,3,3,3,3,3,3,3,3,3,3,3,3,3,3,3,3,3,3,3,3,3,3,3,3,3,3,3,3,3,3,3,
3,3,3,3,3,3,3,3,3,3,3,3,4),(21.9911485751286,22.1121823813204,22.2333768389223,
22.3546485764804,22.4762007130821,22.5844326019703,22.7079787155974,22.8276354609262,
22.9471744316454,23.0666481973393,23.1861092145952,23.3056903830167,23.425344887959,
23.5452110906813,23.572801510987,23.6963476246141,23.816001439762,23.9355374275848,
24.055008163879,24.1744661113735,24.2940441733778,24.4136955472502,24.5335586139338,
24.5611704200037,24.6847165336308,24.8043720806431,24.9239098215702,25.0433823285495,
25.1628420606792,25.2824219145154,25.4020750862542,25.5219399418086,25.5495393290204,
25.6730854426475,25.7927407520977,25.9122782564462,26.0317505283277,26.1512100273392,
26.2707896527571,26.3904425986054,26.5103072341942,26.5379082380372,26.6614543516643,
26.7811093846743,26.9006466071252,27.0201185922384,27.1395778001901,27.2591571303837,
27.378809778265,27.4986741148352,27.5262771470539,27.5698739474015),
 .UNSPECIFIED.);
#743=B_SPLINE_CURVE_WITH_KNOTS('',3,(#72253,#72254,#72255,#72256,#72257,
#72258,#72259,#72260,#72261,#72262,#72263,#72264,#72265,#72266,#72267,#72268,
#72269,#72270,#72271,#72272,#72273,#72274,#72275,#72276,#72277,#72278,#72279,
#72280,#72281,#72282,#72283,#72284,#72285,#72286,#72287,#72288,#72289,#72290,
#72291,#72292,#72293,#72294,#72295,#72296,#72297,#72298,#72299,#72300,#72301,
#72302,#72303,#72304,#72305,#72306,#72307,#72308,#72309,#72310,#72311,#72312,
#72313,#72314,#72315,#72316,#72317,#72318,#72319,#72320,#72321,#72322,#72323,
#72324,#72325,#72326,#72327,#72328,#72329,#72330,#72331,#72332,#72333,#72334,
#72335,#72336,#72337,#72338,#72339,#72340,#72341,#72342,#72343,#72344,#72345,
#72346,#72347,#72348,#72349,#72350,#72351,#72352,#72353,#72354,#72355,#72356,
#72357,#72358,#72359,#72360,#72361,#72362,#72363,#72364,#72365,#72366,#72367,
#72368,#72369,#72370,#72371,#72372,#72373,#72374,#72375,#72376,#72377,#72378,
#72379,#72380,#72381,#72382,#72383,#72384,#72385,#72386,#72387,#72388,#72389,
#72390,#72391,#72392,#72393,#72394,#72395,#72396,#72397,#72398,#72399,#72400,
#72401,#72402,#72403,#72404,#72405,#72406,#72407,#72408,#72409,#72410,#72411,
#72412,#72413,#72414,#72415,#72416,#72417,#72418,#72419,#72420,#72421,#72422,
#72423,#72424,#72425,#72426,#72427,#72428,#72429,#72430,#72431,#72432,#72433,
#72434,#72435,#72436,#72437,#72438,#72439,#72440),.UNSPECIFIED.,.F.,.F.,
(4,2,2,2,2,2,2,2,2,2,2,2,2,2,2,2,2,2,2,2,2,2,2,2,2,2,2,2,2,2,2,2,2,2,2,
2,2,2,2,2,2,2,2,2,2,2,2,2,2,2,2,2,2,2,2,2,2,2,2,2,2,2,2,2,2,2,2,2,2,2,2,
2,2,2,2,2,2,2,2,2,2,2,2,2,2,2,2,2,2,2,2,2,2,4),(-2.34888331669559,-2.34746415791081,
-2.33323501160312,-2.31883357825542,-2.31447996064606,-2.31158122471084,
-2.30876529751478,-2.30534295492001,-2.29673264795989,-2.26767399338713,
-2.26070236836814,-2.25598079788759,-2.25391860690272,-2.25236218744963,
-2.25048461817488,-2.24689008239023,-2.22702347649825,-2.21075478489965,
-2.20084034995889,-2.19696105929532,-2.19415012164969,-2.19119206971483,
-2.18654543399744,-2.16838822503978,-2.14901876408084,-2.14023740420851,
-2.13766996337183,-2.13603081806866,-2.13436724699173,-2.13168561909365,
-2.12246215236684,-2.08921550586199,-2.08251215181169,-2.079143853725,-2.07665996373838,
-2.07353461166598,-2.0682163769144,-2.04238737122532,-2.02984770173124,
-2.02289939478388,-2.02052184400997,-2.0189206744297,-2.01720292774031,
-2.0142692296875,-2.00005059485172,-1.97886294912189,-1.96745217568005,
-1.96338785874221,-1.96054463947029,-1.95797827887605,-1.95452846178216,
-1.94568771125277,-1.91690388219679,-1.90995277786879,-1.9052410964534,
-1.9031806101222,-1.90162436717276,-1.89974565078447,-1.89603211724303,
-1.87774127830691,-1.86047504687243,-1.85021759831574,-1.84629323668752,
-1.84347475358181,-1.84053085849146,-1.83595321550095,-1.81985346040924,
-1.79870863276069,-1.78956971120447,-1.78697104487409,-1.78532531851077,
-1.78366900536073,-1.78102099926561,-1.77210934584716,-1.7390312587843,
-1.73197807340727,-1.72854589354364,-1.72579214161752,-1.72261617274575,
-1.71706132757492,-1.697428494358,-1.68064602341512,-1.67246658763078,-1.66995596791786,
-1.66832875544202,-1.66665124653546,-1.66390430137832,-1.65382627828294,
-1.62704668560031,-1.61648688426369,-1.61252441522423,-1.60969960464756,
-1.60676733176927,-1.60658442102956),.UNSPECIFIED.);
#744=B_SPLINE_CURVE_WITH_KNOTS('',3,(#72442,#72443,#72444,#72445,#72446,
#72447,#72448,#72449,#72450,#72451,#72452,#72453,#72454,#72455,#72456,#72457,
#72458,#72459,#72460),.UNSPECIFIED.,.F.,.F.,(4,3,3,3,3,3,4),(27.5698739474015,
27.6882231470401,27.806414976291,27.924540614238,28.0426184394307,28.1607993193961,
28.2743338823079),.UNSPECIFIED.);
#745=B_SPLINE_CURVE_WITH_KNOTS('',3,(#72461,#72462,#72463,#72464,#72465,
#72466,#72467,#72468,#72469,#72470,#72471,#72472,#72473,#72474,#72475,#72476,
#72477,#72478,#72479,#72480,#72481,#72482,#72483,#72484,#72485,#72486,#72487,
#72488,#72489,#72490,#72491,#72492,#72493,#72494,#72495,#72496,#72497,#72498,
#72499,#72500,#72501,#72502,#72503,#72504,#72505,#72506,#72507,#72508,#72509,
#72510,#72511,#72512,#72513,#72514,#72515,#72516,#72517,#72518,#72519,#72520,
#72521,#72522,#72523,#72524,#72525,#72526,#72527,#72528,#72529,#72530,#72531,
#72532,#72533,#72534,#72535,#72536,#72537,#72538,#72539,#72540,#72541,#72542,
#72543,#72544,#72545,#72546,#72547,#72548,#72549,#72550,#72551,#72552,#72553,
#72554,#72555,#72556,#72557,#72558,#72559,#72560,#72561,#72562,#72563,#72564,
#72565,#72566,#72567,#72568,#72569,#72570,#72571,#72572,#72573,#72574,#72575,
#72576,#72577,#72578,#72579,#72580,#72581,#72582,#72583,#72584,#72585,#72586,
#72587,#72588,#72589,#72590,#72591,#72592,#72593,#72594,#72595,#72596,#72597,
#72598,#72599,#72600,#72601,#72602,#72603,#72604,#72605,#72606,#72607,#72608,
#72609,#72610,#72611,#72612,#72613,#72614),.UNSPECIFIED.,.F.,.F.,(4,3,3,
3,3,3,3,3,3,3,3,3,3,3,3,3,3,3,3,3,3,3,3,3,3,3,3,3,3,3,3,3,3,3,3,3,3,3,3,
3,3,3,3,3,3,3,3,3,3,3,3,4),(28.2743338827468,28.4302483032949,28.5146460560706,
28.6381921696977,28.7578473617235,28.8773847457103,28.9968568945427,29.1163162680635,
29.2358957653182,29.3555485813052,29.4754130858408,29.5030149650873,29.6265610787144,
29.7462162465358,29.865753605776,29.985225729371,30.1046850772144,30.2242645483331,
30.3439173378884,30.4637818158228,30.491383874104,30.6149299877311,30.7345851783267,
30.8541225606624,30.9735947076261,31.0930540790636,31.2126335739322,31.3322863873531,
31.4521508890851,31.4797527831207,31.6032988967478,31.7229540808906,31.842491456729,
31.9619635971646,32.0814229620567,32.2010024504039,32.3206552573107,32.4405197526041,
32.4681216921375,32.5916678057646,32.7113229880375,32.830860361955,32.9503325004226,
33.0697918633034,33.1893713495904,33.3090241544062,33.4288886475844,33.4564906011542,
33.5763334259412,33.6960035678199,33.8155402609469,33.8531165668701),
 .UNSPECIFIED.);
#746=B_SPLINE_CURVE_WITH_KNOTS('',3,(#72619,#72620,#72621,#72622,#72623,
#72624,#72625,#72626,#72627,#72628,#72629,#72630,#72631,#72632,#72633,#72634,
#72635,#72636,#72637,#72638,#72639,#72640,#72641,#72642,#72643,#72644,#72645,
#72646,#72647,#72648,#72649,#72650,#72651,#72652,#72653,#72654,#72655,#72656,
#72657,#72658,#72659,#72660,#72661,#72662,#72663,#72664,#72665,#72666,#72667,
#72668,#72669,#72670,#72671,#72672,#72673,#72674,#72675,#72676,#72677,#72678,
#72679,#72680,#72681,#72682,#72683,#72684,#72685,#72686,#72687,#72688,#72689,
#72690,#72691,#72692,#72693,#72694,#72695,#72696,#72697,#72698,#72699,#72700,
#72701,#72702,#72703,#72704,#72705,#72706,#72707,#72708,#72709,#72710,#72711,
#72712,#72713,#72714,#72715,#72716,#72717,#72718,#72719,#72720,#72721,#72722,
#72723,#72724,#72725,#72726,#72727,#72728,#72729,#72730,#72731,#72732,#72733,
#72734,#72735,#72736,#72737,#72738,#72739,#72740,#72741,#72742,#72743,#72744,
#72745,#72746,#72747,#72748,#72749,#72750,#72751,#72752,#72753,#72754,#72755,
#72756,#72757,#72758,#72759,#72760,#72761,#72762,#72763,#72764,#72765,#72766,
#72767,#72768,#72769,#72770,#72771,#72772,#72773,#72774,#72775,#72776,#72777,
#72778,#72779,#72780,#72781,#72782,#72783,#72784,#72785,#72786,#72787,#72788,
#72789,#72790,#72791,#72792,#72793,#72794,#72795,#72796,#72797,#72798,#72799,
#72800,#72801,#72802,#72803,#72804,#72805,#72806,#72807,#72808,#72809,#72810,
#72811,#72812,#72813,#72814),.UNSPECIFIED.,.F.,.F.,(4,2,2,2,2,2,2,2,2,2,
2,2,2,2,2,2,2,2,2,2,2,2,2,2,2,2,2,2,2,2,2,2,2,2,2,2,2,2,2,2,2,2,2,2,2,2,
2,2,2,2,2,2,2,2,2,2,2,2,2,2,2,2,2,2,2,2,2,2,2,2,2,2,2,2,2,2,2,2,2,2,2,2,
2,2,2,2,2,2,2,2,2,2,2,2,2,2,2,4),(-3.09104302557684,-3.07869878069296,-3.07412504340968,
-3.07208831983924,-3.07068215664841,-3.06885526655861,-3.06549798479306,
-3.04262401148008,-3.0280981740137,-3.02175927212834,-3.01659361681389,
-3.01352909921991,-3.01075789248408,-3.00720469848718,-2.99922146495274,
-2.97399056061458,-2.96389059346649,-2.95971844085165,-2.95648392273833,
-2.95470259192764,-2.95312795377868,-2.95090658683942,-2.94555301107947,
-2.92419057452729,-2.91935931921853,-2.90876099397085,-2.90123549326599,
-2.89772054260378,-2.89496012383153,-2.89184003507607,-2.88654517357406,
-2.86050324433681,-2.84808737661496,-2.84118059236707,-2.83880815862638,
-2.83720807092551,-2.83548884548837,-2.83254766854845,-2.81797261796609,
-2.79706805317956,-2.78573137778136,-2.78167585709646,-2.77883448728534,
-2.77626699321988,-2.77281139923282,-2.7638986200414,-2.73519821507583,
-2.72825392149456,-2.72354566748474,-2.72148590315028,-2.71992987522484,
-2.71805101371321,-2.71433606945545,-2.69927560193353,-2.68636556568058,
-2.67531891311813,-2.66757506820202,-2.66402285119664,-2.66125840988038,
-2.65815994273199,-2.65283077653672,-2.62653116316866,-2.61425677167171,
-2.60739724243166,-2.60503033515024,-2.60343116695458,-2.60170978947573,
-2.59875900737969,-2.58304110008063,-2.56299801580036,-2.55189338449423,
-2.54786463471413,-2.54502794492976,-2.54211332216001,-2.537679496406,-2.52405674287668,
-2.50061017391584,-2.49106678474372,-2.48843487079744,-2.48678210911646,
-2.4853302148218,-2.48289901835696,-2.4760552473746,-2.45345968718261,-2.44189573564967,
-2.43390671610912,-2.4303137324783,-2.42754459258856,-2.42446832179646,
-2.41924754495441,-2.3920615076513,-2.38026370220506,-2.37356726627186,
-2.37122014142609,-2.36962452179197,-2.36789591906688,-2.36491160636841,
-2.34888331669559),.UNSPECIFIED.);
#747=B_SPLINE_CURVE_WITH_KNOTS('',3,(#72816,#72817,#72818,#72819,#72820,
#72821,#72822,#72823,#72824,#72825,#72826,#72827,#72828,#72829,#72830,#72831,
#72832,#72833,#72834),.UNSPECIFIED.,.F.,.F.,(4,3,3,3,3,3,4),(33.8531165668701,
33.9725797586397,34.0921356915886,34.2117312225598,34.3315652548219,34.4448595101709,
34.5575191894876),.UNSPECIFIED.);
#748=B_SPLINE_CURVE_WITH_KNOTS('',3,(#72835,#72836,#72837,#72838,#72839,
#72840,#72841,#72842,#72843,#72844,#72845,#72846,#72847,#72848,#72849,#72850,
#72851,#72852,#72853,#72854,#72855,#72856,#72857,#72858,#72859,#72860,#72861,
#72862,#72863,#72864,#72865,#72866,#72867,#72868,#72869,#72870,#72871,#72872,
#72873,#72874,#72875,#72876,#72877,#72878,#72879,#72880,#72881,#72882,#72883,
#72884,#72885,#72886,#72887,#72888,#72889,#72890,#72891,#72892,#72893,#72894,
#72895,#72896,#72897,#72898,#72899,#72900,#72901,#72902,#72903,#72904,#72905,
#72906,#72907,#72908,#72909,#72910,#72911,#72912,#72913,#72914,#72915,#72916,
#72917,#72918,#72919,#72920,#72921,#72922,#72923,#72924,#72925,#72926,#72927,
#72928,#72929,#72930,#72931,#72932,#72933,#72934,#72935,#72936,#72937,#72938,
#72939,#72940,#72941,#72942,#72943,#72944,#72945,#72946,#72947,#72948,#72949,
#72950,#72951,#72952,#72953,#72954,#72955,#72956,#72957,#72958,#72959,#72960,
#72961,#72962,#72963,#72964,#72965,#72966,#72967,#72968,#72969,#72970,#72971,
#72972,#72973,#72974,#72975,#72976,#72977,#72978,#72979,#72980,#72981,#72982,
#72983,#72984,#72985,#72986,#72987,#72988),.UNSPECIFIED.,.F.,.F.,(4,3,3,
3,3,3,3,3,3,3,3,3,3,3,3,3,3,3,3,3,3,3,3,3,3,3,3,3,3,3,3,3,3,3,3,3,3,3,3,
3,3,3,3,3,3,3,3,3,3,3,3,4),(34.55751919,34.675703821994,34.7937403930487,
34.9116842733924,35.0295906618769,35.1475953577675,35.265656218042,35.3839289477292,
35.4332284191876,35.5567745328147,35.6764297165833,35.7959670920215,35.9154392320316,
36.0348985964736,36.1544780843377,36.2741308907417,36.3939953855082,36.4215973282043,
36.5451434418314,36.6647986258637,36.7843360015699,36.9038081418515,37.0232675065683,
37.1428469947097,37.2624998013925,37.3823642964378,37.409966237221,37.5335123508481,
37.6531675347659,37.7727049103562,37.8921770505211,38.0116364151202,38.1312159031439,
38.2508687097089,38.3707332046372,38.3983351462378,38.5218812598649,38.6415364437821,
38.7610738193715,38.8805459595352,39.000005324133,39.1195848121547,39.2392376187173,
39.3591021136428,39.3867040552545,39.5065507243149,39.6262160664111,39.7457528850742,
39.8652414842152,39.9847042607615,40.1042406011651,40.1354661882622),
 .UNSPECIFIED.);
#749=B_SPLINE_CURVE_WITH_KNOTS('',3,(#72994,#72995,#72996,#72997,#72998,
#72999,#73000,#73001,#73002,#73003,#73004,#73005,#73006,#73007,#73008,#73009,
#73010,#73011,#73012,#73013,#73014,#73015,#73016,#73017,#73018,#73019,#73020,
#73021,#73022,#73023,#73024,#73025,#73026,#73027,#73028,#73029,#73030,#73031,
#73032,#73033,#73034,#73035,#73036,#73037,#73038,#73039,#73040,#73041,#73042,
#73043,#73044,#73045,#73046,#73047,#73048,#73049,#73050,#73051,#73052,#73053,
#73054,#73055,#73056,#73057,#73058,#73059,#73060,#73061,#73062,#73063,#73064,
#73065,#73066,#73067,#73068,#73069,#73070,#73071,#73072,#73073,#73074,#73075,
#73076,#73077,#73078,#73079,#73080,#73081,#73082,#73083,#73084,#73085,#73086,
#73087,#73088,#73089,#73090,#73091,#73092,#73093,#73094,#73095,#73096,#73097,
#73098,#73099,#73100,#73101,#73102,#73103,#73104,#73105,#73106,#73107,#73108,
#73109,#73110,#73111,#73112,#73113,#73114,#73115,#73116,#73117,#73118,#73119,
#73120,#73121,#73122,#73123,#73124,#73125,#73126,#73127,#73128,#73129,#73130,
#73131,#73132,#73133,#73134,#73135,#73136,#73137,#73138,#73139,#73140,#73141,
#73142,#73143,#73144,#73145,#73146,#73147,#73148,#73149,#73150,#73151,#73152,
#73153,#73154,#73155,#73156,#73157,#73158,#73159,#73160,#73161,#73162,#73163,
#73164,#73165,#73166,#73167,#73168,#73169,#73170,#73171),.UNSPECIFIED.,
 .F.,.F.,(4,2,2,2,2,2,2,2,2,2,2,2,2,2,2,2,2,2,2,2,2,2,2,2,2,2,2,2,2,2,2,
2,2,2,2,2,2,2,2,2,2,2,2,2,2,2,2,2,2,2,2,2,2,2,2,2,2,2,2,2,2,2,2,2,2,2,2,
2,2,2,2,2,2,2,2,2,2,2,2,2,2,2,2,2,2,2,2,2,4),(-0.659092247150748,-0.657847337165459,
-0.655117324673011,-0.65166110052353,-0.644471813353595,-0.63454222140134,
-0.62053307279676,-0.604672714135786,-0.600913572830821,-0.599026192226777,
-0.597486005894416,-0.595447050537588,-0.590860376322777,-0.564932054450223,
-0.547893993018436,-0.543278235310928,-0.540327061979064,-0.53751370605405,
-0.53361642252045,-0.523562176068924,-0.506891094712074,-0.48765388920764,
-0.484026385933713,-0.482142235428155,-0.480586905160501,-0.478534701890131,
-0.473870318637051,-0.467017533005013,-0.439446449898104,-0.429605580366987,
-0.425635873237102,-0.42283811613999,-0.419914856274393,-0.415436408075053,
-0.399304690616214,-0.394388719380452,-0.372340388808994,-0.368089572832143,
-0.365847938672911,-0.36427030973432,-0.362498727035257,-0.359310560306125,
-0.355217272983698,-0.345425935937014,-0.315799574579589,-0.310366274793167,
-0.307216738613679,-0.304487124135408,-0.301032662642798,-0.293852047114042,
-0.283938994344236,-0.269912783892604,-0.254045872222858,-0.250286522225629,
-0.248399219286063,-0.246859201201512,-0.244820604207227,-0.240235270568493,
-0.214324914418814,-0.197273095786802,-0.192657296110063,-0.189706319921042,
-0.186893308904515,-0.182996760882585,-0.172946090052386,-0.156284068821107,
-0.137037260742728,-0.133410648173939,-0.131526798691344,-0.129971617569289,
-0.127919481821253,-0.123254734520903,-0.116400908893694,-0.0888112863161954,
-0.0789893013279216,-0.0750226842041575,-0.0722256779482118,-0.0693019805793304,
-0.0648203378049058,-0.0486333330234812,-0.0374569332473158,-0.0208126834134555,
-0.0167378495564204,-0.0147905127745936,-0.0132386998545472,-0.0117300280505381,
-0.00975889164009274,-0.00612376957510279,-0.000334755479537651),
 .UNSPECIFIED.);
#750=B_SPLINE_CURVE_WITH_KNOTS('',3,(#73172,#73173,#73174,#73175,#73176,
#73177,#73178,#73179,#73180,#73181,#73182,#73183,#73184,#73185,#73186,#73187,
#73188,#73189),.UNSPECIFIED.,.F.,.F.,(4,2,2,2,2,2,2,2,4),(-3.17436405700199,
-3.14598172734965,-3.13597100235351,-3.1320797025494,-3.12926746014941,
-3.12631460486497,-3.1216901755824,-3.10439275289458,-3.09104302557684),
 .UNSPECIFIED.);
#751=B_SPLINE_CURVE_WITH_KNOTS('',3,(#73191,#73192,#73193,#73194,#73195,
#73196,#73197,#73198,#73199,#73200,#73201,#73202,#73203,#73204,#73205,#73206,
#73207,#73208,#73209),.UNSPECIFIED.,.F.,.F.,(4,3,3,3,3,3,4),(40.1354661882622,
40.2552991262847,40.3750729642712,40.5025546826919,40.6297310288095,40.756488685127,
40.8407044962357),.UNSPECIFIED.);
#752=B_SPLINE_CURVE_WITH_KNOTS('',3,(#73210,#73211,#73212,#73213,#73214,
#73215,#73216,#73217,#73218,#73219,#73220,#73221,#73222,#73223,#73224,#73225,
#73226,#73227,#73228,#73229,#73230,#73231,#73232,#73233,#73234,#73235,#73236,
#73237,#73238,#73239,#73240,#73241,#73242,#73243,#73244,#73245,#73246,#73247,
#73248,#73249,#73250,#73251,#73252,#73253,#73254,#73255,#73256,#73257,#73258,
#73259,#73260,#73261,#73262,#73263,#73264,#73265,#73266,#73267,#73268,#73269,
#73270,#73271,#73272,#73273,#73274,#73275,#73276,#73277,#73278,#73279,#73280,
#73281,#73282,#73283,#73284,#73285,#73286,#73287,#73288,#73289,#73290,#73291,
#73292,#73293,#73294,#73295,#73296,#73297,#73298,#73299,#73300,#73301,#73302,
#73303,#73304,#73305,#73306,#73307,#73308,#73309,#73310,#73311,#73312,#73313,
#73314,#73315,#73316,#73317,#73318,#73319,#73320,#73321,#73322,#73323,#73324,
#73325,#73326,#73327,#73328,#73329,#73330,#73331,#73332,#73333,#73334,#73335,
#73336,#73337,#73338,#73339,#73340,#73341,#73342,#73343,#73344,#73345,#73346,
#73347,#73348,#73349,#73350,#73351,#73352,#73353,#73354,#73355,#73356,#73357,
#73358,#73359,#73360,#73361,#73362,#73363),.UNSPECIFIED.,.F.,.F.,(4,3,3,
3,3,3,3,3,3,3,3,3,3,3,3,3,3,3,3,3,3,3,3,3,3,3,3,3,3,3,3,3,3,3,3,3,3,3,3,
3,3,3,3,3,3,3,3,3,3,3,3,4),(40.8407044966672,40.9643627484298,41.0883098175793,
41.2124204083489,41.3368376192527,41.3634418732879,41.486987986915,41.6066431708463,
41.7261805464501,41.8456526866283,41.965112051241,42.0846915392776,42.2043443458554,
42.3242088407961,42.3518107823046,42.4753568959317,42.5950120798656,42.714549455472,
42.8340215956529,42.9534809602682,43.0730604483076,43.1927132548881,43.3125777498315,
43.3401796913213,43.4637258049484,43.5833809888806,43.7029183644854,43.8223905046646,
43.9418498692783,44.0614293573159,44.1810821638947,44.3009466588365,44.3285486003381,
44.4520947139652,44.5717498978977,44.6912872735026,44.8107594136822,44.9302187782958,
45.0497982663337,45.1694510729129,45.289315567855,45.3169175093548,45.4404636229819,
45.5601188069146,45.6796561825198,45.7991283226996,45.9185876873136,46.0381671753518,
46.1578199819315,46.2776844768739,46.3052864183715,46.4196372410064),
 .UNSPECIFIED.);
#753=B_SPLINE_CURVE_WITH_KNOTS('',3,(#73368,#73369,#73370,#73371,#73372,
#73373,#73374,#73375,#73376,#73377,#73378,#73379,#73380,#73381,#73382,#73383,
#73384,#73385,#73386,#73387,#73388,#73389,#73390,#73391,#73392,#73393,#73394,
#73395,#73396,#73397,#73398,#73399,#73400,#73401,#73402,#73403,#73404,#73405,
#73406,#73407,#73408,#73409,#73410,#73411,#73412,#73413,#73414,#73415,#73416,
#73417,#73418,#73419,#73420,#73421,#73422,#73423,#73424,#73425,#73426,#73427,
#73428,#73429,#73430,#73431,#73432,#73433,#73434,#73435,#73436,#73437,#73438,
#73439,#73440,#73441,#73442,#73443,#73444,#73445,#73446,#73447,#73448,#73449,
#73450,#73451,#73452,#73453,#73454,#73455,#73456,#73457,#73458,#73459,#73460,
#73461,#73462,#73463,#73464,#73465,#73466,#73467,#73468,#73469,#73470,#73471,
#73472,#73473,#73474,#73475,#73476,#73477,#73478,#73479,#73480,#73481,#73482,
#73483,#73484,#73485,#73486,#73487,#73488,#73489,#73490,#73491,#73492,#73493,
#73494,#73495,#73496,#73497,#73498,#73499,#73500,#73501,#73502,#73503,#73504,
#73505,#73506,#73507,#73508,#73509,#73510,#73511,#73512,#73513,#73514,#73515,
#73516,#73517,#73518,#73519,#73520,#73521,#73522,#73523,#73524,#73525,#73526,
#73527,#73528,#73529,#73530,#73531,#73532,#73533,#73534,#73535,#73536,#73537,
#73538,#73539,#73540,#73541,#73542,#73543),.UNSPECIFIED.,.F.,.F.,(4,2,2,
2,2,2,2,2,2,2,2,2,2,2,2,2,2,2,2,2,2,2,2,2,2,2,2,2,2,2,2,2,2,2,2,2,2,2,2,
2,2,2,2,2,2,2,2,2,2,2,2,2,2,2,2,2,2,2,2,2,2,2,2,2,2,2,2,2,2,2,2,2,2,2,2,
2,2,2,2,2,2,2,2,2,2,2,2,4),(-1.40166030916385,-1.37074872889547,-1.3636355541024,
-1.36019165817904,-1.35746122843946,-1.35430060238847,-1.34882185197481,
-1.32518254109912,-1.31127029750981,-1.30388514246043,-1.30145681422145,
-1.29984551946185,-1.29835559220305,-1.2957228104434,-1.2869965045143,-1.25377252721205,
-1.24666060403705,-1.24321716387714,-1.2404870327011,-1.23732668258277,
-1.23184822887434,-1.20821893014021,-1.19430311750791,-1.18691721660821,
-1.18448897746441,-1.18287782180291,-1.1813880928463,-1.17875579423015,
-1.17003276639959,-1.13681063724061,-1.12969878395935,-1.12625558837016,
-1.12352573916631,-1.12036581318139,-1.11488834943471,-1.0912510841642,
-1.07734384068059,-1.06996087918445,-1.0675331380666,-1.06592220078658,
-1.06443257611345,-1.06180027575788,-1.05307489220482,-1.01985869540226,
-1.01274856860719,-1.00930591358912,-1.006576369543,-1.00341665982202,-0.997939213915288,
-0.974319198894698,-0.960403498097602,-0.953018306682525,-0.950590489948238,
-0.948979659799876,-0.947490271238418,-0.94485864915994,-0.936138811395806,
-0.902922817532087,-0.895812093640249,-0.892369563957432,-0.889640292474709,
-0.886481090461841,-0.881005025615726,-0.857366915098181,-0.843466620408091,
-0.836086444308368,-0.83365935594194,-0.832048788812946,-0.830559451536752,
-0.827927554475934,-0.819202186325314,-0.785994425378115,-0.778886361423134,
-0.775444539068679,-0.772690334038145,-0.769521822841325,-0.764001148159297,
-0.742256424281249,-0.721251916090213,-0.717734189210468,-0.715872944427697,
-0.714314887116222,-0.712230601003129,-0.707374781410603,-0.700120614599103,
-0.666425615302329,-0.660996237232752,-0.659092247150748),.UNSPECIFIED.);
#754=B_SPLINE_CURVE_WITH_KNOTS('',3,(#73545,#73546,#73547,#73548,#73549,
#73550,#73551,#73552,#73553,#73554,#73555,#73556,#73557,#73558,#73559,#73560,
#73561,#73562,#73563),.UNSPECIFIED.,.F.,.F.,(4,3,3,3,3,3,4),(46.4196372410064,
46.5375477121673,46.6553395633796,46.773127793545,46.8909019183037,47.0088381638724,
47.1238898031507),.UNSPECIFIED.);
#755=B_SPLINE_CURVE_WITH_KNOTS('',3,(#73564,#73565,#73566,#73567,#73568,
#73569,#73570,#73571,#73572,#73573,#73574,#73575,#73576,#73577,#73578,#73579,
#73580,#73581,#73582,#73583,#73584,#73585,#73586,#73587,#73588,#73589,#73590,
#73591,#73592,#73593,#73594,#73595,#73596,#73597,#73598,#73599,#73600,#73601,
#73602,#73603,#73604,#73605,#73606,#73607,#73608,#73609,#73610,#73611,#73612,
#73613,#73614,#73615,#73616,#73617,#73618,#73619,#73620,#73621,#73622,#73623,
#73624,#73625,#73626,#73627,#73628,#73629,#73630,#73631,#73632,#73633,#73634,
#73635,#73636,#73637,#73638,#73639,#73640,#73641,#73642,#73643,#73644,#73645,
#73646,#73647,#73648,#73649,#73650,#73651,#73652,#73653,#73654,#73655,#73656,
#73657,#73658,#73659,#73660,#73661,#73662,#73663,#73664,#73665,#73666,#73667,
#73668,#73669,#73670,#73671,#73672,#73673,#73674,#73675,#73676,#73677,#73678,
#73679,#73680,#73681,#73682,#73683,#73684,#73685,#73686,#73687,#73688,#73689,
#73690,#73691,#73692,#73693,#73694,#73695,#73696,#73697,#73698,#73699,#73700,
#73701,#73702,#73703,#73704,#73705,#73706,#73707,#73708,#73709,#73710,#73711,
#73712,#73713,#73714),.UNSPECIFIED.,.F.,.F.,(4,3,3,3,3,3,3,3,3,3,3,3,3,
3,3,3,3,3,3,3,3,3,3,3,3,3,3,3,3,3,3,3,3,3,3,3,3,3,3,3,3,3,3,3,3,3,3,3,3,
3,4),(47.1238898038469,47.2936553273882,47.4172014410153,47.5368566249479,
47.656394000553,47.7758661407327,47.8953255053465,48.0149049933845,48.1345577999637,
48.2544222949058,48.2820242364049,48.405570350032,48.5252255339646,48.6447629095697,
48.7642350497494,48.8836944143633,49.0032739024013,49.1229267089805,49.2427912039227,
49.2703931454216,49.3939392590487,49.5135944429813,49.6331318185864,49.752603958766,
49.8720633233799,49.991642811418,50.1112956179972,50.2311601129393,50.2587620544383,
50.3823081680654,50.501963351998,50.6215007276031,50.7409728677827,50.8604322323966,
50.9800117204346,51.0996645270139,51.219529021956,51.2471309634551,51.3706770770822,
51.4903322610148,51.6098696366199,51.7293417767995,51.8488011414135,51.9683806294515,
52.0880334360308,52.2078979309729,52.2354998724718,52.355333838859,52.4749962045213,
52.5945469089048,52.7024741778816),.UNSPECIFIED.);
#756=B_SPLINE_CURVE_WITH_KNOTS('',3,(#73720,#73721,#73722,#73723,#73724,
#73725,#73726,#73727,#73728,#73729,#73730,#73731,#73732,#73733,#73734,#73735,
#73736,#73737,#73738,#73739,#73740,#73741,#73742,#73743,#73744,#73745,#73746,
#73747,#73748,#73749,#73750,#73751,#73752,#73753,#73754,#73755,#73756,#73757,
#73758,#73759,#73760,#73761,#73762,#73763,#73764,#73765,#73766,#73767,#73768,
#73769,#73770,#73771,#73772,#73773,#73774,#73775,#73776,#73777,#73778,#73779,
#73780,#73781,#73782,#73783,#73784,#73785,#73786,#73787,#73788,#73789,#73790,
#73791,#73792,#73793,#73794,#73795,#73796,#73797,#73798,#73799,#73800,#73801,
#73802,#73803,#73804,#73805,#73806,#73807,#73808,#73809,#73810,#73811,#73812,
#73813,#73814,#73815,#73816,#73817,#73818,#73819,#73820,#73821,#73822,#73823,
#73824,#73825,#73826,#73827,#73828,#73829,#73830,#73831,#73832,#73833,#73834,
#73835,#73836,#73837,#73838,#73839,#73840,#73841,#73842,#73843,#73844,#73845,
#73846,#73847,#73848,#73849,#73850,#73851,#73852,#73853,#73854,#73855,#73856,
#73857,#73858,#73859,#73860,#73861,#73862,#73863,#73864,#73865,#73866,#73867,
#73868,#73869,#73870,#73871,#73872,#73873,#73874,#73875,#73876,#73877,#73878,
#73879,#73880,#73881),.UNSPECIFIED.,.F.,.F.,(4,2,2,2,2,2,2,2,2,2,2,2,2,
2,2,2,2,2,2,2,2,2,2,2,2,2,2,2,2,2,2,2,2,2,2,2,2,2,2,2,2,2,2,2,2,2,2,2,2,
2,2,2,2,2,2,2,2,2,2,2,2,2,2,2,2,2,2,2,2,2,2,2,2,2,2,2,2,2,2,2,4),(-0.658976676139878,
-0.647559402944162,-0.637927955387454,-0.635212731971702,-0.63354277089442,
-0.631911429201569,-0.629377370601124,-0.620942458873841,-0.603098942762448,
-0.583272956277358,-0.578527048138876,-0.575550129005866,-0.572751425594615,
-0.56893724197842,-0.559483638379049,-0.544457139694901,-0.52251619138621,
-0.519057656415479,-0.517209586673753,-0.515665535348846,-0.513574049582365,
-0.508669836456843,-0.50131056459068,-0.474302815240831,-0.464695293598529,
-0.460760082909462,-0.457969203304208,-0.455038070071776,-0.450516166955131,
-0.433647955426323,-0.412767864189028,-0.404113671448546,-0.401488938447733,
-0.400001601301243,-0.398391108095587,-0.395960827919078,-0.388542165799128,
-0.37450773680041,-0.351120645350932,-0.345640890748171,-0.342482130135672,
-0.339754700192193,-0.336316412085633,-0.329222161378755,-0.296045771902395,
-0.287279273822127,-0.284644595690969,-0.282991774699758,-0.281344520600445,
-0.278735867794029,-0.269464638098045,-0.247581486561486,-0.232322135022478,
-0.22779876784903,-0.22486702568353,-0.222043860556855,-0.218085625133857,
-0.207551564710205,-0.178245401026454,-0.170279900333843,-0.167718353155734,
-0.166242919825262,-0.164620654983839,-0.162132366470803,-0.15416915973964,
-0.138213785211149,-0.117498585330046,-0.111966962519322,-0.108796677554783,
-0.106043495548194,-0.102606319690159,-0.0955210762894671,-0.0623627300998356,
-0.0535584119753678,-0.0509200626184618,-0.0492662023159992,-0.0476192065506048,
-0.045012939858365,-0.0357753380878062,-0.0198319199248591,-0.000335325052894208),
 .UNSPECIFIED.);
#757=B_SPLINE_CURVE_WITH_KNOTS('',3,(#73882,#73883,#73884,#73885,#73886,
#73887,#73888,#73889,#73890,#73891,#73892,#73893,#73894,#73895,#73896,#73897,
#73898,#73899,#73900,#73901,#73902,#73903,#73904,#73905,#73906,#73907,#73908,
#73909,#73910,#73911,#73912,#73913),.UNSPECIFIED.,.F.,.F.,(4,2,2,2,2,2,
2,2,2,2,2,2,2,2,2,4),(-1.48497886615627,-1.4804211924715,-1.47768304987249,
-1.47504991531636,-1.47243836288595,-1.46807733810784,-1.45459659168007,
-1.44217058245323,-1.4282532491641,-1.42086621108752,-1.41843750201499,
-1.41682601157226,-1.41533595304441,-1.41270303395089,-1.40397746823474,
-1.40166030916385),.UNSPECIFIED.);
#758=B_SPLINE_CURVE_WITH_KNOTS('',3,(#73915,#73916,#73917,#73918,#73919,
#73920,#73921,#73922,#73923,#73924,#73925,#73926,#73927,#73928,#73929,#73930,
#73931,#73932,#73933),.UNSPECIFIED.,.F.,.F.,(4,3,3,3,3,3,4),(52.7024741778816,
52.8219322553359,52.9415057835748,53.0611466250366,53.1810035178623,53.2238687814885,
53.4070751110266),.UNSPECIFIED.);
#759=B_SPLINE_CURVE_WITH_KNOTS('',3,(#73934,#73935,#73936,#73937,#73938,
#73939,#73940,#73941,#73942),.UNSPECIFIED.,.F.,.F.,(4,1,1,1,1,1,4),(53.4070796080658,
54.2122376905052,55.2006065995219,56.1889755085386,57.1773444175554,58.1657133265721,
58.98478654205),.UNSPECIFIED.);
#760=B_SPLINE_CURVE_WITH_KNOTS('',3,(#73947,#73948,#73949,#73950,#73951,
#73952,#73953,#73954,#73955,#73956,#73957,#73958,#73959,#73960,#73961,#73962,
#73963,#73964,#73965,#73966,#73967,#73968,#73969,#73970,#73971,#73972,#73973,
#73974,#73975,#73976,#73977,#73978,#73979,#73980,#73981,#73982,#73983,#73984,
#73985,#73986,#73987,#73988,#73989,#73990,#73991,#73992,#73993,#73994,#73995,
#73996,#73997,#73998,#73999,#74000,#74001,#74002,#74003,#74004,#74005,#74006,
#74007,#74008,#74009,#74010,#74011,#74012,#74013,#74014,#74015,#74016,#74017,
#74018,#74019,#74020,#74021,#74022,#74023,#74024,#74025,#74026,#74027,#74028,
#74029,#74030,#74031,#74032,#74033,#74034,#74035,#74036,#74037,#74038,#74039,
#74040,#74041,#74042,#74043,#74044,#74045,#74046,#74047,#74048,#74049,#74050,
#74051,#74052,#74053,#74054,#74055,#74056,#74057,#74058,#74059,#74060,#74061,
#74062,#74063,#74064,#74065,#74066,#74067,#74068,#74069,#74070,#74071,#74072,
#74073,#74074,#74075,#74076,#74077,#74078,#74079,#74080,#74081,#74082,#74083,
#74084,#74085,#74086,#74087,#74088,#74089,#74090,#74091,#74092,#74093,#74094,
#74095,#74096,#74097,#74098,#74099,#74100,#74101,#74102,#74103,#74104,#74105,
#74106,#74107,#74108,#74109,#74110,#74111,#74112,#74113,#74114,#74115,#74116,
#74117,#74118,#74119,#74120,#74121,#74122,#74123,#74124,#74125,#74126,#74127,
#74128,#74129,#74130,#74131,#74132,#74133,#74134,#74135,#74136,#74137,#74138,
#74139,#74140,#74141,#74142,#74143,#74144,#74145,#74146,#74147,#74148,#74149,
#74150,#74151,#74152,#74153,#74154),.UNSPECIFIED.,.F.,.F.,(4,2,2,2,2,2,
2,2,2,2,2,2,2,2,2,2,2,2,2,2,2,2,2,2,2,2,2,2,2,2,2,2,2,2,2,2,2,2,2,2,2,2,
2,2,2,2,2,2,2,2,2,2,2,2,2,2,2,2,2,2,2,2,2,2,2,2,2,2,2,2,2,2,2,2,2,2,2,2,
2,2,2,2,2,2,2,2,2,2,2,2,2,2,2,2,2,2,2,2,2,2,2,2,2,4),(-1.40060990531413,
-1.40037382044156,-1.39599762339415,-1.39575014915383,-1.39549983618132,
-1.39524186425832,-1.39516781273781,-1.39505951916284,-1.39489267534928,
-1.39461066040855,-1.391847860589,-1.38875732348354,-1.38345759566904,-1.35708953943928,
-1.34486077766074,-1.33801921058626,-1.33565591630552,-1.33405850864429,
-1.33233826489298,-1.32938798604826,-1.31324310260407,-1.30028806780615,
-1.28363297625614,-1.27912507054162,-1.27619739954667,-1.27340585518658,
-1.26946293789873,-1.25979633343448,-1.23202932454018,-1.2251617019475,
-1.22049151812755,-1.21843925448782,-1.21688497266861,-1.21500340595402,
-1.21126965979811,-1.19577217506231,-1.18250816094592,-1.16673162330973,
-1.16227931564973,-1.15936273881688,-1.15656395137175,-1.15257987465595,
-1.14263109077572,-1.11617567805781,-1.108752560566,-1.10381934049315,-1.10172341948776,
-1.10016536994534,-1.0983146323749,-1.09484236522338,-1.07317886049711,
-1.05800997387861,-1.04850268178769,-1.04468155758812,-1.04188219612432,
-1.03890861504133,-1.03417698814248,-1.01441705704065,-0.996487009525404,
-0.988031896282643,-0.985496169880248,-0.983864709844933,-0.982399085711126,
-0.979887372692515,-0.972372504022307,-0.950459221245068,-0.939018778799972,
-0.931089847324866,-0.927508715300317,-0.924743000140185,-0.921664744636298,
-0.916425885117246,-0.885594270838664,-0.876285131506364,-0.872318696963878,
-0.869206742945008,-0.867451871419008,-0.865869548480569,-0.86395344603747,
-0.859248924877213,-0.834431670681573,-0.822515504419465,-0.814365700373937,
-0.810748355721052,-0.807978054468326,-0.804918124638505,-0.799769184076685,
-0.768524176491352,-0.759369992386026,-0.755444718228545,-0.752357352827093,
-0.750607575485915,-0.74902301711675,-0.747097527128348,-0.742222305069737,
-0.734736854557467,-0.706522372836859,-0.697969709706433,-0.694557648814438,
-0.69174568931771,-0.688846522420659,-0.684483322910936,-0.669936264616971,
-0.658976676139878),.UNSPECIFIED.);
#761=B_SPLINE_CURVE_WITH_KNOTS('',3,(#74156,#74157,#74158,#74159,#74160),
 .UNSPECIFIED.,.F.,.F.,(4,1,4),(58.98478654205,59.1540822355888,59.6902604182062),
 .UNSPECIFIED.);
#762=B_SPLINE_CURVE_WITH_KNOTS('',3,(#74161,#74162,#74163,#74164,#74165,
#74166,#74167,#74168,#74169,#74170,#74171,#74172,#74173,#74174,#74175,#74176,
#74177,#74178,#74179,#74180,#74181,#74182,#74183,#74184,#74185,#74186,#74187,
#74188,#74189,#74190,#74191,#74192,#74193,#74194,#74195,#74196,#74197,#74198,
#74199,#74200,#74201,#74202,#74203,#74204,#74205,#74206,#74207,#74208,#74209,
#74210,#74211,#74212,#74213,#74214,#74215,#74216,#74217,#74218,#74219,#74220,
#74221,#74222,#74223,#74224,#74225,#74226,#74227,#74228,#74229,#74230,#74231,
#74232,#74233,#74234,#74235,#74236,#74237,#74238,#74239,#74240,#74241,#74242,
#74243,#74244,#74245,#74246,#74247,#74248,#74249,#74250,#74251,#74252,#74253,
#74254,#74255,#74256,#74257,#74258,#74259,#74260,#74261,#74262,#74263,#74264,
#74265,#74266,#74267,#74268,#74269,#74270,#74271,#74272,#74273,#74274,#74275,
#74276,#74277,#74278,#74279,#74280,#74281,#74282,#74283,#74284,#74285,#74286,
#74287,#74288,#74289,#74290,#74291,#74292,#74293,#74294,#74295,#74296,#74297,
#74298,#74299,#74300,#74301,#74302,#74303,#74304,#74305,#74306,#74307,#74308,
#74309,#74310,#74311,#74312,#74313,#74314),.UNSPECIFIED.,.F.,.F.,(4,3,3,
3,3,3,3,3,3,3,3,3,3,3,3,3,3,3,3,3,3,3,3,3,3,3,3,3,3,3,3,3,3,3,3,3,3,3,3,
3,3,3,3,3,3,3,3,3,3,3,3,4),(59.6902604182062,59.8178925384765,59.9458188551941,
60.07422224745,60.1424511446055,60.2659972582326,60.3856524421651,60.5051898177701,
60.6246619579496,60.7441213225634,60.8637008106013,60.9833536171804,61.1032181121225,
61.1308200536222,61.2543661672493,61.3740213511815,61.4935587267862,61.6130308669655,
61.7324902315789,61.8520697196166,61.9717225261954,62.0915870211372,62.119188962639,
62.2427350762661,62.3623902602,62.4819276358065,62.6013997759875,62.7208591406027,
62.840438628642,62.9600914352225,63.0799559301659,63.1075578716557,63.2311039852828,
63.3507591692139,63.4702965448176,63.5897686849959,63.7092280496084,63.8288075376451,
63.948460344223,64.0683248391639,64.0959267806724,64.2194728942995,64.3391280782295,
64.458665453832,64.578137594009,64.6975969586204,64.8171764466558,64.9368292532324,
65.056693748172,65.0842956896891,65.2026640796911,65.2692561001133),
 .UNSPECIFIED.);
#763=B_SPLINE_CURVE_WITH_KNOTS('',3,(#74320,#74321,#74322,#74323,#74324,
#74325,#74326,#74327,#74328,#74329,#74330,#74331,#74332,#74333,#74334,#74335,
#74336,#74337,#74338,#74339,#74340,#74341,#74342,#74343,#74344,#74345,#74346,
#74347,#74348,#74349,#74350,#74351,#74352,#74353,#74354,#74355,#74356,#74357,
#74358,#74359,#74360,#74361,#74362,#74363,#74364,#74365,#74366,#74367,#74368,
#74369,#74370,#74371,#74372,#74373,#74374,#74375,#74376,#74377,#74378,#74379,
#74380,#74381,#74382,#74383,#74384,#74385,#74386,#74387,#74388,#74389,#74390,
#74391,#74392,#74393,#74394,#74395,#74396,#74397,#74398,#74399,#74400,#74401,
#74402,#74403,#74404,#74405,#74406,#74407,#74408,#74409,#74410,#74411,#74412,
#74413,#74414,#74415,#74416,#74417,#74418,#74419,#74420,#74421,#74422,#74423,
#74424,#74425,#74426,#74427,#74428,#74429,#74430,#74431,#74432,#74433,#74434,
#74435,#74436,#74437,#74438,#74439,#74440,#74441,#74442,#74443,#74444,#74445,
#74446,#74447,#74448,#74449,#74450,#74451,#74452,#74453,#74454,#74455,#74456,
#74457,#74458,#74459,#74460,#74461,#74462,#74463,#74464,#74465,#74466,#74467,
#74468,#74469,#74470,#74471,#74472,#74473,#74474,#74475,#74476,#74477,#74478,
#74479,#74480,#74481,#74482,#74483,#74484,#74485,#74486,#74487,#74488,#74489,
#74490,#74491,#74492,#74493),.UNSPECIFIED.,.F.,.F.,(4,2,2,2,2,2,2,2,2,2,
2,2,2,2,2,2,2,2,2,2,2,2,2,2,2,2,2,2,2,2,2,2,2,2,2,2,2,2,2,2,2,2,2,2,2,2,
2,2,2,2,2,2,2,2,2,2,2,2,2,2,2,2,2,2,2,2,2,2,2,2,2,2,2,2,2,2,2,2,2,2,2,2,
2,2,2,2,4),(-0.659264417620488,-0.658306668539297,-0.645960048448501,-0.61982461602658,
-0.614480758731446,-0.611379560346641,-0.608616074379269,-0.605069816617077,
-0.597359875485747,-0.586381773310217,-0.573396687769836,-0.558275719414295,
-0.55455810877067,-0.55267886559312,-0.551123078322035,-0.549064391818707,
-0.544361546636229,-0.537428919706541,-0.508841969400668,-0.499844679485265,
-0.496383326405695,-0.493814681747486,-0.490975095378717,-0.486928206583286,
-0.475665123989059,-0.455040104275854,-0.440080751097174,-0.437133901566631,
-0.435413564555328,-0.433814276145509,-0.43144568631414,-0.424569465088856,
-0.412244386001662,-0.386071865031164,-0.380732430853882,-0.377632204285496,
-0.374868647312202,-0.371320993230495,-0.363602330709988,-0.352605978667221,
-0.339642846793759,-0.324531966155127,-0.320814893554997,-0.318935793468338,
-0.317380048331269,-0.315321318398518,-0.310617973524586,-0.303684215060326,
-0.275080294815655,-0.26610001569161,-0.262640009980384,-0.260071734880583,
-0.25723194005492,-0.253183536014559,-0.24190660401442,-0.221228980428054,
-0.206339977461716,-0.203393986108559,-0.201673867861735,-0.200074544553195,
-0.197705563126124,-0.190825659362085,-0.178489353268304,-0.152338529549808,
-0.146996925142279,-0.143896317902965,-0.141132938135055,-0.137586231032848,
-0.129872763694196,-0.11888702869055,-0.105916195971956,-0.090796970585841,
-0.0870796324137364,-0.0852005170170505,-0.0836448293163537,-0.0815862667767107,
-0.0815454327891802,-0.0768592190584028,-0.0673422136539098,-0.0406636701991896,
-0.0322018785559816,-0.0288030993362951,-0.0259935531815042,-0.02308821969655,
-0.0201488702907366,-0.0159551229479655,-0.000334955112094566),
 .UNSPECIFIED.);
#764=B_SPLINE_CURVE_WITH_KNOTS('',3,(#74494,#74495,#74496,#74497,#74498,
#74499,#74500,#74501,#74502,#74503,#74504,#74505,#74506,#74507,#74508,#74509,
#74510,#74511,#74512,#74513,#74514,#74515),.UNSPECIFIED.,.F.,.F.,(4,2,2,
2,2,2,2,2,2,2,4),(-1.4836709134642,-1.45834033302783,-1.45524331960259,
-1.45267009041877,-1.451030912921,-1.44937115674332,-1.4467017984514,-1.43755481426339,
-1.41636892125086,-1.40565146373752,-1.40060990531413),.UNSPECIFIED.);
#765=B_SPLINE_CURVE_WITH_KNOTS('',3,(#74517,#74518,#74519,#74520,#74521,
#74522,#74523,#74524,#74525,#74526,#74527,#74528,#74529,#74530,#74531,#74532,
#74533,#74534,#74535),.UNSPECIFIED.,.F.,.F.,(4,3,3,3,3,3,4),(65.2692561001133,
65.3873720613773,65.5054033502643,65.6234822689178,65.7415755373178,65.8598751587599,
65.9734457248711),.UNSPECIFIED.);
#766=B_SPLINE_CURVE_WITH_KNOTS('',3,(#74536,#74537,#74538,#74539,#74540,
#74541,#74542,#74543,#74544,#74545,#74546,#74547,#74548,#74549,#74550,#74551,
#74552,#74553,#74554,#74555,#74556,#74557,#74558,#74559,#74560,#74561,#74562,
#74563,#74564,#74565,#74566,#74567,#74568,#74569,#74570,#74571,#74572,#74573,
#74574,#74575,#74576,#74577,#74578,#74579,#74580,#74581,#74582,#74583,#74584,
#74585,#74586,#74587,#74588,#74589,#74590,#74591,#74592,#74593,#74594,#74595,
#74596,#74597,#74598,#74599,#74600,#74601,#74602,#74603,#74604,#74605,#74606,
#74607,#74608,#74609,#74610,#74611,#74612,#74613,#74614,#74615,#74616,#74617,
#74618,#74619,#74620,#74621,#74622,#74623,#74624,#74625,#74626,#74627,#74628,
#74629,#74630,#74631,#74632,#74633,#74634,#74635,#74636,#74637,#74638,#74639,
#74640,#74641,#74642,#74643,#74644,#74645,#74646,#74647,#74648,#74649,#74650,
#74651,#74652,#74653,#74654,#74655,#74656,#74657,#74658,#74659,#74660,#74661,
#74662,#74663,#74664,#74665,#74666,#74667,#74668,#74669,#74670,#74671,#74672,
#74673,#74674,#74675,#74676,#74677,#74678,#74679,#74680,#74681,#74682,#74683,
#74684,#74685,#74686,#74687,#74688,#74689),.UNSPECIFIED.,.F.,.F.,(4,3,3,
3,3,3,3,3,3,3,3,3,3,3,3,3,3,3,3,3,3,3,3,3,3,3,3,3,3,3,3,3,3,3,3,3,3,3,3,
3,3,3,3,3,3,3,3,3,3,3,3,4),(65.9734457253855,66.0726645987058,66.1962107123329,
66.3158658962491,66.435403271838,66.5548754120015,66.6743347765995,66.793914264622,
66.913567071186,67.0334315661134,67.0610335077225,67.1845796213496,67.304234805268,
67.4237721808587,67.5432443210237,67.6627036856228,67.782283173646,67.9019359802104,
68.0218004751376,68.0494024167392,68.1729485303663,68.2926037144019,68.41214109011,
68.5316132303923,68.6510725951084,68.7706520832471,68.8903048899263,69.0101693849663,
69.037771325756,69.1613174393831,69.2809726231416,69.4005099985737,69.5199821385816,
69.6394415030256,69.7590209908976,69.8786737973129,69.9985382920956,70.0261402347727,
70.1496863483998,70.2693415322863,70.3888789078432,70.5083510479725,70.6278104125342,
70.7473899005178,70.8670427070412,70.9869072019259,71.0145091437894,71.1343809419583,
71.2540404936461,71.3735768465406,71.4930579961026,71.5518219705938),
 .UNSPECIFIED.);
#767=B_SPLINE_CURVE_WITH_KNOTS('',3,(#74694,#74695,#74696,#74697,#74698,
#74699,#74700,#74701,#74702,#74703,#74704,#74705,#74706,#74707,#74708,#74709,
#74710,#74711,#74712,#74713,#74714,#74715,#74716,#74717,#74718,#74719,#74720,
#74721,#74722,#74723,#74724,#74725,#74726,#74727,#74728,#74729,#74730,#74731,
#74732,#74733,#74734,#74735,#74736,#74737,#74738,#74739,#74740,#74741,#74742,
#74743,#74744,#74745,#74746,#74747,#74748,#74749,#74750,#74751,#74752,#74753,
#74754,#74755,#74756,#74757,#74758,#74759,#74760,#74761,#74762,#74763,#74764,
#74765,#74766,#74767,#74768,#74769,#74770,#74771,#74772,#74773,#74774,#74775,
#74776,#74777,#74778,#74779,#74780,#74781,#74782,#74783,#74784,#74785,#74786,
#74787,#74788,#74789,#74790,#74791,#74792,#74793,#74794,#74795,#74796,#74797,
#74798,#74799,#74800,#74801,#74802,#74803,#74804,#74805,#74806,#74807,#74808,
#74809,#74810,#74811,#74812,#74813,#74814,#74815,#74816,#74817,#74818,#74819,
#74820,#74821,#74822,#74823,#74824,#74825,#74826,#74827,#74828,#74829,#74830,
#74831,#74832,#74833,#74834,#74835,#74836,#74837,#74838,#74839,#74840,#74841,
#74842,#74843,#74844,#74845,#74846,#74847,#74848,#74849,#74850,#74851,#74852,
#74853,#74854,#74855,#74856,#74857,#74858,#74859,#74860,#74861,#74862,#74863,
#74864,#74865,#74866,#74867,#74868,#74869,#74870,#74871,#74872,#74873,#74874,
#74875,#74876,#74877,#74878,#74879,#74880,#74881,#74882,#74883,#74884,#74885,
#74886,#74887,#74888,#74889),.UNSPECIFIED.,.F.,.F.,(4,2,2,2,2,2,2,2,2,2,
2,2,2,2,2,2,2,2,2,2,2,2,2,2,2,2,2,2,2,2,2,2,2,2,2,2,2,2,2,2,2,2,2,2,2,2,
2,2,2,2,2,2,2,2,2,2,2,2,2,2,2,2,2,2,2,2,2,2,2,2,2,2,2,2,2,2,2,2,2,2,2,2,
2,2,2,2,2,2,2,2,2,2,2,2,2,2,2,4),(-1.40128003339357,-1.39210941171292,-1.38043630308909,
-1.3737845005758,-1.37144360238271,-1.3698496377744,-1.36811984913717,-1.36512794361135,
-1.34833028183322,-1.33498901578421,-1.3192905432365,-1.3148417287557,-1.31192476653075,
-1.30912369157327,-1.30575915304785,-1.29737868129969,-1.27271691874549,
-1.26276733121124,-1.25863363351139,-1.25542192331339,-1.25364553967208,
-1.25206973021645,-1.24983906667524,-1.24440631083524,-1.22311320238154,
-1.21831559728887,-1.20772254920655,-1.20020010179226,-1.19668610621486,
-1.19392624880157,-1.19080659628913,-1.18551198137943,-1.15948182869849,
-1.14706432456199,-1.14015752285836,-1.1377853930556,-1.13618559271827,
-1.13446677244753,-1.13152646805925,-1.11697017177115,-1.10481838502156,
-1.09222494207606,-1.08376967217366,-1.0801027578258,-1.07732493605402,
-1.07428656651196,-1.06924666999661,-1.04076802383121,-1.02445723200069,
-1.02150162161994,-1.01977943105424,-1.01819967404407,-1.01585169881057,
-1.00962322763275,-0.986409728095614,-0.96893295280559,-0.964376153966052,
-0.961437037890596,-0.958648733233082,-0.954734450646943,-0.945255570838767,
-0.917228341016276,-0.910336449632518,-0.90565353335338,-0.903598157775324,
-0.902042584926881,-0.900160763029455,-0.896544548772937,-0.877099456031107,
-0.860576107283148,-0.850573056878916,-0.846682562952161,-0.843870276742218,
-0.84091681986949,-0.83629026310259,-0.818931252705608,-0.802545998320124,
-0.794332166578819,-0.789040367208318,-0.786886950727362,-0.785321627262545,
-0.783504375718744,-0.780191744834745,-0.756790572935862,-0.742555974090395,
-0.733587423972396,-0.730128104464985,-0.727559876792625,-0.724719682142326,
-0.720669814902384,-0.70938173381975,-0.688663578273523,-0.673824868879985,
-0.670879315580966,-0.669159222157904,-0.667559725729801,-0.665190209532858,
-0.659264417620488),.UNSPECIFIED.);
#768=B_SPLINE_CURVE_WITH_KNOTS('',3,(#74891,#74892,#74893,#74894,#74895,
#74896,#74897,#74898,#74899,#74900,#74901,#74902,#74903,#74904,#74905,#74906,
#74907,#74908,#74909),.UNSPECIFIED.,.F.,.F.,(4,3,3,3,3,3,4),(71.5518219705938,
71.6713814952313,71.7909889789199,71.9108277902384,72.0028780528061,72.155509984639,
72.2566310318613),.UNSPECIFIED.);
#769=B_SPLINE_CURVE_WITH_KNOTS('',3,(#74910,#74911,#74912,#74913,#74914,
#74915,#74916,#74917,#74918,#74919,#74920,#74921,#74922,#74923,#74924,#74925,
#74926,#74927,#74928,#74929,#74930,#74931,#74932,#74933,#74934,#74935,#74936,
#74937,#74938,#74939,#74940,#74941,#74942,#74943,#74944,#74945,#74946,#74947,
#74948,#74949,#74950,#74951,#74952,#74953,#74954,#74955,#74956,#74957,#74958,
#74959,#74960,#74961,#74962,#74963,#74964,#74965,#74966,#74967,#74968,#74969,
#74970,#74971,#74972,#74973,#74974,#74975,#74976,#74977,#74978,#74979,#74980,
#74981,#74982,#74983,#74984,#74985,#74986,#74987,#74988,#74989,#74990,#74991,
#74992,#74993,#74994,#74995,#74996,#74997,#74998,#74999,#75000,#75001,#75002,
#75003,#75004,#75005,#75006,#75007,#75008,#75009,#75010,#75011,#75012,#75013,
#75014,#75015,#75016,#75017,#75018,#75019,#75020,#75021,#75022,#75023,#75024,
#75025,#75026,#75027,#75028,#75029,#75030,#75031,#75032,#75033,#75034,#75035,
#75036,#75037,#75038,#75039,#75040,#75041,#75042,#75043,#75044,#75045,#75046,
#75047,#75048,#75049,#75050,#75051,#75052,#75053,#75054,#75055,#75056,#75057,
#75058,#75059,#75060,#75061,#75062,#75063),.UNSPECIFIED.,.F.,.F.,(4,3,3,
3,3,3,3,3,3,3,3,3,3,3,3,3,3,3,3,3,3,3,3,3,3,3,3,3,3,3,3,3,3,3,3,3,3,3,3,
3,3,3,3,3,3,3,3,3,3,3,3,4),(72.2566310325651,72.3749180120349,72.4931281764082,
72.6113162646557,72.7296157230161,72.8479843387787,72.9665609847747,72.9912469618228,
73.1147930754499,73.2344482597025,73.3539856356069,73.4734577760647,73.5929171409353,
73.7124966291971,73.8321494359811,73.9520139310986,73.9796158708395,74.1031619844666,
74.2228171752065,74.342354557629,74.4618267046219,74.5812860760313,74.7008655707878,
74.8205183840471,74.9403828855481,74.9679847798563,75.0915308934834,75.2111860605028,
75.3307234192612,75.4501955426938,75.5696548906937,75.6892343624356,75.8088871528883,
75.9287516321069,75.956353688873,76.0798998025001,76.1995549957352,76.3190923804485,
76.4385645295258,76.5580239028104,76.6776033991253,76.7972562137593,76.9171207163584,
76.9447225978897,77.0645588437826,77.1842191415837,77.3037562699964,77.4232228139605,
77.542731903974,77.6622643053389,77.7819561071778,77.8347123306237),
 .UNSPECIFIED.);
#770=B_SPLINE_CURVE_WITH_KNOTS('',3,(#75069,#75070,#75071,#75072,#75073,
#75074,#75075,#75076,#75077,#75078,#75079,#75080,#75081,#75082,#75083,#75084,
#75085,#75086,#75087,#75088,#75089,#75090,#75091,#75092,#75093,#75094,#75095,
#75096,#75097,#75098,#75099,#75100,#75101,#75102,#75103,#75104,#75105,#75106,
#75107,#75108,#75109,#75110,#75111,#75112,#75113,#75114,#75115,#75116,#75117,
#75118,#75119,#75120,#75121,#75122,#75123,#75124,#75125,#75126,#75127,#75128,
#75129,#75130,#75131,#75132,#75133,#75134,#75135,#75136,#75137,#75138,#75139,
#75140,#75141,#75142,#75143,#75144,#75145,#75146,#75147,#75148,#75149,#75150,
#75151,#75152,#75153,#75154,#75155,#75156,#75157,#75158,#75159,#75160,#75161,
#75162,#75163,#75164,#75165,#75166,#75167,#75168,#75169,#75170,#75171,#75172,
#75173,#75174,#75175,#75176,#75177,#75178,#75179,#75180,#75181,#75182,#75183,
#75184,#75185,#75186,#75187,#75188,#75189,#75190,#75191,#75192,#75193,#75194,
#75195,#75196,#75197,#75198,#75199,#75200,#75201,#75202,#75203,#75204,#75205,
#75206,#75207,#75208,#75209,#75210,#75211,#75212,#75213,#75214,#75215,#75216,
#75217,#75218,#75219,#75220,#75221,#75222,#75223,#75224,#75225,#75226,#75227,
#75228,#75229,#75230,#75231,#75232,#75233,#75234,#75235,#75236,#75237,#75238,
#75239,#75240,#75241,#75242,#75243,#75244,#75245,#75246),.UNSPECIFIED.,
 .F.,.F.,(4,2,2,2,2,2,2,2,2,2,2,2,2,2,2,2,2,2,2,2,2,2,2,2,2,2,2,2,2,2,2,
2,2,2,2,2,2,2,2,2,2,2,2,2,2,2,2,2,2,2,2,2,2,2,2,2,2,2,2,2,2,2,2,2,2,2,2,
2,2,2,2,2,2,2,2,2,2,2,2,2,2,2,2,2,2,2,2,2,4),(-0.659170325149453,-0.655256623528942,
-0.649784001405313,-0.646666348339993,-0.643922255609298,-0.640448200383027,
-0.633100017464438,-0.607089608807798,-0.596760357812911,-0.592534883661284,
-0.589272090014849,-0.587491318556743,-0.585922400426226,-0.583724000050673,
-0.578132244094427,-0.569222056456834,-0.540136017048644,-0.533563692045375,
-0.530176200660663,-0.527421915066887,-0.524204202362348,-0.518296138243247,
-0.510718176186608,-0.490293883619145,-0.475179063581887,-0.472228741143748,
-0.47050513421987,-0.468903326492536,-0.466528517525274,-0.459610265416756,
-0.447162378644605,-0.421223496116864,-0.415921823155921,-0.412799589114962,
-0.410038315090225,-0.406523657458192,-0.399004654764951,-0.38842020640015,
-0.383825145689173,-0.362920836027997,-0.357002122308034,-0.354695199602874,
-0.35312256171966,-0.351385555207384,-0.348358433767659,-0.329206254415996,
-0.304537463323012,-0.299122392672783,-0.295977777984708,-0.293249228730659,
-0.289791957447864,-0.282589546689366,-0.27263314195551,-0.258650231520054,
-0.242797284850174,-0.239039239971014,-0.237152861500545,-0.235613207142084,
-0.233574952373678,-0.228992107513741,-0.203128551472326,-0.186026285584048,
-0.181408154134144,-0.178456270294801,-0.175642776124923,-0.171746134850384,
-0.161698126017314,-0.145042792044167,-0.12579786732056,-0.122171372228599,
-0.120287198930523,-0.118731668144502,-0.11667879106968,-0.112010428535118,
-0.105149324099089,-0.0774720162932436,-0.0677246689046249,-0.0637686764328149,
-0.0609733952386566,-0.0580465437958409,-0.0535497882993478,-0.0371255518100336,
-0.0190527454480019,-0.0129595916652631,-0.00654563670509995,-0.00421896730293171,
-0.00264042997467122,-0.00137147600074732,-0.000346630335231024),
 .UNSPECIFIED.);
#771=B_SPLINE_CURVE_WITH_KNOTS('',3,(#75247,#75248,#75249,#75250,#75251,
#75252,#75253,#75254,#75255,#75256,#75257,#75258,#75259,#75260,#75261,#75262,
#75263,#75264,#75265,#75266,#75267,#75268),.UNSPECIFIED.,.F.,.F.,(4,2,2,
2,2,2,2,2,2,2,4),(-1.48452167401131,-1.48321766816317,-1.48078181711199,
-1.45391592152954,-1.44220222492896,-1.43414473492672,-1.43054163756083,
-1.42777239058184,-1.42470374612459,-1.4195154426393,-1.40128003339357),
 .UNSPECIFIED.);
#772=B_SPLINE_CURVE_WITH_KNOTS('',3,(#75270,#75271,#75272,#75273,#75274,
#75275,#75276,#75277,#75278,#75279,#75280,#75281,#75282,#75283,#75284,#75285,
#75286,#75287,#75288),.UNSPECIFIED.,.F.,.F.,(4,3,3,3,3,3,4),(77.8347123306237,
77.9330915069064,78.0542613844013,78.1756501232371,78.2964289099056,78.4181226248252,
78.5398163397448),.UNSPECIFIED.);
#773=B_SPLINE_CURVE_WITH_KNOTS('',3,(#75289,#75290,#75291,#75292,#75293,
#75294,#75295,#75296,#75297,#75298,#75299,#75300,#75301,#75302,#75303,#75304,
#75305,#75306,#75307,#75308,#75309,#75310,#75311,#75312,#75313,#75314,#75315,
#75316,#75317,#75318,#75319,#75320,#75321,#75322,#75323,#75324,#75325,#75326,
#75327,#75328,#75329,#75330,#75331,#75332,#75333,#75334,#75335,#75336,#75337,
#75338,#75339,#75340,#75341,#75342,#75343,#75344,#75345,#75346,#75347,#75348,
#75349,#75350,#75351,#75352,#75353,#75354,#75355,#75356,#75357,#75358,#75359,
#75360,#75361,#75362,#75363,#75364,#75365,#75366,#75367,#75368,#75369,#75370,
#75371,#75372,#75373,#75374,#75375,#75376,#75377,#75378,#75379,#75380,#75381,
#75382,#75383,#75384,#75385,#75386,#75387,#75388,#75389,#75390,#75391,#75392,
#75393,#75394,#75395,#75396,#75397,#75398,#75399,#75400,#75401,#75402,#75403,
#75404,#75405,#75406,#75407,#75408,#75409,#75410,#75411,#75412,#75413,#75414,
#75415,#75416,#75417,#75418,#75419,#75420,#75421,#75422,#75423,#75424,#75425,
#75426,#75427,#75428,#75429,#75430,#75431,#75432,#75433,#75434,#75435,#75436,
#75437,#75438,#75439,#75440,#75441,#75442),.UNSPECIFIED.,.F.,.F.,(4,3,3,
3,3,3,3,3,3,3,3,3,3,3,3,3,3,3,3,3,3,3,3,3,3,3,3,3,3,3,3,3,3,3,3,3,3,3,3,
3,3,3,3,3,3,3,3,3,3,3,3,4),(78.5398163404196,78.6729079988692,78.8069522576926,
78.9214604159231,79.0450065295502,79.1646618515047,79.284199363364,79.4036716377764,
79.5231311343454,79.6427107500453,79.7623636819029,79.8822282974684,79.9098293249398,
80.0333754385669,80.1530309862348,80.2725687275557,80.3920412346678,80.5115009666695,
80.6310808199963,80.7507339910015,80.870598845506,80.8981982339565,81.0217443475836,
81.1413981074268,81.2609340620303,81.3804047871306,81.4998627454262,81.6194408504108,
81.7390922861601,81.8589554414028,81.8865671429733,82.0101132566004,82.1297701253563,
82.2493091702118,82.3687829608855,82.4882439540318,82.6078250265274,82.7274793933696,
82.8473453984445,82.87493605199,82.9984821656171,83.1181396337386,83.2376793157842,
83.3571537797169,83.4766154804869,83.5961973051156,83.7158524508728,83.8357192653888,
83.8633049610067,83.9826046296134,84.1017010849209,84.1188182559913),
 .UNSPECIFIED.);
#774=B_SPLINE_CURVE_WITH_KNOTS('',3,(#75446,#75447,#75448,#75449,#75450,
#75451,#75452),.UNSPECIFIED.,.F.,.F.,(4,2,1,4),(-4.09202352044837,-4.0499104913527,
-3.06154158233598,-2.07317267331961),.UNSPECIFIED.);
#775=B_SPLINE_CURVE_WITH_KNOTS('',3,(#75456,#75457,#75458,#75459,#75460),
 .UNSPECIFIED.,.F.,.F.,(4,1,4),(0.,0.989559462785669,1.12274180646041),
 .UNSPECIFIED.);
#776=B_SPLINE_CURVE_WITH_KNOTS('',3,(#75462,#75463,#75464,#75465,#75466,
#75467,#75468,#75469,#75470,#75471,#75472,#75473,#75474,#75475,#75476,#75477,
#75478,#75479,#75480,#75481,#75482,#75483,#75484,#75485,#75486,#75487,#75488,
#75489,#75490,#75491,#75492,#75493,#75494,#75495,#75496,#75497,#75498,#75499,
#75500,#75501,#75502,#75503,#75504,#75505,#75506,#75507,#75508,#75509,#75510,
#75511,#75512,#75513,#75514,#75515,#75516,#75517,#75518,#75519,#75520,#75521,
#75522,#75523,#75524,#75525,#75526,#75527,#75528,#75529,#75530,#75531,#75532,
#75533,#75534,#75535,#75536,#75537,#75538,#75539,#75540,#75541,#75542,#75543,
#75544,#75545,#75546,#75547,#75548,#75549,#75550,#75551,#75552,#75553,#75554,
#75555,#75556,#75557,#75558,#75559,#75560,#75561,#75562,#75563,#75564,#75565,
#75566,#75567,#75568,#75569,#75570,#75571,#75572,#75573,#75574,#75575,#75576,
#75577,#75578,#75579,#75580,#75581,#75582,#75583,#75584,#75585,#75586,#75587,
#75588,#75589,#75590,#75591,#75592,#75593,#75594,#75595,#75596,#75597,#75598,
#75599,#75600,#75601,#75602,#75603,#75604,#75605,#75606,#75607,#75608,#75609,
#75610,#75611,#75612,#75613,#75614,#75615,#75616,#75617,#75618,#75619,#75620,
#75621,#75622,#75623,#75624,#75625,#75626,#75627,#75628,#75629,#75630,#75631,
#75632,#75633),.UNSPECIFIED.,.F.,.F.,(4,3,3,3,3,3,3,3,3,3,3,3,3,3,3,3,3,
3,3,3,3,3,3,3,3,3,3,3,3,3,3,3,3,3,3,3,3,3,3,3,3,3,3,3,3,3,3,3,3,3,3,3,3,
3,3,3,3,4),(1.12274180646041,1.23382961778976,1.34478346838675,1.45565131443454,
1.56648094818943,1.67739799460759,1.78835809282476,1.89952234791358,1.97911892557135,
2.09267048898284,2.20601859343239,2.31925352705299,2.43241996957223,2.545562499232,
2.65880529165444,2.77209826670266,2.88559915987598,2.96867838835702,3.08237111938443,
3.19586878054423,3.30925828831477,3.42258402266246,3.53589026815068,3.64930230557827,
3.7627678535008,3.87644462139266,3.9582378511427,4.07166735977434,4.18489457552661,
4.29800943267414,4.41105683010432,4.5240815661709,4.63720945218514,4.75038895656566,
4.86378013355541,4.94779731392838,5.06133349396987,5.17466928122119,5.28789378838566,
5.40105171175323,5.51418764845825,5.62742688859855,5.74071800081016,5.85421981781746,
5.93735677671406,6.05089770957896,6.16423890038886,6.27746920605335,6.39063331211564,
6.50377580544888,6.61702213100323,6.73032063390784,6.84383025098836,6.92691623949973,
7.04689316765889,7.16661181918139,7.28626946610256,7.40592711302372),
 .UNSPECIFIED.);
#777=B_SPLINE_CURVE_WITH_KNOTS('',3,(#75635,#75636,#75637,#75638,#75639,
#75640,#75641,#75642,#75643,#75644,#75645,#75646,#75647,#75648,#75649,#75650,
#75651,#75652,#75653,#75654,#75655,#75656,#75657,#75658,#75659,#75660,#75661,
#75662,#75663,#75664,#75665,#75666,#75667,#75668,#75669,#75670,#75671,#75672,
#75673,#75674,#75675,#75676,#75677,#75678,#75679,#75680,#75681,#75682,#75683,
#75684,#75685,#75686,#75687,#75688,#75689,#75690,#75691,#75692,#75693,#75694,
#75695,#75696,#75697,#75698,#75699,#75700,#75701,#75702,#75703,#75704,#75705,
#75706,#75707,#75708,#75709,#75710,#75711,#75712,#75713,#75714,#75715,#75716,
#75717,#75718,#75719,#75720,#75721,#75722,#75723,#75724,#75725,#75726,#75727,
#75728,#75729,#75730,#75731,#75732,#75733,#75734,#75735,#75736,#75737,#75738,
#75739,#75740,#75741,#75742,#75743,#75744,#75745,#75746,#75747,#75748,#75749,
#75750,#75751,#75752,#75753,#75754,#75755,#75756,#75757,#75758,#75759,#75760,
#75761,#75762,#75763,#75764,#75765,#75766,#75767,#75768,#75769,#75770,#75771,
#75772,#75773,#75774,#75775,#75776,#75777,#75778,#75779,#75780,#75781,#75782,
#75783,#75784,#75785,#75786,#75787,#75788,#75789,#75790,#75791,#75792,#75793,
#75794,#75795,#75796,#75797,#75798,#75799,#75800,#75801,#75802,#75803,#75804,
#75805,#75806,#75807,#75808,#75809),.UNSPECIFIED.,.F.,.F.,(4,3,3,3,3,3,
3,3,3,3,3,3,3,3,3,3,3,3,3,3,3,3,3,3,3,3,3,3,3,3,3,3,3,3,3,3,3,3,3,3,3,3,
3,3,3,3,3,3,3,3,3,3,3,3,3,3,3,3,4),(7.40592711364008,7.52358787815993,7.64154429499719,
7.75966365595211,7.87808317498899,7.91647570228541,8.03000264719238,8.14332932527602,
8.25654480818245,8.36969380919324,8.4828209425382,8.59605163600875,8.70933433192551,
8.82282805122039,8.90603516507109,9.01956138335161,9.13288737703557,9.24610220203009,
9.35925057286215,9.47237710503925,9.5856072473793,9.69888941923431,9.81238266542286,
9.89559462785677,10.0091181085231,10.1224412796891,10.2356532323887,10.3487986865135,
10.4619222628744,10.5751494124928,10.6884285665954,10.8019187914085,10.8851540906425,
10.998679191203,11.1120040174162,11.2252176453697,11.3383647918229,11.4514900744797,
11.5647189382983,11.677999813562,11.7914917495915,11.8747135534281,11.9882384330826,
12.1015630395301,12.2147764485999,12.3279233774626,12.4410484442335,12.5542770965709,
12.6675577624936,12.7810494952956,12.8642730162138,12.9760889596331,13.087748618379,
13.1992993741481,13.3107884237349,13.4223163638858,13.5338668329265,13.6455583786727,
13.689112420188),.UNSPECIFIED.);
#778=B_SPLINE_CURVE_WITH_KNOTS('',3,(#75811,#75812,#75813,#75814,#75815,
#75816,#75817,#75818,#75819,#75820,#75821,#75822,#75823,#75824,#75825,#75826,
#75827,#75828,#75829,#75830,#75831,#75832,#75833,#75834,#75835,#75836,#75837,
#75838,#75839,#75840,#75841,#75842,#75843,#75844,#75845,#75846,#75847,#75848,
#75849,#75850,#75851,#75852,#75853,#75854,#75855,#75856,#75857,#75858,#75859,
#75860,#75861,#75862,#75863,#75864,#75865,#75866,#75867,#75868,#75869,#75870,
#75871,#75872,#75873,#75874,#75875,#75876,#75877,#75878,#75879,#75880,#75881,
#75882,#75883,#75884,#75885,#75886,#75887,#75888,#75889,#75890,#75891,#75892,
#75893,#75894,#75895,#75896,#75897,#75898,#75899,#75900,#75901,#75902,#75903,
#75904,#75905,#75906,#75907,#75908,#75909,#75910,#75911,#75912,#75913,#75914,
#75915,#75916,#75917,#75918,#75919,#75920,#75921,#75922,#75923,#75924,#75925,
#75926,#75927,#75928,#75929,#75930,#75931,#75932,#75933,#75934,#75935,#75936,
#75937,#75938,#75939,#75940,#75941,#75942,#75943,#75944,#75945,#75946,#75947,
#75948,#75949,#75950,#75951,#75952,#75953,#75954,#75955,#75956,#75957,#75958,
#75959,#75960,#75961,#75962,#75963,#75964,#75965,#75966,#75967,#75968,#75969,
#75970,#75971,#75972,#75973,#75974,#75975,#75976,#75977,#75978,#75979,#75980,
#75981,#75982),.UNSPECIFIED.,.F.,.F.,(4,3,3,3,3,3,3,3,3,3,3,3,3,3,3,3,3,
3,3,3,3,3,3,3,3,3,3,3,3,3,3,3,3,3,3,3,3,3,3,3,3,3,3,3,3,3,3,3,3,3,3,3,3,
3,3,3,3,4),(13.6891124208198,13.8538324789995,13.9673572877926,14.0806818189803,
14.1938951501528,14.3070419986254,14.4201669826556,14.5333955492639,14.6466761276639,
14.7601677710853,14.8433919417852,14.9569167108435,15.0702412020156,15.1834544930335,
15.2966013012875,15.4097262451101,15.5229547718542,15.636235310522,15.7497269149215,
15.8329514045708,15.946476150597,16.0598006178626,16.1730138844571,16.2861606678164,
16.3992855863179,16.5125140872826,16.6257945998772,16.7392861780446,16.8225108673565,
16.9360356348413,17.0493601240942,17.1625734129822,17.2757202188998,17.388845160183,
17.5020736840922,17.6153542197563,17.728845820912,17.8120703301422,17.9255950916193,
18.038919574788,18.1521328575499,18.2652796573108,18.3784045924182,18.4916331101721,
18.604913639683,18.7184052347656,18.8016297929279,18.9151545525914,19.0284790338638,
19.1416923146804,19.2548391124505,19.3679640455252,19.4811925611976,19.5944730885968,
19.7079646815442,19.7911892557135,19.9596425437774,19.972297727999),
 .UNSPECIFIED.);
#779=B_SPLINE_CURVE_WITH_KNOTS('',3,(#75984,#75985,#75986,#75987,#75988,
#75989,#75990,#75991,#75992,#75993,#75994,#75995,#75996,#75997,#75998,#75999,
#76000,#76001,#76002,#76003,#76004,#76005,#76006,#76007,#76008,#76009,#76010,
#76011,#76012,#76013,#76014,#76015,#76016,#76017,#76018,#76019,#76020,#76021,
#76022,#76023,#76024,#76025,#76026,#76027,#76028,#76029,#76030,#76031,#76032,
#76033,#76034,#76035,#76036,#76037,#76038,#76039,#76040,#76041,#76042,#76043,
#76044,#76045,#76046,#76047,#76048,#76049,#76050,#76051,#76052,#76053,#76054,
#76055,#76056,#76057,#76058,#76059,#76060,#76061,#76062,#76063,#76064,#76065,
#76066,#76067,#76068,#76069,#76070,#76071,#76072,#76073,#76074,#76075,#76076,
#76077,#76078,#76079,#76080,#76081,#76082,#76083,#76084,#76085,#76086,#76087,
#76088,#76089,#76090,#76091,#76092,#76093,#76094,#76095,#76096,#76097,#76098,
#76099,#76100,#76101,#76102,#76103,#76104,#76105,#76106,#76107,#76108,#76109,
#76110,#76111,#76112,#76113,#76114,#76115,#76116,#76117,#76118,#76119,#76120,
#76121,#76122,#76123,#76124,#76125,#76126,#76127,#76128,#76129,#76130,#76131,
#76132,#76133,#76134,#76135,#76136,#76137,#76138,#76139,#76140,#76141,#76142,
#76143,#76144,#76145,#76146,#76147,#76148,#76149,#76150,#76151,#76152,#76153,
#76154,#76155,#76156,#76157,#76158),.UNSPECIFIED.,.F.,.F.,(4,3,3,3,3,3,
3,3,3,3,3,3,3,3,3,3,3,3,3,3,3,3,3,3,3,3,3,3,3,3,3,3,3,3,3,3,3,3,3,3,3,3,
3,3,3,3,3,3,3,3,3,3,3,3,3,3,3,3,4),(19.972297728497,20.0839743113852,20.1955429489355,
20.3070508212707,20.4185450026315,20.5301439596349,20.6418068892393,20.753658132519,
20.7807487184992,20.8942734796944,21.0075979625469,21.1208112449716,21.2339580443754,
21.3470829791058,21.4603114964553,21.573592025546,21.6870836201873,21.7703081812849,
21.8838329423694,21.997157425104,22.1103707074066,22.2235175066839,22.3366424412841,
22.4498709584984,22.5631514874508,22.6766430819507,22.7598676440706,22.8733924054068,
22.9867168883998,23.0999301709649,23.2130769705083,23.3262019053778,23.4394304228638,
23.5527109520897,23.6662025468629,23.7494271068562,23.8629518680848,23.9762763509684,
24.0894896334229,24.2026364328546,24.3157613676117,24.4289898849852,24.5422704140983,
24.6557620087595,24.7389865696419,24.8525113308689,24.9658358137503,25.0790490962022,
25.1921958956312,25.3053208303848,25.4185493477547,25.5318298768639,25.6453214715208,
25.7285460324276,25.8462362390639,25.9636191281052,26.0808182478312,26.1978234044031,
26.2554830351787),.UNSPECIFIED.);
#780=B_SPLINE_CURVE_WITH_KNOTS('',3,(#76160,#76161,#76162,#76163,#76164,
#76165,#76166,#76167,#76168,#76169,#76170,#76171,#76172,#76173,#76174,#76175,
#76176,#76177,#76178,#76179,#76180,#76181,#76182,#76183,#76184,#76185,#76186,
#76187,#76188,#76189,#76190,#76191,#76192,#76193,#76194,#76195,#76196,#76197,
#76198,#76199,#76200,#76201,#76202,#76203,#76204,#76205,#76206,#76207,#76208,
#76209,#76210,#76211,#76212,#76213,#76214,#76215,#76216,#76217,#76218,#76219,
#76220,#76221,#76222,#76223,#76224,#76225,#76226,#76227,#76228,#76229,#76230,
#76231,#76232,#76233,#76234,#76235,#76236,#76237,#76238,#76239,#76240,#76241,
#76242,#76243,#76244,#76245,#76246,#76247,#76248,#76249,#76250,#76251,#76252,
#76253,#76254,#76255,#76256,#76257,#76258,#76259,#76260,#76261,#76262,#76263,
#76264,#76265,#76266,#76267,#76268,#76269,#76270,#76271,#76272,#76273,#76274,
#76275,#76276,#76277,#76278,#76279,#76280,#76281,#76282,#76283,#76284,#76285,
#76286,#76287,#76288,#76289,#76290,#76291,#76292,#76293,#76294,#76295,#76296,
#76297,#76298,#76299,#76300,#76301,#76302,#76303,#76304,#76305,#76306,#76307,
#76308,#76309,#76310,#76311,#76312,#76313,#76314,#76315,#76316,#76317,#76318,
#76319,#76320,#76321,#76322,#76323,#76324,#76325,#76326,#76327,#76328,#76329,
#76330,#76331),.UNSPECIFIED.,.F.,.F.,(4,3,3,3,3,3,3,3,3,3,3,3,3,3,3,3,3,
3,3,3,3,3,3,3,3,3,3,3,3,3,3,3,3,3,3,3,3,3,3,3,3,3,3,3,3,3,3,3,3,3,3,3,3,
3,3,3,3,4),(26.2554830357989,26.3757798650132,26.4963153854641,26.6172862332497,
26.7181054952133,26.8316302564529,26.9449547393473,27.0581680218127,27.1713148212552,
27.284439756023,27.3976682734069,27.5109488025305,27.6244403972019,27.707664957999,
27.8211897192396,27.934514202135,28.0477274846013,28.1608742840448,28.2739992188135,
28.3872277361983,28.5005082653227,28.6139998599949,28.6972244207846,28.8107491820277,
28.9240736649257,29.0372869473946,29.1504337468408,29.2635586816123,29.3767871989999,
29.4900677281271,29.603559322802,29.6867838835703,29.8003086448119,29.9136331277083,
30.0268464101756,30.1399932096202,30.25311814439,30.3663466617759,30.4796271909015,
30.5931187855748,30.676343346356,30.7898681075978,30.9031925904945,31.0164058729621,
31.1295526724069,31.2426776071769,31.3559061245631,31.4691866536889,31.5826782483624,
31.6659028091417,31.7778650422759,31.8896720534227,32.0013710373486,32.1130090117127,
32.2246998396253,32.3364127594324,32.4483027983562,32.5386683419253),
 .UNSPECIFIED.);
#781=B_SPLINE_CURVE_WITH_KNOTS('',3,(#76333,#76334,#76335,#76336,#76337,
#76338,#76339,#76340,#76341,#76342,#76343,#76344,#76345,#76346,#76347,#76348,
#76349,#76350,#76351,#76352,#76353,#76354,#76355,#76356,#76357,#76358,#76359,
#76360,#76361,#76362,#76363,#76364,#76365,#76366,#76367,#76368,#76369,#76370,
#76371,#76372,#76373,#76374,#76375,#76376,#76377,#76378,#76379,#76380,#76381,
#76382,#76383,#76384,#76385,#76386,#76387,#76388,#76389,#76390,#76391,#76392,
#76393,#76394,#76395,#76396,#76397,#76398,#76399,#76400,#76401,#76402,#76403,
#76404,#76405,#76406,#76407,#76408,#76409,#76410,#76411,#76412,#76413,#76414,
#76415,#76416,#76417,#76418,#76419,#76420,#76421,#76422,#76423,#76424,#76425,
#76426,#76427,#76428,#76429,#76430,#76431,#76432,#76433,#76434,#76435,#76436,
#76437,#76438,#76439,#76440,#76441,#76442,#76443,#76444,#76445,#76446,#76447,
#76448,#76449,#76450,#76451,#76452,#76453,#76454,#76455,#76456,#76457,#76458,
#76459,#76460,#76461,#76462,#76463,#76464,#76465,#76466,#76467,#76468,#76469,
#76470,#76471,#76472,#76473,#76474,#76475,#76476,#76477,#76478,#76479,#76480,
#76481,#76482,#76483,#76484,#76485,#76486,#76487,#76488,#76489,#76490,#76491,
#76492,#76493,#76494,#76495,#76496,#76497,#76498,#76499,#76500,#76501,#76502,
#76503,#76504),.UNSPECIFIED.,.F.,.F.,(4,3,3,3,3,3,3,3,3,3,3,3,3,3,3,3,3,
3,3,3,3,3,3,3,3,3,3,3,3,3,3,3,3,3,3,3,3,3,3,3,3,3,3,3,3,3,3,3,3,3,3,3,3,
3,3,3,3,4),(32.5386683423583,32.6554622719273,32.7689870331684,32.8823115160644,
32.9955247985313,33.1086715979755,33.2217965327449,33.3350250501304,33.4483055792554,
33.5617971739282,33.645021734713,33.758546495955,33.8718709788518,33.9850842613196,
34.0982310607647,34.211355995535,34.3245845129214,34.4378650420474,34.5513566367211,
34.6345811974987,34.7481059587407,34.8614304416375,34.9746437241053,35.0877905235503,
35.2009154583206,35.3141439757069,35.4274245048329,35.5409160995067,35.6241406602844,
35.7376654215263,35.850989904423,35.9642031868906,36.0773499863355,36.1904749211056,
36.3037034384918,36.4169839676176,36.5304755622912,36.6137001230701,36.727224884312,
36.8405493672087,36.9537626496764,37.0669094491213,37.1800343838914,37.2932629012777,
37.4065434304035,37.5200350250771,37.6032595858557,37.7167843470976,37.8301088299943,
37.943322112462,38.0564689119069,38.1695938466771,38.2828223640633,38.3961028931892,
38.5095944878629,38.5928190486414,38.7436256884796,38.821853649538),
 .UNSPECIFIED.);
#782=B_SPLINE_CURVE_WITH_KNOTS('',3,(#76506,#76507,#76508,#76509,#76510,
#76511,#76512,#76513,#76514,#76515,#76516,#76517,#76518,#76519,#76520,#76521,
#76522,#76523,#76524,#76525,#76526,#76527,#76528,#76529,#76530,#76531,#76532,
#76533,#76534,#76535,#76536,#76537,#76538,#76539,#76540,#76541,#76542,#76543,
#76544,#76545,#76546,#76547,#76548,#76549,#76550,#76551,#76552,#76553,#76554,
#76555,#76556,#76557,#76558,#76559,#76560,#76561,#76562,#76563,#76564,#76565,
#76566,#76567,#76568,#76569,#76570,#76571,#76572,#76573,#76574,#76575,#76576,
#76577,#76578,#76579,#76580,#76581,#76582,#76583,#76584,#76585,#76586,#76587,
#76588,#76589,#76590,#76591,#76592,#76593,#76594,#76595,#76596,#76597,#76598,
#76599,#76600,#76601,#76602,#76603,#76604,#76605,#76606,#76607,#76608,#76609,
#76610,#76611,#76612,#76613,#76614,#76615,#76616,#76617,#76618,#76619,#76620,
#76621,#76622,#76623,#76624,#76625,#76626,#76627,#76628,#76629,#76630,#76631,
#76632,#76633,#76634,#76635,#76636,#76637,#76638,#76639,#76640,#76641,#76642,
#76643,#76644,#76645,#76646,#76647,#76648,#76649,#76650,#76651,#76652,#76653,
#76654,#76655,#76656,#76657,#76658,#76659,#76660,#76661,#76662,#76663,#76664,
#76665,#76666,#76667,#76668,#76669,#76670,#76671,#76672,#76673,#76674,#76675,
#76676,#76677),.UNSPECIFIED.,.F.,.F.,(4,3,3,3,3,3,3,3,3,3,3,3,3,3,3,3,3,
3,3,3,3,3,3,3,3,3,3,3,3,3,3,3,3,3,3,3,3,3,3,3,3,3,3,3,3,3,3,3,3,3,3,3,3,
3,3,3,3,4),(38.8218536499613,38.933680849631,39.045423619069,39.1571288157185,
39.268922463434,39.3807581546526,39.4928019474818,39.5823785114271,39.695903272669,
39.8092277555658,39.9224410380335,40.0355878374784,40.1487127722487,40.2619412896349,
40.3752218187608,40.4887134134344,40.5719379742128,40.6854627354546,40.7987872183514,
40.912000500819,41.0251473002639,41.1382722350339,41.2515007524201,41.3647812815461,
41.4782728762197,41.5614974369984,41.6750221982403,41.7883466811369,41.9015599636045,
42.0147067630493,42.1278316978194,42.2410602152056,42.3543407443315,42.467832339005,
42.5510568997841,42.664581661026,42.7779061439229,42.8911194263906,43.0042662258358,
43.1173911606058,43.2306196779922,43.3439002071181,43.4573918017918,43.5406163625698,
43.6541411238117,43.7674656067085,43.8806788891762,43.993825688621,44.1069506233916,
44.2201791407778,44.3334596699036,44.4469512645772,44.5301758253555,44.6459654331288,
44.7615021168754,44.8768893229516,44.9921613263788,45.1050389567177),
 .UNSPECIFIED.);
#783=B_SPLINE_CURVE_WITH_KNOTS('',3,(#76679,#76680,#76681,#76682,#76683,
#76684,#76685,#76686,#76687,#76688,#76689,#76690,#76691,#76692,#76693,#76694,
#76695,#76696,#76697,#76698,#76699,#76700,#76701,#76702,#76703,#76704,#76705,
#76706,#76707,#76708,#76709,#76710,#76711,#76712,#76713,#76714,#76715,#76716,
#76717,#76718,#76719,#76720,#76721,#76722,#76723,#76724,#76725,#76726,#76727,
#76728,#76729,#76730,#76731,#76732,#76733,#76734,#76735,#76736,#76737,#76738,
#76739,#76740,#76741,#76742,#76743,#76744,#76745,#76746,#76747,#76748,#76749,
#76750,#76751,#76752,#76753,#76754,#76755,#76756,#76757,#76758,#76759,#76760,
#76761,#76762,#76763,#76764,#76765,#76766,#76767,#76768,#76769,#76770,#76771,
#76772,#76773,#76774,#76775,#76776,#76777,#76778,#76779,#76780,#76781,#76782,
#76783,#76784,#76785,#76786,#76787,#76788,#76789,#76790,#76791,#76792,#76793,
#76794,#76795,#76796,#76797,#76798,#76799,#76800,#76801,#76802,#76803,#76804,
#76805,#76806,#76807,#76808,#76809,#76810,#76811,#76812,#76813,#76814,#76815,
#76816,#76817,#76818,#76819,#76820,#76821,#76822,#76823,#76824,#76825,#76826,
#76827,#76828,#76829,#76830,#76831,#76832,#76833,#76834,#76835,#76836,#76837,
#76838,#76839,#76840,#76841,#76842,#76843,#76844,#76845,#76846,#76847,#76848,
#76849,#76850,#76851,#76852,#76853),.UNSPECIFIED.,.F.,.F.,(4,3,3,3,3,3,
3,3,3,3,3,3,3,3,3,3,3,3,3,3,3,3,3,3,3,3,3,3,3,3,3,3,3,3,3,3,3,3,3,3,3,3,
3,3,3,3,3,3,3,3,3,3,3,3,3,3,3,3,4),(45.1050389573923,45.2284792407024,45.3523119932056,
45.4766794256201,45.5197352881411,45.6332600493829,45.7465845322797,45.8597978147473,
45.9729446141923,46.0860695489624,46.1992980663486,46.3125785954745,46.4260701901482,
46.5092947509268,46.6228195121686,46.7361439950652,46.8493572775328,46.9625040769776,
47.0756290117477,47.1888575291339,47.3021380582597,47.4156296529332,47.4988542137125,
47.6123789749546,47.7257034578515,47.8389167403194,47.9520635397645,48.0651884745348,
48.1784169919213,48.2916975210474,48.4051891157212,48.4884136764982,48.60193843774,
48.7152629206367,48.8284762031042,48.9416230025491,49.0547479373191,49.1679764547053,
49.2812569838311,49.3947485785046,49.4779731392839,49.5914979005253,49.7048223834217,
49.8180356658889,49.9311824653334,50.0443074001032,50.157535917489,50.2708164466145,
50.3843080412877,50.4675326020695,50.5826190597494,50.6948414249508,50.8069563908371,
50.9190104334366,51.0363138909547,51.1484549007705,51.2606600856853,51.3730430728924,
51.3882242635088),.UNSPECIFIED.);
#784=B_SPLINE_CURVE_WITH_KNOTS('',3,(#76855,#76856,#76857,#76858,#76859,
#76860,#76861,#76862,#76863,#76864,#76865,#76866,#76867,#76868,#76869,#76870,
#76871,#76872,#76873,#76874,#76875,#76876,#76877,#76878,#76879,#76880,#76881,
#76882,#76883,#76884,#76885,#76886,#76887,#76888,#76889,#76890,#76891,#76892,
#76893,#76894,#76895,#76896,#76897,#76898,#76899,#76900,#76901,#76902,#76903,
#76904,#76905,#76906,#76907,#76908,#76909,#76910,#76911,#76912,#76913,#76914,
#76915,#76916,#76917,#76918,#76919,#76920,#76921,#76922,#76923,#76924,#76925,
#76926,#76927,#76928,#76929,#76930,#76931,#76932,#76933,#76934,#76935,#76936,
#76937,#76938,#76939,#76940,#76941,#76942,#76943,#76944,#76945,#76946,#76947,
#76948,#76949,#76950,#76951,#76952,#76953,#76954,#76955,#76956,#76957,#76958,
#76959,#76960,#76961,#76962,#76963,#76964,#76965,#76966,#76967,#76968,#76969,
#76970,#76971,#76972,#76973,#76974,#76975,#76976,#76977,#76978,#76979,#76980,
#76981,#76982,#76983,#76984,#76985,#76986,#76987,#76988,#76989,#76990,#76991,
#76992,#76993,#76994,#76995,#76996,#76997,#76998,#76999,#77000,#77001,#77002,
#77003,#77004,#77005,#77006,#77007,#77008,#77009,#77010,#77011,#77012,#77013,
#77014,#77015,#77016,#77017,#77018,#77019,#77020,#77021,#77022,#77023,#77024,
#77025,#77026),.UNSPECIFIED.,.F.,.F.,(4,3,3,3,3,3,3,3,3,3,3,3,3,3,3,3,3,
3,3,3,3,3,3,3,3,3,3,3,3,3,3,3,3,3,3,3,3,3,3,3,3,3,3,3,3,3,3,3,3,3,3,3,3,
3,3,3,3,4),(51.3882242638969,51.4570920648552,51.570616826096,51.6839413089917,
51.7971545914583,51.9103013909022,52.0234263256714,52.1366548430567,52.2499353721816,
52.3634269668544,52.4466515276409,52.5601762888804,52.6735007717747,52.7867140542399,
52.8998608536823,53.01298578845,53.1262143058338,53.2394948349572,53.3529864296283,
53.4362109904266,53.5497357516802,53.6630602345886,53.7762735170679,53.8894203165245,
54.0025452513062,54.1157737687038,54.229054297841,54.3425458925257,54.4257704532122,
54.5392952144374,54.6526196973177,54.7658329797689,54.8789797791976,54.9921047139516,
55.1053332313221,55.2186137604324,55.332105355091,55.4153299159979,55.5288546772276,
55.6421791601119,55.7553924425668,55.8685392419988,55.9816641767559,56.094892694129,
56.2081732232416,56.321664817902,56.4048893787836,56.5184141401249,56.6317386231211,
56.7449519056883,56.8580987052325,56.9712236401015,57.0844521575854,57.1977326868084,
57.3112242815769,57.3944488415693,57.5345561648524,57.6714095706393),
 .UNSPECIFIED.);
#785=B_SPLINE_CURVE_WITH_KNOTS('',3,(#77028,#77029,#77030,#77031,#77032,
#77033,#77034,#77035,#77036,#77037,#77038,#77039,#77040,#77041,#77042,#77043,
#77044,#77045,#77046,#77047,#77048,#77049,#77050,#77051,#77052,#77053,#77054,
#77055,#77056,#77057,#77058,#77059,#77060,#77061,#77062,#77063,#77064,#77065,
#77066,#77067,#77068,#77069,#77070,#77071,#77072,#77073,#77074,#77075,#77076,
#77077,#77078,#77079,#77080,#77081,#77082,#77083,#77084,#77085,#77086,#77087,
#77088,#77089,#77090,#77091,#77092,#77093,#77094,#77095,#77096,#77097,#77098,
#77099,#77100,#77101,#77102,#77103,#77104,#77105,#77106,#77107,#77108,#77109,
#77110,#77111,#77112,#77113,#77114,#77115,#77116,#77117,#77118,#77119,#77120,
#77121,#77122,#77123,#77124,#77125,#77126,#77127,#77128,#77129,#77130,#77131,
#77132,#77133,#77134,#77135,#77136,#77137,#77138,#77139,#77140,#77141,#77142,
#77143,#77144,#77145,#77146,#77147,#77148,#77149,#77150,#77151,#77152,#77153,
#77154,#77155,#77156,#77157,#77158,#77159,#77160,#77161,#77162,#77163,#77164,
#77165,#77166,#77167,#77168,#77169,#77170,#77171,#77172,#77173,#77174,#77175,
#77176,#77177,#77178,#77179,#77180,#77181,#77182,#77183,#77184,#77185,#77186,
#77187,#77188,#77189,#77190,#77191,#77192,#77193,#77194,#77195,#77196,#77197,
#77198,#77199,#77200,#77201,#77202),.UNSPECIFIED.,.F.,.F.,(4,3,3,3,3,3,
3,3,3,3,3,3,3,3,3,3,3,3,3,3,3,3,3,3,3,3,3,3,3,3,3,3,3,3,3,3,3,3,3,3,3,3,
3,3,3,3,3,3,3,3,3,3,3,3,3,3,3,3,4),(57.6714095710766,57.7836618564575,57.8958578534188,
58.0080436898146,58.1203406487452,58.2327029112056,58.3452626102307,58.3840083043549,
58.4975330655654,58.6108575484274,58.7240708308583,58.8372176302646,58.9503425649941,
59.0635710823374,59.1768516114188,59.2903432060463,59.3735677671406,59.4870925291998,
59.6004170129164,59.7136302962048,59.8267770964696,59.9399020320575,60.0531305502517,
60.1664110801815,60.2799026756419,60.3631272299263,60.4766519894433,60.589976470624,
60.7031897513823,60.8163365491278,60.9294614822111,61.0426899979435,61.1559705254315,
61.269462118513,61.352686692712,61.4662114543692,61.5795359376507,61.6927492204843,
61.8058960202756,61.9190209553724,62.0322494730526,62.1455300024545,62.2590215973724,
62.3422461554977,62.4557709232019,62.5690954125922,62.6823087015674,62.795455507522,
62.908580448792,63.0218089726113,63.1350895081424,63.2485811090971,63.3318056182834,
63.4461307719924,63.5602703458314,63.6742546758765,63.7881483652435,63.9020107023695,
63.9545948782563),.UNSPECIFIED.);
#786=B_SPLINE_CURVE_WITH_KNOTS('',3,(#77204,#77205,#77206,#77207,#77208,
#77209,#77210,#77211,#77212,#77213,#77214,#77215,#77216,#77217,#77218,#77219,
#77220,#77221,#77222,#77223,#77224,#77225,#77226,#77227,#77228,#77229,#77230,
#77231,#77232,#77233,#77234,#77235,#77236,#77237,#77238,#77239,#77240,#77241,
#77242,#77243,#77244,#77245,#77246,#77247,#77248,#77249,#77250,#77251,#77252,
#77253,#77254,#77255,#77256,#77257,#77258,#77259,#77260,#77261,#77262,#77263,
#77264,#77265,#77266,#77267,#77268,#77269,#77270,#77271,#77272,#77273,#77274,
#77275,#77276,#77277,#77278,#77279,#77280,#77281,#77282,#77283,#77284,#77285,
#77286,#77287,#77288,#77289,#77290,#77291,#77292,#77293,#77294,#77295,#77296,
#77297,#77298,#77299,#77300,#77301,#77302,#77303,#77304,#77305,#77306,#77307,
#77308,#77309,#77310,#77311,#77312,#77313,#77314,#77315,#77316,#77317,#77318,
#77319,#77320,#77321,#77322,#77323,#77324,#77325,#77326,#77327,#77328,#77329,
#77330,#77331,#77332,#77333,#77334,#77335,#77336,#77337,#77338,#77339,#77340,
#77341,#77342,#77343,#77344,#77345,#77346,#77347,#77348,#77349,#77350,#77351,
#77352,#77353,#77354,#77355,#77356,#77357,#77358,#77359,#77360,#77361,#77362,
#77363,#77364,#77365,#77366,#77367,#77368,#77369,#77370,#77371,#77372,#77373,
#77374,#77375),.UNSPECIFIED.,.F.,.F.,(4,3,3,3,3,3,3,3,3,3,3,3,3,3,3,3,3,
3,3,3,3,3,3,3,3,3,3,3,3,3,3,3,3,3,3,3,3,3,3,3,3,3,3,3,3,3,3,3,3,3,3,3,3,
3,3,3,3,4),(63.9545948786762,64.0820709043049,64.2105457420236,64.321365081069,
64.4348898520805,64.5482143444765,64.6614276362709,64.7745744448554,64.887699388563,
65.0009279145079,65.1142084519941,65.2277000546061,65.3109245438547,65.4244493536668,
65.5377738854928,65.6509872170703,65.7641340657149,65.8772590496844,65.9904876158749,
66.1037681936576,66.2172598361454,66.3004840066404,66.4140086154073,66.5273329461732,
66.6405460768399,66.753692725083,66.8668175095198,66.9800458790991,67.0933262616046,
67.2068177133869,67.2900434694261,67.4035683690671,67.5168929880384,67.6301064050546,
67.7432533372985,67.8563784028926,67.9696070470509,68.0828877008817,68.1963794153923,
68.2796029322117,68.3931280332697,68.5064528597947,68.6196664879459,68.7328136344833,
68.8459389171108,68.9591677807257,69.0724486556885,69.1859405912626,69.2691623949974,
69.3822861022301,69.4952102742419,69.6080242981855,69.7207735977211,69.8335034979201,
69.946337047213,70.0592261968963,70.1723185919593,70.2377801848146),
 .UNSPECIFIED.);
#787=B_SPLINE_CURVE_WITH_KNOTS('',3,(#77377,#77378,#77379,#77380,#77381,
#77382,#77383,#77384,#77385,#77386,#77387,#77388,#77389,#77390,#77391,#77392,
#77393,#77394,#77395,#77396,#77397,#77398,#77399,#77400,#77401,#77402,#77403,
#77404,#77405,#77406,#77407,#77408,#77409,#77410,#77411,#77412,#77413,#77414,
#77415,#77416,#77417,#77418,#77419,#77420,#77421,#77422,#77423,#77424,#77425,
#77426,#77427,#77428,#77429,#77430,#77431,#77432,#77433,#77434,#77435,#77436,
#77437,#77438,#77439,#77440,#77441,#77442,#77443,#77444,#77445,#77446,#77447,
#77448,#77449,#77450,#77451,#77452,#77453,#77454,#77455,#77456,#77457,#77458,
#77459,#77460,#77461,#77462,#77463,#77464,#77465,#77466,#77467,#77468,#77469,
#77470,#77471,#77472,#77473,#77474,#77475,#77476,#77477,#77478,#77479,#77480,
#77481,#77482,#77483,#77484,#77485,#77486,#77487,#77488,#77489,#77490,#77491,
#77492,#77493,#77494,#77495,#77496,#77497,#77498,#77499,#77500,#77501,#77502,
#77503,#77504,#77505,#77506,#77507,#77508,#77509,#77510,#77511,#77512,#77513,
#77514,#77515,#77516,#77517,#77518,#77519,#77520,#77521,#77522,#77523,#77524,
#77525,#77526,#77527,#77528,#77529,#77530,#77531,#77532,#77533,#77534,#77535,
#77536,#77537,#77538,#77539,#77540,#77541,#77542,#77543,#77544,#77545,#77546,
#77547,#77548,#77549,#77550,#77551),.UNSPECIFIED.,.F.,.F.,(4,3,3,3,3,3,
3,3,3,3,3,3,3,3,3,3,3,3,3,3,3,3,3,3,3,3,3,3,3,3,3,3,3,3,3,3,3,3,3,3,3,3,
3,3,3,3,3,3,3,3,3,3,3,3,3,3,3,3,4),(70.2377801854359,70.2587218577831,70.3722482718241,
70.4855743881732,70.5987892909973,70.7119376949459,70.8250642155941,70.93829427782,
71.0515763312372,71.1650693982657,71.2482813205688,71.361808193455,71.4751348264099,
71.5883502806829,71.7014992695103,71.8146264070972,71.9278571300423,72.0411398695331,
72.1546336547418,72.2378407833544,72.3513536455233,72.4646662250971,72.577867610997,
72.6910025419092,72.8041156574683,72.9173325254023,73.0306014822085,73.1440817724136,
73.2274002461401,73.340943030771,73.4542853818596,73.5675164236272,73.6806808427758,
73.7938232268161,73.9070687942867,74.0203661765388,74.1338740986414,74.2169597089258,
74.3304945869268,74.4438295583308,74.5570535478833,74.6702112510593,74.783347264545,
74.8965870376472,75.0098789377407,75.1233819464769,75.2065191717115,75.3199437476938,
75.4331678716963,75.5462807658169,75.6593273258388,75.7723523484109,75.8854822487551,
75.9986647322451,76.1120604195263,76.1960786344971,76.3301552019644,76.4628063366748,
76.5209654922348),.UNSPECIFIED.);
#788=B_SPLINE_CURVE_WITH_KNOTS('',3,(#77553,#77554,#77555,#77556,#77557,
#77558,#77559,#77560,#77561,#77562,#77563,#77564,#77565,#77566,#77567,#77568,
#77569,#77570,#77571,#77572,#77573,#77574,#77575,#77576,#77577,#77578,#77579,
#77580,#77581,#77582,#77583,#77584,#77585,#77586,#77587,#77588,#77589,#77590,
#77591,#77592,#77593,#77594,#77595),.UNSPECIFIED.,.F.,.F.,(4,3,3,3,3,3,
3,3,3,3,3,3,3,3,4),(76.5209654926156,76.6340655761394,76.7471410409961,
76.8603208092053,76.9735499264755,77.0869996187066,77.1856380972828,77.2977002565008,
77.4096095529624,77.52141302601,77.6331575453624,77.7451540359881,77.8569843073373,
77.9690639076012,78.0811435078651),.UNSPECIFIED.);
#789=B_SPLINE_CURVE_WITH_KNOTS('',3,(#77599,#77600,#77601,#77602,#77603,
#77604,#77605,#77606,#77607,#77608,#77609,#77610,#77611,#77612,#77613,#77614,
#77615,#77616,#77617),.UNSPECIFIED.,.F.,.F.,(4,3,3,3,3,3,4),(-80.1543164856399,
-80.0391241641348,-79.9240212140723,-79.8089315194197,-79.6938570316342,
-79.5786881247276,-79.4902472066036),.UNSPECIFIED.);
#790=B_SPLINE_CURVE_WITH_KNOTS('',3,(#77619,#77620,#77621,#77622,#77623,
#77624,#77625,#77626,#77627,#77628,#77629,#77630,#77631,#77632,#77633,#77634,
#77635,#77636,#77637,#77638,#77639,#77640,#77641,#77642,#77643,#77644,#77645,
#77646,#77647,#77648,#77649,#77650,#77651,#77652,#77653,#77654,#77655,#77656,
#77657,#77658,#77659,#77660,#77661,#77662,#77663,#77664,#77665,#77666,#77667,
#77668,#77669,#77670,#77671,#77672,#77673,#77674,#77675,#77676,#77677,#77678,
#77679,#77680,#77681,#77682,#77683,#77684,#77685,#77686,#77687,#77688,#77689,
#77690,#77691,#77692,#77693,#77694,#77695,#77696,#77697,#77698,#77699,#77700,
#77701,#77702,#77703,#77704,#77705,#77706,#77707,#77708,#77709,#77710,#77711,
#77712,#77713,#77714,#77715,#77716,#77717,#77718,#77719,#77720,#77721,#77722,
#77723,#77724,#77725,#77726,#77727,#77728,#77729,#77730,#77731,#77732,#77733,
#77734,#77735,#77736,#77737,#77738,#77739,#77740,#77741,#77742,#77743,#77744,
#77745,#77746,#77747,#77748,#77749,#77750,#77751,#77752,#77753,#77754,#77755,
#77756,#77757,#77758,#77759,#77760,#77761,#77762,#77763,#77764,#77765,#77766,
#77767,#77768,#77769,#77770,#77771,#77772,#77773,#77774,#77775,#77776,#77777,
#77778,#77779,#77780,#77781,#77782,#77783,#77784,#77785,#77786,#77787,#77788,
#77789,#77790,#77791,#77792,#77793),.UNSPECIFIED.,.F.,.F.,(4,3,3,3,3,3,
3,3,3,3,3,3,3,3,3,3,3,3,3,3,3,3,3,3,3,3,3,3,3,3,3,3,3,3,3,3,3,3,3,3,3,3,
3,3,3,3,3,3,3,3,3,3,3,3,3,3,3,3,4),(-79.4902472059884,-79.3517265673382,
-79.2109681612931,-79.1659475766232,-79.0532136190919,-78.9406994479234,
-78.8283078716632,-78.7159927295406,-78.6037079777077,-78.4913266274999,
-78.3788983233038,-78.2662576917523,-78.1775786676064,-78.0640108726353,
-77.9506460297327,-77.8373940448906,-77.7242102710254,-77.6110501621686,
-77.4977899323899,-77.3844793408537,-77.2709617991828,-77.1892097585897,
-77.0755011786657,-76.9619871711567,-76.8485810089956,-76.7352383459469,
-76.6219149308344,-76.5084858806415,-76.3950031491562,-76.281310178521,
-76.200840849573,-76.087393653663,-75.9741482172093,-75.8610148098562,-75.7479485673088,
-75.6349047254006,-75.521757871416,-75.408559211561,-75.2951498661576,-75.2124719405563,
-75.0989187057383,-74.985565332653,-74.872322911805,-74.7591467814323,-74.6459923785403,
-74.5327348079852,-74.4194251795107,-74.3059058225146,-74.2241030315395,
-74.1105453008867,-73.9971867919935,-73.8839388466325,-73.7707568133287,
-73.6575961388973,-73.5443317745932,-73.431015050961,-73.3174881929719,
-73.2357341225228,-73.2070618994239),.UNSPECIFIED.);
#791=B_SPLINE_CURVE_WITH_KNOTS('',3,(#77795,#77796,#77797,#77798,#77799,
#77800,#77801,#77802,#77803,#77804,#77805,#77806,#77807,#77808,#77809,#77810,
#77811,#77812,#77813,#77814,#77815,#77816,#77817,#77818,#77819,#77820,#77821,
#77822,#77823,#77824,#77825,#77826,#77827,#77828,#77829,#77830,#77831,#77832,
#77833,#77834,#77835,#77836,#77837,#77838,#77839,#77840,#77841,#77842,#77843,
#77844,#77845,#77846,#77847,#77848,#77849,#77850,#77851,#77852,#77853,#77854,
#77855,#77856,#77857,#77858,#77859,#77860,#77861,#77862,#77863,#77864,#77865,
#77866,#77867,#77868,#77869,#77870,#77871,#77872,#77873,#77874,#77875,#77876,
#77877,#77878,#77879,#77880,#77881,#77882,#77883,#77884,#77885,#77886,#77887,
#77888,#77889,#77890,#77891,#77892,#77893,#77894,#77895,#77896,#77897,#77898,
#77899,#77900,#77901,#77902,#77903,#77904,#77905,#77906,#77907,#77908,#77909,
#77910,#77911,#77912,#77913,#77914,#77915,#77916,#77917,#77918,#77919,#77920,
#77921,#77922,#77923,#77924,#77925,#77926,#77927,#77928,#77929,#77930,#77931,
#77932,#77933,#77934,#77935,#77936,#77937,#77938,#77939,#77940,#77941,#77942,
#77943,#77944,#77945,#77946,#77947,#77948,#77949,#77950,#77951,#77952,#77953,
#77954,#77955,#77956,#77957,#77958,#77959,#77960,#77961,#77962,#77963,#77964,
#77965,#77966),.UNSPECIFIED.,.F.,.F.,(4,3,3,3,3,3,3,3,3,3,3,3,3,3,3,3,3,
3,3,3,3,3,3,3,3,3,3,3,3,3,3,3,3,3,3,3,3,3,3,3,3,3,3,3,3,3,3,3,3,3,3,3,3,
3,3,3,3,4),(-73.2070618990321,-73.094069831628,-72.9812742087319,-72.8685866160268,
-72.7559614314162,-72.6433531292006,-72.5306393615614,-72.4178673681802,
-72.3048943277318,-72.2473652135061,-72.1338212398093,-72.0204770062008,
-71.9072436423942,-71.7940764694817,-71.680930907221,-71.5676819239201,
-71.4543807539108,-71.3408695399352,-71.2589963044894,-71.1454530983356,
-71.0321095918641,-70.9188769297667,-70.805710431801,-70.6925655163593,
-70.5793171308957,-70.4660165322699,-70.3525058392914,-70.2706273954727,
-70.1570868730669,-70.0437461340144,-69.9305162883949,-69.8173526506773,
-69.7042106340253,-69.5909651837839,-69.4776675450336,-69.3641598157257,
-69.282258486456,-69.1687163625939,-69.0553739871095,-68.9421424849538,
-68.8289771737097,-68.7158334696301,-68.6025863240228,-68.4892869829797,
-68.3757775610722,-68.2938895774393,-68.1803476792412,-68.0670055285297,
-67.9537742504107,-67.8406091620442,-67.7274656792597,-67.6142187506927,
-67.5009196246352,-67.3874104116913,-67.3055206684225,-67.178427761061,
-67.051152176854,-66.9238765926471),.UNSPECIFIED.);
#792=B_SPLINE_CURVE_WITH_KNOTS('',3,(#77968,#77969,#77970,#77971,#77972,
#77973,#77974,#77975,#77976,#77977,#77978,#77979,#77980,#77981,#77982,#77983,
#77984,#77985,#77986,#77987,#77988,#77989,#77990,#77991,#77992,#77993,#77994,
#77995,#77996,#77997,#77998,#77999,#78000,#78001,#78002,#78003,#78004,#78005,
#78006,#78007,#78008,#78009,#78010,#78011,#78012,#78013,#78014,#78015,#78016,
#78017,#78018,#78019,#78020,#78021,#78022,#78023,#78024,#78025,#78026,#78027,
#78028,#78029,#78030,#78031,#78032,#78033,#78034,#78035,#78036,#78037,#78038,
#78039,#78040,#78041,#78042,#78043,#78044,#78045,#78046,#78047,#78048,#78049,
#78050,#78051,#78052,#78053,#78054,#78055,#78056,#78057,#78058,#78059,#78060,
#78061,#78062,#78063,#78064,#78065,#78066,#78067,#78068,#78069,#78070,#78071,
#78072,#78073,#78074,#78075,#78076,#78077,#78078,#78079,#78080,#78081,#78082,
#78083,#78084,#78085,#78086,#78087,#78088,#78089,#78090,#78091,#78092,#78093,
#78094,#78095,#78096,#78097,#78098,#78099,#78100,#78101,#78102,#78103,#78104,
#78105,#78106,#78107,#78108,#78109,#78110,#78111,#78112,#78113,#78114,#78115,
#78116,#78117,#78118,#78119,#78120,#78121,#78122,#78123,#78124,#78125,#78126,
#78127,#78128,#78129,#78130,#78131,#78132,#78133,#78134,#78135,#78136,#78137,
#78138,#78139,#78140,#78141,#78142),.UNSPECIFIED.,.F.,.F.,(4,3,3,3,3,3,
3,3,3,3,3,3,3,3,3,3,3,3,3,3,3,3,3,3,3,3,3,3,3,3,3,3,3,3,3,3,3,3,3,3,3,3,
3,3,3,3,3,3,3,3,3,3,3,3,3,3,3,3,4),(-66.9238765922442,-66.8096120241358,
-66.6953173784797,-66.5808654330042,-66.4663215349714,-66.3515549173767,
-66.3171517594058,-66.2036099273518,-66.0902678470314,-65.9770366418524,
-65.8638716288386,-65.7507282236856,-65.6374813756652,-65.5241823318996,
-65.4106732030888,-65.3287828503891,-65.2152410584719,-65.1018990185986,
-64.9886678540232,-64.8755028816931,-64.7623595172278,-64.649112709571,
-64.5358137060477,-64.4223046167831,-64.3404139413724,-64.2268721714598,
-64.113530154438,-64.0002990132152,-63.8871340646948,-63.7739907244533,
-63.6607439414676,-63.5474449629013,-63.4339358987536,-63.3520450323557,
-63.2385032414485,-63.1251612029106,-63.0119300398699,-62.8987650692705,
-62.7856217067293,-62.6723749012822,-62.5590759001311,-62.4455668134755,
-62.363676123339,-62.2501343384519,-62.136792306014,-62.0235611491169,-61.9103961846934,
-61.7972528283492,-61.6840060290806,-61.570707034107,-61.457197953551,-61.3753072143223,
-61.2630150155433,-61.1508849762602,-61.0388702925052,-60.926894102488,
-60.8149424610336,-60.702909004196,-60.6406912850646),.UNSPECIFIED.);
#793=B_SPLINE_CURVE_WITH_KNOTS('',3,(#78144,#78145,#78146,#78147,#78148,
#78149,#78150,#78151,#78152,#78153,#78154,#78155,#78156,#78157,#78158,#78159,
#78160,#78161,#78162,#78163,#78164,#78165,#78166,#78167,#78168,#78169,#78170,
#78171,#78172,#78173,#78174,#78175,#78176,#78177,#78178,#78179,#78180,#78181,
#78182,#78183,#78184,#78185,#78186,#78187,#78188,#78189,#78190,#78191,#78192,
#78193,#78194,#78195,#78196,#78197,#78198,#78199,#78200,#78201,#78202,#78203,
#78204,#78205,#78206,#78207,#78208,#78209,#78210,#78211,#78212,#78213,#78214,
#78215,#78216,#78217,#78218,#78219,#78220,#78221,#78222,#78223,#78224,#78225,
#78226,#78227,#78228,#78229,#78230,#78231,#78232,#78233,#78234,#78235,#78236,
#78237,#78238,#78239,#78240,#78241,#78242,#78243,#78244,#78245,#78246,#78247,
#78248,#78249,#78250,#78251,#78252,#78253,#78254,#78255,#78256,#78257,#78258,
#78259,#78260,#78261,#78262,#78263,#78264,#78265,#78266,#78267,#78268,#78269,
#78270,#78271,#78272,#78273,#78274,#78275,#78276,#78277,#78278,#78279,#78280,
#78281,#78282,#78283,#78284,#78285,#78286,#78287,#78288,#78289,#78290,#78291,
#78292,#78293,#78294,#78295,#78296,#78297,#78298,#78299,#78300,#78301,#78302,
#78303,#78304,#78305,#78306,#78307,#78308,#78309,#78310,#78311,#78312,#78313,
#78314,#78315),.UNSPECIFIED.,.F.,.F.,(4,3,3,3,3,3,3,3,3,3,3,3,3,3,3,3,3,
3,3,3,3,3,3,3,3,3,3,3,3,3,3,3,3,3,3,3,3,3,3,3,3,3,3,3,3,3,3,3,3,3,3,3,3,
3,3,3,3,4),(-60.6406912846449,-60.4961271710891,-60.3869383053055,-60.2733965198114,
-60.160054486785,-60.0468233293113,-59.9336583643241,-59.8205150074302,
-59.7072682076384,-59.5939692121555,-59.4804601311195,-59.3985693962888,
-59.285027611619,-59.1716855794305,-59.0584544228024,-58.9452894586669,
-58.8321461026291,-58.7188993036937,-58.6056003090684,-58.4920912288815,
-58.4102004872721,-58.2966587026979,-58.1833166706118,-58.0700855140902,
-57.9569205500651,-57.8437771941414,-57.7305303953247,-57.6172314008211,
-57.5037223207591,-57.4218315782554,-57.308289793439,-57.194947761104,-57.0817166043295,
-56.968551640048,-56.855408283865,-56.7421614847864,-56.6288624900191,-56.5153534096935,
-56.4334626692387,-56.3199208845285,-56.2065788523017,-56.0933476956365,
-55.9801827314653,-55.8670393753932,-55.7537925764259,-55.6404935817701,
-55.5269845015553,-55.445093760222,-55.3315519755118,-55.2182099432853,
-55.1049787866209,-54.9918138224506,-54.8786704663798,-54.7654236674143,
-54.6521246727606,-54.5386155925483,-54.4567248512052,-54.3575059778849),
 .UNSPECIFIED.);
#794=B_SPLINE_CURVE_WITH_KNOTS('',3,(#78317,#78318,#78319,#78320,#78321,
#78322,#78323,#78324,#78325,#78326,#78327,#78328,#78329,#78330,#78331,#78332,
#78333,#78334,#78335,#78336,#78337,#78338,#78339,#78340,#78341,#78342,#78343,
#78344,#78345,#78346,#78347,#78348,#78349,#78350,#78351,#78352,#78353,#78354,
#78355,#78356,#78357,#78358,#78359,#78360,#78361,#78362,#78363,#78364,#78365,
#78366,#78367,#78368,#78369,#78370,#78371,#78372,#78373,#78374,#78375,#78376,
#78377,#78378,#78379,#78380,#78381,#78382,#78383,#78384,#78385,#78386,#78387,
#78388,#78389,#78390,#78391,#78392,#78393,#78394,#78395,#78396,#78397,#78398,
#78399,#78400,#78401,#78402,#78403,#78404,#78405,#78406,#78407,#78408,#78409,
#78410,#78411,#78412,#78413,#78414,#78415,#78416,#78417,#78418,#78419,#78420,
#78421,#78422,#78423,#78424,#78425,#78426,#78427,#78428,#78429,#78430,#78431,
#78432,#78433,#78434,#78435,#78436,#78437,#78438,#78439,#78440,#78441,#78442,
#78443,#78444,#78445,#78446,#78447,#78448,#78449,#78450,#78451,#78452,#78453,
#78454,#78455,#78456,#78457,#78458,#78459,#78460,#78461,#78462,#78463,#78464,
#78465,#78466,#78467,#78468,#78469,#78470,#78471,#78472,#78473,#78474,#78475,
#78476,#78477,#78478,#78479,#78480,#78481,#78482,#78483,#78484,#78485,#78486,
#78487,#78488),.UNSPECIFIED.,.F.,.F.,(4,3,3,3,3,3,3,3,3,3,3,3,3,3,3,3,3,
3,3,3,3,3,3,3,3,3,3,3,3,3,3,3,3,3,3,3,3,3,3,3,3,3,3,3,3,3,3,3,3,3,3,3,3,
3,3,3,3,4),(-54.3575059774559,-54.2454588905404,-54.133550138024,-54.021732773941,
-53.9099599987096,-53.7981045612228,-53.686213474605,-53.5741099150809,
-53.4683559421885,-53.3548141574668,-53.2414721252284,-53.1282409685518,
-53.0150760043692,-52.9019326482856,-52.7886858493072,-52.6753868546403,
-52.5618777744148,-52.4799870331718,-52.3664452484487,-52.2531032162091,
-52.1398720595313,-52.0267070953474,-51.9135637392627,-51.8003169402832,
-51.6870179456152,-51.5735088653886,-51.4916181241551,-51.3780763394296,
-51.2647343071875,-51.1515031505072,-51.0383381863207,-50.9251948302337,
-50.8119480312515,-50.6986490365809,-50.5851399563517,-50.5032492151384,
-50.3897074304145,-50.2763653981741,-50.1631342414952,-50.0499692773104,
-49.9368259212247,-49.8235791222442,-49.7102801275752,-49.5967710473476,
-49.5148803061217,-49.4013385213976,-49.2879964891568,-49.1747653324776,
-49.0616003682925,-48.9484570122066,-48.8352102132257,-48.7219112185563,
-48.6084021383284,-48.5265113971049,-48.4049309512446,-48.2836454588316,
-48.1627910448778,-48.0743206711006),.UNSPECIFIED.);
#795=B_SPLINE_CURVE_WITH_KNOTS('',3,(#78490,#78491,#78492,#78493,#78494,
#78495,#78496,#78497,#78498,#78499,#78500,#78501,#78502,#78503,#78504,#78505,
#78506,#78507,#78508,#78509,#78510,#78511,#78512,#78513,#78514,#78515,#78516,
#78517,#78518,#78519,#78520,#78521,#78522,#78523,#78524,#78525,#78526,#78527,
#78528,#78529,#78530,#78531,#78532,#78533,#78534,#78535,#78536,#78537,#78538,
#78539,#78540,#78541,#78542,#78543,#78544,#78545,#78546,#78547,#78548,#78549,
#78550,#78551,#78552,#78553,#78554,#78555,#78556,#78557,#78558,#78559,#78560,
#78561,#78562,#78563,#78564,#78565,#78566,#78567,#78568,#78569,#78570,#78571,
#78572,#78573,#78574,#78575,#78576,#78577,#78578,#78579,#78580,#78581,#78582,
#78583,#78584,#78585,#78586,#78587,#78588,#78589,#78590,#78591,#78592,#78593,
#78594,#78595,#78596,#78597,#78598,#78599,#78600,#78601,#78602,#78603,#78604,
#78605,#78606,#78607,#78608,#78609,#78610,#78611,#78612,#78613,#78614,#78615,
#78616,#78617,#78618,#78619,#78620,#78621,#78622,#78623,#78624,#78625,#78626,
#78627,#78628,#78629,#78630,#78631,#78632,#78633,#78634,#78635,#78636,#78637,
#78638,#78639,#78640,#78641,#78642,#78643,#78644,#78645,#78646,#78647,#78648,
#78649,#78650,#78651,#78652,#78653,#78654,#78655,#78656,#78657,#78658,#78659,
#78660,#78661,#78662,#78663,#78664),.UNSPECIFIED.,.F.,.F.,(4,3,3,3,3,3,
3,3,3,3,3,3,3,3,3,3,3,3,3,3,3,3,3,3,3,3,3,3,3,3,3,3,3,3,3,3,3,3,3,3,3,3,
3,3,3,3,3,3,3,3,3,3,3,3,3,3,3,3,4),(-48.0743206707057,-47.9577457517774,
-47.8409315728867,-47.7239904093878,-47.6067638311109,-47.5381424880882,
-47.424600703364,-47.3112586711233,-47.1980275144443,-47.0848625502592,
-46.9717191941734,-46.8584723951926,-46.7451734005234,-46.6316643202955,
-46.5497735790715,-46.4362317943472,-46.3228897621064,-46.2096586054272,
-46.096493641242,-45.9833502851561,-45.8701034861752,-45.7568044915059,
-45.6432954112779,-45.5614046700548,-45.4478628853305,-45.3345208530897,
-45.2212896964106,-45.1081247322255,-44.9949813761396,-44.8817345771588,
-44.7684355824895,-44.6549265022615,-44.5730357610381,-44.4594939763138,
-44.3461519440729,-44.2329207873937,-44.1197558232086,-44.0066124671228,
-43.8933656681419,-43.7800666734726,-43.6665575932446,-43.5846668520214,
-43.4711250672973,-43.3577830350565,-43.2445518783773,-43.1313869141921,
-43.0182435581061,-42.9049967591252,-42.7916977644559,-42.6781886842278,
-42.5962979430046,-42.4844449995889,-42.3727487802306,-42.2611619429958,
-42.1496373311032,-42.0380799748944,-41.9265002728943,-41.814793727549,
-41.791135364003),.UNSPECIFIED.);
#796=B_SPLINE_CURVE_WITH_KNOTS('',3,(#78666,#78667,#78668,#78669,#78670,
#78671,#78672,#78673,#78674,#78675,#78676,#78677,#78678,#78679,#78680,#78681,
#78682,#78683,#78684,#78685,#78686,#78687,#78688,#78689,#78690,#78691,#78692,
#78693,#78694,#78695,#78696,#78697,#78698,#78699,#78700,#78701,#78702,#78703,
#78704,#78705,#78706,#78707,#78708,#78709,#78710,#78711,#78712,#78713,#78714,
#78715,#78716,#78717,#78718,#78719,#78720,#78721,#78722,#78723,#78724,#78725,
#78726,#78727,#78728,#78729,#78730,#78731,#78732,#78733,#78734,#78735,#78736,
#78737,#78738,#78739,#78740,#78741,#78742,#78743,#78744,#78745,#78746,#78747,
#78748,#78749,#78750,#78751,#78752,#78753,#78754,#78755,#78756,#78757,#78758,
#78759,#78760,#78761,#78762,#78763,#78764,#78765,#78766,#78767,#78768,#78769,
#78770,#78771,#78772,#78773,#78774,#78775,#78776,#78777,#78778,#78779,#78780,
#78781,#78782,#78783,#78784,#78785,#78786,#78787,#78788,#78789,#78790,#78791,
#78792,#78793,#78794,#78795,#78796,#78797,#78798,#78799,#78800,#78801,#78802,
#78803,#78804,#78805,#78806,#78807,#78808,#78809,#78810,#78811,#78812,#78813,
#78814,#78815,#78816,#78817,#78818,#78819,#78820,#78821,#78822,#78823,#78824,
#78825,#78826,#78827,#78828,#78829,#78830,#78831,#78832,#78833,#78834,#78835,
#78836,#78837),.UNSPECIFIED.,.F.,.F.,(4,3,3,3,3,3,3,3,3,3,3,3,3,3,3,3,3,
3,3,3,3,3,3,3,3,3,3,3,3,3,3,3,3,3,3,3,3,3,3,3,3,3,3,3,3,3,3,3,3,3,3,3,3,
3,3,3,3,4),(-41.791135363526,-41.6240474718283,-41.6079290339879,-41.4943872492642,
-41.3810452170238,-41.267814060345,-41.1546490961603,-41.0415057400747,
-40.9282589410942,-40.8149599464254,-40.7014508661978,-40.6195601249712,
-40.506018340247,-40.3926763080061,-40.2794451513269,-40.1662801871417,
-40.0531368310557,-39.9398900320748,-39.8265910374055,-39.7130819571774,
-39.6311912159545,-39.5176494312303,-39.4043073989894,-39.2910762423102,
-39.177911278125,-39.064767922039,-38.951521123058,-38.8382221283887,-38.7247130481606,
-38.6428223069378,-38.5292805222136,-38.4159384899729,-38.3027073332938,
-38.1895423691087,-38.0763990130228,-37.963152214042,-37.8498532193727,
-37.7363441391448,-37.6544533979211,-37.5409116131968,-37.427569580956,
-37.3143384242768,-37.2011734600916,-37.0880301040056,-36.9747833050247,
-36.8614843103553,-36.7479752301273,-36.6660844889043,-36.55254270418,-36.4392006719391,
-36.3259695152599,-36.2128045510747,-36.0996611949886,-35.9864143960077,
-35.8731154013383,-35.7596063211103,-35.6777155798876,-35.5079500563463),
 .UNSPECIFIED.);
#797=B_SPLINE_CURVE_WITH_KNOTS('',3,(#78839,#78840,#78841,#78842,#78843,
#78844,#78845,#78846,#78847,#78848,#78849,#78850,#78851,#78852,#78853,#78854,
#78855,#78856,#78857,#78858,#78859,#78860,#78861,#78862,#78863,#78864,#78865,
#78866,#78867,#78868,#78869,#78870,#78871,#78872,#78873,#78874,#78875,#78876,
#78877,#78878,#78879,#78880,#78881,#78882,#78883,#78884,#78885,#78886,#78887,
#78888,#78889,#78890,#78891,#78892,#78893,#78894,#78895,#78896,#78897,#78898,
#78899,#78900,#78901,#78902,#78903,#78904,#78905,#78906,#78907,#78908,#78909,
#78910,#78911,#78912,#78913,#78914,#78915,#78916,#78917,#78918,#78919,#78920,
#78921,#78922,#78923,#78924,#78925,#78926,#78927,#78928,#78929,#78930,#78931,
#78932,#78933,#78934,#78935,#78936,#78937,#78938,#78939,#78940,#78941,#78942,
#78943,#78944,#78945,#78946,#78947,#78948,#78949,#78950,#78951,#78952,#78953,
#78954,#78955,#78956,#78957,#78958,#78959,#78960,#78961,#78962,#78963,#78964,
#78965,#78966,#78967,#78968,#78969,#78970,#78971,#78972,#78973,#78974,#78975,
#78976,#78977,#78978,#78979,#78980,#78981,#78982,#78983,#78984,#78985,#78986,
#78987,#78988,#78989,#78990,#78991,#78992,#78993,#78994,#78995,#78996,#78997,
#78998,#78999,#79000,#79001,#79002,#79003,#79004,#79005,#79006,#79007,#79008,
#79009,#79010,#79011,#79012,#79013),.UNSPECIFIED.,.F.,.F.,(4,3,3,3,3,3,
3,3,3,3,3,3,3,3,3,3,3,3,3,3,3,3,3,3,3,3,3,3,3,3,3,3,3,3,3,3,3,3,3,3,3,3,
3,3,3,3,3,3,3,3,3,3,3,3,3,3,3,3,4),(-35.5079500557628,-35.39624939281,-35.2846613019993,
-35.1731385997513,-35.0616342152309,-34.9500286488472,-34.8383632661675,
-34.7265074019316,-34.6893466708709,-34.5758048861466,-34.4624628539057,
-34.3492316972264,-34.2360667330411,-34.1229233769552,-34.0096765779742,
-33.8963775833048,-33.7828685030767,-33.7009777618542,-33.5874359771301,
-33.4740939448894,-33.3608627882104,-33.2476978240254,-33.1345544679397,
-33.0213076689589,-32.9080086742896,-32.7944995940618,-32.7126088528375,
-32.5990670681136,-32.4857250358731,-32.3724938791943,-32.2593289150094,
-32.1461855589239,-32.0329387599433,-31.9196397652743,-31.8061306850466,
-31.7242399438208,-31.6106981590953,-31.4973561268532,-31.3841249701728,
-31.2709600059863,-31.1578166498988,-31.0445698509166,-30.9312708562461,
-30.8177617760168,-30.735871034804,-30.6223292500811,-30.5089872178417,
-30.395756061164,-30.2825910969801,-30.1694477408954,-30.0562009419158,
-29.9429019472477,-29.8293928670209,-29.7475021257873,-29.6296432390198,
-29.5120953361175,-29.3947339709123,-29.2775721209935,-29.2247647491666),
 .UNSPECIFIED.);
#798=B_SPLINE_CURVE_WITH_KNOTS('',3,(#79015,#79016,#79017,#79018,#79019,
#79020,#79021,#79022,#79023,#79024,#79025,#79026,#79027,#79028,#79029,#79030,
#79031,#79032,#79033,#79034,#79035,#79036,#79037,#79038,#79039,#79040,#79041,
#79042,#79043,#79044,#79045,#79046,#79047,#79048,#79049,#79050,#79051,#79052,
#79053,#79054,#79055,#79056,#79057,#79058,#79059,#79060,#79061,#79062,#79063,
#79064,#79065,#79066,#79067,#79068,#79069,#79070,#79071,#79072,#79073,#79074,
#79075,#79076,#79077,#79078,#79079,#79080,#79081,#79082,#79083,#79084,#79085,
#79086,#79087,#79088,#79089,#79090,#79091,#79092,#79093,#79094,#79095,#79096,
#79097,#79098,#79099,#79100,#79101,#79102,#79103,#79104,#79105,#79106,#79107,
#79108,#79109,#79110,#79111,#79112,#79113,#79114,#79115,#79116,#79117,#79118,
#79119,#79120,#79121,#79122,#79123,#79124,#79125,#79126,#79127,#79128,#79129,
#79130,#79131,#79132,#79133,#79134,#79135,#79136,#79137,#79138,#79139,#79140,
#79141,#79142,#79143,#79144,#79145,#79146,#79147,#79148,#79149,#79150,#79151,
#79152,#79153,#79154,#79155,#79156,#79157,#79158,#79159,#79160,#79161,#79162,
#79163,#79164,#79165,#79166,#79167,#79168,#79169,#79170,#79171,#79172,#79173,
#79174,#79175,#79176,#79177,#79178,#79179,#79180,#79181,#79182,#79183,#79184,
#79185,#79186),.UNSPECIFIED.,.F.,.F.,(4,3,3,3,3,3,3,3,3,3,3,3,3,3,3,3,3,
3,3,3,3,3,3,3,3,3,3,3,3,3,3,3,3,3,3,3,3,3,3,3,3,3,3,3,3,3,3,3,3,3,3,3,3,
3,3,3,3,4),(-29.2247647486182,-29.1046697390539,-28.9843458860535,-28.8635945576143,
-28.7591332167706,-28.6455914320349,-28.5322493997827,-28.4190182430922,
-28.3058532788957,-28.1927099227984,-28.0794631238063,-27.966164129126,
-27.8526550488872,-27.7707643077539,-27.6572225230454,-27.5438804908201,
-27.4306493341564,-27.3174843699866,-27.2043410139158,-27.0910942149496,
-26.9777952202949,-26.8642861400811,-26.7823953987372,-26.6688536140261,
-26.5555115817988,-26.4422804251333,-26.329115460962,-26.21597210489,-26.1027253059232,
-25.989426311268,-25.8759172310541,-25.7940264897205,-25.6804847048989,
-25.5671426725605,-25.4539115157839,-25.3407465515014,-25.2276031953185,
-25.1143563962419,-25.0010574014776,-24.8875483211567,-24.8056575807037,
-24.6921157961455,-24.5787737640694,-24.4655426075542,-24.3523776435318,
-24.2392342876072,-24.1259874887841,-24.0126884942709,-23.8991794141944,
-23.817288671687,-23.7052818012017,-23.5934297836473,-23.4816854814853,
-23.3700019323537,-23.258264522408,-23.1465049263617,-23.0345659897191,
-22.9415794424194),.UNSPECIFIED.);
#799=B_SPLINE_CURVE_WITH_KNOTS('',3,(#79188,#79189,#79190,#79191,#79192,
#79193,#79194,#79195,#79196,#79197,#79198,#79199,#79200,#79201,#79202,#79203,
#79204,#79205,#79206,#79207,#79208,#79209,#79210,#79211,#79212,#79213,#79214,
#79215,#79216,#79217,#79218,#79219,#79220,#79221,#79222,#79223,#79224,#79225,
#79226,#79227,#79228,#79229,#79230,#79231,#79232,#79233,#79234,#79235,#79236,
#79237,#79238,#79239,#79240,#79241,#79242,#79243,#79244,#79245,#79246,#79247,
#79248,#79249,#79250,#79251,#79252,#79253,#79254,#79255,#79256,#79257,#79258,
#79259,#79260,#79261,#79262,#79263,#79264,#79265,#79266,#79267,#79268,#79269,
#79270,#79271,#79272,#79273,#79274,#79275,#79276,#79277,#79278,#79279,#79280,
#79281,#79282,#79283,#79284,#79285,#79286,#79287,#79288,#79289,#79290,#79291,
#79292,#79293,#79294,#79295,#79296,#79297,#79298,#79299,#79300,#79301,#79302,
#79303,#79304,#79305,#79306,#79307,#79308,#79309,#79310,#79311,#79312,#79313,
#79314,#79315,#79316,#79317,#79318,#79319,#79320,#79321,#79322,#79323,#79324,
#79325,#79326,#79327,#79328,#79329,#79330,#79331,#79332,#79333,#79334,#79335,
#79336,#79337,#79338,#79339,#79340,#79341,#79342,#79343,#79344,#79345,#79346,
#79347,#79348,#79349,#79350,#79351,#79352,#79353,#79354,#79355,#79356,#79357,
#79358,#79359),.UNSPECIFIED.,.F.,.F.,(4,3,3,3,3,3,3,3,3,3,3,3,3,3,3,3,3,
3,3,3,3,3,3,3,3,3,3,3,3,3,3,3,3,3,3,3,3,3,3,3,3,3,3,3,3,3,3,3,3,3,3,3,3,
3,3,3,3,4),(-22.941579441987,-22.8289197626703,-22.7153779771406,-22.6020359440922,
-22.4888047866046,-22.3756398216119,-22.2624964647207,-22.1492496649442,
-22.0359506694838,-21.9224415884814,-21.8405508536536,-21.7270090705954,
-21.6136670400118,-21.5004358849831,-21.3872709224387,-21.2741275679811,
-21.1608807705963,-21.0475817775076,-20.9340726988158,-20.8521819446369,
-20.7386401595786,-20.6252981270335,-20.5120669700684,-20.398902005616,
-20.2857586492819,-20.1725118500836,-20.0592128552139,-19.9457037748149,
-19.8638130356202,-19.7502712444879,-19.6369292058091,-19.523698042679,
-19.4105330720417,-19.2973897095143,-19.1841429041596,-19.0708439031449,
-18.9573348166956,-18.8754441266034,-18.7619023579417,-18.6485603417033,
-18.5353292009772,-18.4221642526673,-18.3090209123506,-18.1957741288513,
-18.0824751495262,-17.9689660842323,-17.8870752175867,-17.7735334237832,
-17.6601913827284,-17.5469602174043,-17.4337952447568,-17.3206518804049,
-17.2074050735226,-17.0941060711434,-16.9805969836074,-16.89870630857,-16.7510332120614,
-16.6583941353321),.UNSPECIFIED.);
#800=B_SPLINE_CURVE_WITH_KNOTS('',3,(#79361,#79362,#79363,#79364,#79365,
#79366,#79367,#79368,#79369,#79370,#79371,#79372,#79373,#79374,#79375,#79376,
#79377,#79378,#79379,#79380,#79381,#79382,#79383,#79384,#79385,#79386,#79387,
#79388,#79389,#79390,#79391,#79392,#79393,#79394,#79395,#79396,#79397,#79398,
#79399,#79400,#79401,#79402,#79403,#79404,#79405,#79406,#79407,#79408,#79409,
#79410,#79411,#79412,#79413,#79414,#79415,#79416,#79417,#79418,#79419,#79420,
#79421,#79422,#79423,#79424,#79425,#79426,#79427,#79428,#79429,#79430,#79431,
#79432,#79433,#79434,#79435,#79436,#79437,#79438,#79439,#79440,#79441,#79442,
#79443,#79444,#79445,#79446,#79447,#79448,#79449,#79450,#79451,#79452,#79453,
#79454,#79455,#79456,#79457,#79458,#79459,#79460,#79461,#79462,#79463,#79464,
#79465,#79466,#79467,#79468,#79469,#79470,#79471,#79472,#79473,#79474,#79475,
#79476,#79477,#79478,#79479,#79480,#79481,#79482,#79483,#79484,#79485,#79486,
#79487,#79488,#79489,#79490,#79491,#79492,#79493,#79494,#79495,#79496,#79497,
#79498,#79499,#79500,#79501,#79502,#79503,#79504,#79505,#79506,#79507,#79508,
#79509,#79510,#79511,#79512,#79513,#79514,#79515,#79516,#79517,#79518,#79519,
#79520,#79521,#79522,#79523,#79524,#79525,#79526,#79527,#79528,#79529,#79530,
#79531,#79532,#79533,#79534,#79535),.UNSPECIFIED.,.F.,.F.,(4,3,3,3,3,3,
3,3,3,3,3,3,3,3,3,3,3,3,3,3,3,3,3,3,3,3,3,3,3,3,3,3,3,3,3,3,3,3,3,3,3,3,
3,3,3,3,3,3,3,3,3,3,3,3,3,3,3,3,4),(-16.6583941348077,-16.5464691647472,
-16.4346221070533,-16.3228062630273,-16.2108970233939,-16.0989402980712,
-15.9867792411841,-15.9103373995533,-15.796795764382,-15.683453881344,-15.5702228735346,
-15.4570580576209,-15.3439148489425,-15.2306681948749,-15.1173693439421,
-15.0038604037858,-14.9219684905366,-14.8084265728354,-14.6950844099091,
-14.5818531240481,-14.4686880324003,-14.3555445507884,-14.2422976302287,
-14.1289985160019,-14.0154893209314,-13.9335995815199,-13.8200574566352,
-13.7067150805103,-13.5934835779487,-13.4803182665326,-13.3671745625144,
-13.2539274173268,-13.140628076904,-13.0271186559336,-12.9452306725032,
-12.831690236357,-12.7183495513293,-12.6051197399521,-12.4919561167483,
-12.3788140949112,-12.2655686092554,-12.1522709181811,-12.0387631098226,
-11.9568617634864,-11.8433183648221,-11.7299747377807,-11.6167419992646,
-11.5035754689113,-11.3904305650464,-11.277182258624,-11.163881776779,-11.0503712602273,
-10.9684928544697,-10.853324442696,-10.733795538929,-10.6190059812326,-10.5043180362164,
-10.3896917480248,-10.375208827628),.UNSPECIFIED.);
#801=B_SPLINE_CURVE_WITH_KNOTS('',3,(#79536,#79537,#79538,#79539,#79540,
#79541,#79542,#79543,#79544,#79545,#79546,#79547,#79548,#79549,#79550,#79551,
#79552,#79553,#79554,#79555,#79556,#79557,#79558,#79559,#79560,#79561,#79562,
#79563,#79564,#79565,#79566,#79567,#79568,#79569,#79570,#79571,#79572,#79573,
#79574,#79575,#79576,#79577,#79578,#79579,#79580,#79581,#79582,#79583,#79584,
#79585,#79586,#79587,#79588,#79589,#79590,#79591,#79592,#79593,#79594,#79595,
#79596,#79597,#79598,#79599,#79600,#79601,#79602,#79603,#79604,#79605,#79606,
#79607,#79608,#79609,#79610,#79611,#79612,#79613,#79614,#79615,#79616,#79617,
#79618,#79619,#79620,#79621,#79622,#79623,#79624,#79625,#79626,#79627,#79628,
#79629,#79630,#79631,#79632,#79633,#79634,#79635,#79636,#79637,#79638,#79639,
#79640,#79641,#79642,#79643,#79644,#79645,#79646,#79647,#79648,#79649,#79650,
#79651,#79652,#79653,#79654,#79655,#79656,#79657,#79658,#79659,#79660,#79661,
#79662,#79663,#79664,#79665,#79666,#79667,#79668,#79669,#79670,#79671,#79672,
#79673,#79674,#79675,#79676,#79677,#79678,#79679,#79680,#79681,#79682,#79683,
#79684,#79685,#79686,#79687,#79688,#79689,#79690,#79691,#79692,#79693,#79694,
#79695,#79696,#79697,#79698,#79699,#79700,#79701,#79702,#79703,#79704,#79705,
#79706,#79707,#79708,#79709,#79710),.UNSPECIFIED.,.F.,.F.,(4,3,3,3,3,3,
3,3,3,3,3,3,3,3,3,3,3,3,3,3,3,3,3,3,3,3,3,3,3,3,3,3,3,3,3,3,3,3,3,3,3,3,
3,3,3,3,3,3,3,3,3,3,3,3,3,3,3,3,4),(-10.3752088272474,-10.2502773954362,
-10.1248700505524,-9.99887819217141,-9.980123945453,-9.86659394391158,-9.75326369870371,
-9.64004432201014,-9.52689110957821,-9.41375945581954,-9.30052419031302,
-9.18723665200623,-9.07373876275237,-8.99175503643628,-8.87819547394066,
-8.76483581781232,-8.65158714539727,-8.53840480407569,-8.42524424003464,
-8.31198062809963,-8.19866501599926,-8.08513983703984,-8.00338612741957,
-7.88983416985714,-7.77648159669808,-7.66323968282041,-7.55006376726034,
-7.4369092874615,-7.32365119238403,-7.21034078897404,-7.09682026133563,
-7.01501721840285,-6.9015749348315,-6.78833257589082,-6.675201120441,-6.56213570727318,
-6.44909157391288,-6.33594270730992,-6.22274107269596,-6.10932722940379,
-6.02664830938613,-5.91292273846379,-5.79939809503559,-5.68598519987283,
-5.57263969617861,-5.45931732698102,-5.34589527909879,-5.23242288611039,
-5.11874551146585,-5.03827940036942,-4.91999754158034,-4.807427696645,-4.69496234793574,
-4.58255554919585,-4.47016144711192,-4.35766024245203,-4.24509639495919,
-4.13233837516928,-4.0920245300568),.UNSPECIFIED.);
#802=B_SPLINE_CURVE_WITH_KNOTS('',3,(#79713,#79714,#79715,#79716,#79717,
#79718,#79719,#79720,#79721,#79722,#79723,#79724,#79725,#79726,#79727,#79728,
#79729,#79730,#79731),.UNSPECIFIED.,.F.,.F.,(4,3,3,3,3,3,4),(84.1188182559913,
84.2377747874144,84.3566749310004,84.4756604736118,84.5946823768654,84.7139370724539,
84.8230016464385),.UNSPECIFIED.);
#803=B_SPLINE_CURVE_WITH_KNOTS('',3,(#79733,#79734,#79735,#79736,#79737,
#79738,#79739,#79740,#79741,#79742,#79743,#79744,#79745,#79746,#79747,#79748,
#79749,#79750,#79751,#79752,#79753,#79754,#79755,#79756,#79757,#79758,#79759,
#79760,#79761,#79762,#79763,#79764,#79765,#79766,#79767,#79768,#79769,#79770,
#79771,#79772,#79773,#79774,#79775,#79776,#79777,#79778,#79779,#79780,#79781,
#79782,#79783,#79784,#79785,#79786,#79787,#79788,#79789,#79790,#79791,#79792,
#79793,#79794,#79795,#79796,#79797,#79798,#79799,#79800,#79801,#79802,#79803,
#79804,#79805,#79806,#79807,#79808,#79809,#79810,#79811,#79812,#79813,#79814,
#79815,#79816,#79817,#79818,#79819,#79820,#79821,#79822,#79823,#79824,#79825,
#79826,#79827,#79828,#79829,#79830,#79831,#79832,#79833,#79834,#79835,#79836,
#79837,#79838,#79839,#79840,#79841,#79842,#79843,#79844,#79845,#79846,#79847,
#79848,#79849,#79850,#79851,#79852,#79853,#79854,#79855,#79856,#79857,#79858,
#79859,#79860,#79861,#79862,#79863,#79864,#79865,#79866,#79867,#79868),
 .UNSPECIFIED.,.F.,.F.,(4,3,3,3,3,3,3,3,3,3,3,3,3,3,3,3,3,3,3,3,3,3,3,3,
3,3,3,3,3,3,3,3,3,3,3,3,3,3,3,3,3,3,3,3,3,4),(84.8230016469245,84.8516738700234,
84.9752199836505,85.0948937895338,85.214449654091,85.333940114396,85.4534175942909,
85.5730147644292,85.6926850173288,85.8125664477791,85.8400427790401,85.9635888926672,
86.0832552402075,86.2028040127739,86.3222877573057,86.4417589080134,86.5613503570413,
86.6810152388168,86.8008918518797,86.8284116880568,86.9519578016839,87.0715076090144,
87.1909396478129,87.3103067004851,87.4296614364613,87.5491377425846,87.6686881070327,
87.7884522382243,87.8167805970736,87.9403267107007,88.0601748712716,88.1799041213034,
88.2995666497992,88.4192145310629,88.5389783935626,88.658813324919,88.7788549188096,
88.8051495060903,88.9234621670989,89.0416062513237,89.1596371181447,89.2776099218732,
89.3956552369875,89.5137386349911,89.6320206411716,89.6970539997882),
 .UNSPECIFIED.);
#804=B_SPLINE_CURVE_WITH_KNOTS('',3,(#79871,#79872,#79873,#79874,#79875,
#79876,#79877,#79878,#79879,#79880,#79881,#79882,#79883,#79884,#79885,#79886,
#79887,#79888,#79889,#79890,#79891,#79892,#79893,#79894,#79895,#79896,#79897,
#79898,#79899,#79900,#79901,#79902,#79903,#79904,#79905,#79906,#79907,#79908,
#79909,#79910,#79911,#79912,#79913,#79914,#79915,#79916,#79917,#79918,#79919,
#79920,#79921,#79922,#79923,#79924,#79925,#79926,#79927,#79928,#79929,#79930,
#79931,#79932,#79933,#79934,#79935,#79936,#79937,#79938,#79939,#79940,#79941,
#79942,#79943,#79944,#79945,#79946,#79947,#79948,#79949,#79950,#79951,#79952,
#79953,#79954,#79955,#79956,#79957,#79958,#79959,#79960,#79961,#79962,#79963,
#79964,#79965,#79966,#79967,#79968,#79969,#79970,#79971,#79972,#79973,#79974,
#79975,#79976,#79977,#79978,#79979,#79980,#79981,#79982,#79983,#79984,#79985,
#79986,#79987,#79988,#79989,#79990,#79991,#79992,#79993,#79994,#79995,#79996,
#79997,#79998,#79999,#80000),.UNSPECIFIED.,.F.,.F.,(4,2,2,2,2,2,2,2,2,2,
2,2,2,2,2,2,2,2,2,2,2,2,2,2,2,2,2,2,2,2,2,2,2,2,2,2,2,2,2,2,2,2,2,2,2,2,
2,2,2,2,2,2,2,2,2,2,2,2,2,2,2,2,2,2,4),(-1.17147551345429,-1.17041713686015,
-1.16918572837233,-1.16564844753094,-1.15001847616683,-1.13401607500194,
-1.12438570179208,-1.12034552846442,-1.11728048252947,-1.11390493508872,
-1.10821504990784,-1.07769516555731,-1.06001325769979,-1.05697285375094,
-1.05522549263754,-1.05366084578698,-1.05176762634352,-1.04708474465781,
-1.02547499614846,-1.02080515614898,-1.01014525025442,-1.00266167458256,
-0.999233957057352,-0.99657391708826,-0.993604704512768,-0.988546528493683,
-0.958921768333237,-0.947339080328778,-0.942844249513928,-0.939450345775342,
-0.937694002922724,-0.93615756660019,-0.934128090749497,-0.929626737542632,
-0.907385479409659,-0.890014022000379,-0.883313757805212,-0.879927605904625,
-0.877421985882495,-0.874256697322647,-0.868830559115028,-0.845641155737674,
-0.832099312629197,-0.824837146876158,-0.822399814519567,-0.820768075456655,
-0.819036637907101,-0.816078805539853,-0.80128721868014,-0.780639481455452,
-0.769373270357963,-0.765314122595176,-0.762461090514392,-0.759533291233767,
-0.755085518342012,-0.741459818616593,-0.71796640205416,-0.708404813167555,
-0.705765778738023,-0.704107888407975,-0.702660192915801,-0.700237000373645,
-0.693413487796553,-0.673264483182991,-0.659170325149453),.UNSPECIFIED.);
#805=B_SPLINE_CURVE_WITH_KNOTS('',3,(#80338,#80339,#80340,#80341,#80342,
#80343,#80344,#80345,#80346,#80347,#80348,#80349,#80350,#80351,#80352,#80353,
#80354,#80355,#80356,#80357,#80358,#80359,#80360,#80361,#80362,#80363,#80364,
#80365),.UNSPECIFIED.,.F.,.F.,(4,2,2,2,2,2,2,2,2,2,2,2,2,4),(-0.863984233696383,
-0.800933779317784,-0.743377583289618,-0.694285453635929,-0.646603013239699,
-0.594660249030955,-0.546279950529435,-0.49124254158724,-0.424015568120234,
-0.331555083406496,-0.269861277973257,-0.218601022857884,-0.163097142851994,
-0.161658288922872),.UNSPECIFIED.);
#806=B_SPLINE_CURVE_WITH_KNOTS('',3,(#80367,#80368,#80369,#80370,#80371,
#80372,#80373,#80374,#80375,#80376,#80377,#80378,#80379,#80380,#80381,#80382,
#80383,#80384,#80385,#80386,#80387,#80388,#80389,#80390,#80391,#80392,#80393,
#80394,#80395,#80396,#80397,#80398,#80399,#80400,#80401,#80402,#80403,#80404,
#80405,#80406,#80407,#80408,#80409,#80410,#80411,#80412,#80413,#80414,#80415,
#80416,#80417,#80418,#80419,#80420,#80421,#80422,#80423,#80424,#80425,#80426,
#80427,#80428,#80429,#80430,#80431,#80432,#80433,#80434,#80435,#80436,#80437,
#80438,#80439,#80440,#80441,#80442,#80443,#80444,#80445,#80446,#80447,#80448),
 .UNSPECIFIED.,.F.,.F.,(4,3,3,3,3,3,3,3,3,3,3,3,3,3,3,3,3,3,3,3,3,3,3,3,
3,3,3,4),(-0.272951148249661,-0.261636095840719,-0.24446844212677,-0.238751575154802,
-0.234137442773466,-0.216941407287095,-0.205360589642349,-0.200111031359439,
-0.196872097333499,-0.180187285724421,-0.163773299048735,-0.153903690818833,
-0.149145887979538,-0.14599519523252,-0.130113230624166,-0.124294866129125,
-0.108025584337116,-0.100828807434257,-0.0956114852142788,-0.0925945277179398,
-0.0768292134716253,-0.0611421123676899,-0.0532933939326321,-0.0475091511222262,
-0.0447106207682135,-0.0296049810521806,-0.0148024905260903,0.),
 .UNSPECIFIED.);
#807=B_SPLINE_CURVE_WITH_KNOTS('',3,(#80449,#80450,#80451,#80452),
 .UNSPECIFIED.,.F.,.F.,(4,4),(-0.0239932585534707,0.),.UNSPECIFIED.);
#808=B_SPLINE_CURVE_WITH_KNOTS('',3,(#80453,#80454,#80455,#80456,#80457,
#80458,#80459,#80460,#80461,#80462),.UNSPECIFIED.,.F.,.F.,(4,2,2,2,4),(-0.161658288922872,
-0.117667468158224,-0.0654756477726669,-0.0331448228557106,0.),
 .UNSPECIFIED.);
#809=B_SPLINE_CURVE_WITH_KNOTS('',3,(#80466,#80467,#80468,#80469,#80470,
#80471,#80472,#80473,#80474,#80475,#80476,#80477,#80478,#80479,#80480,#80481,
#80482,#80483,#80484,#80485,#80486,#80487,#80488,#80489,#80490,#80491,#80492,
#80493,#80494,#80495,#80496,#80497,#80498,#80499,#80500,#80501,#80502,#80503,
#80504,#80505,#80506,#80507,#80508,#80509,#80510,#80511,#80512,#80513,#80514,
#80515,#80516,#80517,#80518,#80519,#80520,#80521,#80522,#80523,#80524,#80525,
#80526,#80527,#80528,#80529,#80530,#80531,#80532,#80533,#80534,#80535,#80536,
#80537,#80538,#80539,#80540,#80541,#80542,#80543,#80544,#80545,#80546,#80547,
#80548,#80549,#80550),.UNSPECIFIED.,.F.,.F.,(4,3,3,3,3,3,3,3,3,3,3,3,3,
3,3,3,3,3,3,3,3,3,3,3,3,3,3,3,4),(-0.276631791712707,-0.2650733968956,-0.250399139533073,
-0.245003811270574,-0.241631211936854,-0.226360488171095,-0.215462829699367,
-0.211534219543691,-0.208388336956343,-0.192443228773931,-0.176580182967181,
-0.167229942324703,-0.162420312376621,-0.159532045368187,-0.143007019282824,
-0.139179220397272,-0.123204100204565,-0.115503843941779,-0.110594323382493,
-0.107673881166793,-0.0909437463342994,-0.0742136115018059,-0.0647340377437841,
-0.0583028985454159,-0.0537579646197444,-0.0363036304783943,-0.018705463131119,
-0.0011072957838437,0.),.UNSPECIFIED.);
#810=B_SPLINE_CURVE_WITH_KNOTS('',3,(#80880,#80881,#80882,#80883,#80884,
#80885,#80886,#80887,#80888,#80889,#80890,#80891,#80892,#80893),
 .UNSPECIFIED.,.F.,.F.,(4,2,2,2,2,2,4),(-0.204007502680633,-0.147316619177464,
-0.101895409296879,-0.0794299502568435,-0.0610500978728551,-0.0287479058543795,
0.),.UNSPECIFIED.);
#820=SHAPE_REPRESENTATION_RELATIONSHIP('SRR','None',#81139,#830);
#830=ADVANCED_BREP_SHAPE_REPRESENTATION('',(#850),#81039);
#840=STYLED_ITEM('',(#81198),#850);
#850=MANIFOLD_SOLID_BREP('Body1',#15093);
#1068=CYLINDRICAL_SURFACE('',#16513,1.17775);
#1069=CYLINDRICAL_SURFACE('',#16515,1.17775);
#1070=CYLINDRICAL_SURFACE('',#16517,1.17775);
#1071=CYLINDRICAL_SURFACE('',#16518,1.17775);
#1072=CYLINDRICAL_SURFACE('',#16519,1.17775);
#1073=CYLINDRICAL_SURFACE('',#16520,1.17775);
#1074=CYLINDRICAL_SURFACE('',#16521,1.17775);
#1075=CYLINDRICAL_SURFACE('',#16522,1.17775);
#1076=CYLINDRICAL_SURFACE('',#16523,1.17775);
#1077=CYLINDRICAL_SURFACE('',#16524,1.17775);
#1078=CYLINDRICAL_SURFACE('',#16525,1.17775);
#1079=CYLINDRICAL_SURFACE('',#16526,1.17775);
#1080=CYLINDRICAL_SURFACE('',#16527,1.4635);
#1081=CYLINDRICAL_SURFACE('',#16530,1.17775);
#1082=CYLINDRICAL_SURFACE('',#16546,2.75);
#1210=FACE_BOUND('',#3209,.T.);
#1598=PLANE('',#16532);
#1599=PLANE('',#16538);
#1600=PLANE('',#16540);
#1601=PLANE('',#16544);
#1602=PLANE('',#16545);
#1603=PLANE('',#16549);
#1604=PLANE('',#16551);
#1605=PLANE('',#16554);
#2320=FACE_OUTER_BOUND('',#3190,.T.);
#2321=FACE_OUTER_BOUND('',#3191,.T.);
#2322=FACE_OUTER_BOUND('',#3192,.T.);
#2323=FACE_OUTER_BOUND('',#3193,.T.);
#2324=FACE_OUTER_BOUND('',#3194,.T.);
#2325=FACE_OUTER_BOUND('',#3195,.T.);
#2326=FACE_OUTER_BOUND('',#3196,.T.);
#2327=FACE_OUTER_BOUND('',#3197,.T.);
#2328=FACE_OUTER_BOUND('',#3198,.T.);
#2329=FACE_OUTER_BOUND('',#3199,.T.);
#2330=FACE_OUTER_BOUND('',#3200,.T.);
#2331=FACE_OUTER_BOUND('',#3201,.T.);
#2332=FACE_OUTER_BOUND('',#3202,.T.);
#2333=FACE_OUTER_BOUND('',#3203,.T.);
#2334=FACE_OUTER_BOUND('',#3204,.T.);
#2335=FACE_OUTER_BOUND('',#3205,.T.);
#2336=FACE_OUTER_BOUND('',#3206,.T.);
#2337=FACE_OUTER_BOUND('',#3207,.T.);
#2338=FACE_OUTER_BOUND('',#3208,.T.);
#2339=FACE_OUTER_BOUND('',#3210,.T.);
#2340=FACE_OUTER_BOUND('',#3211,.T.);
#2341=FACE_OUTER_BOUND('',#3212,.T.);
#2342=FACE_OUTER_BOUND('',#3213,.T.);
#2343=FACE_OUTER_BOUND('',#3214,.T.);
#2344=FACE_OUTER_BOUND('',#3215,.T.);
#2345=FACE_OUTER_BOUND('',#3216,.T.);
#2346=FACE_OUTER_BOUND('',#3217,.T.);
#2347=FACE_OUTER_BOUND('',#3218,.T.);
#2348=FACE_OUTER_BOUND('',#3219,.T.);
#3190=EDGE_LOOP('',(#14000,#14001,#14002));
#3191=EDGE_LOOP('',(#14003,#14004,#14005,#14006,#14007,#14008));
#3192=EDGE_LOOP('',(#14009,#14010,#14011,#14012,#14013));
#3193=EDGE_LOOP('',(#14014,#14015,#14016,#14017,#14018));
#3194=EDGE_LOOP('',(#14019,#14020,#14021,#14022,#14023));
#3195=EDGE_LOOP('',(#14024,#14025,#14026,#14027,#14028,#14029));
#3196=EDGE_LOOP('',(#14030,#14031,#14032,#14033,#14034));
#3197=EDGE_LOOP('',(#14035,#14036,#14037,#14038,#14039,#14040));
#3198=EDGE_LOOP('',(#14041,#14042,#14043,#14044,#14045));
#3199=EDGE_LOOP('',(#14046,#14047,#14048,#14049,#14050,#14051));
#3200=EDGE_LOOP('',(#14052,#14053,#14054,#14055,#14056));
#3201=EDGE_LOOP('',(#14057,#14058,#14059,#14060,#14061,#14062));
#3202=EDGE_LOOP('',(#14063,#14064,#14065,#14066,#14067,#14068,#14069,#14070,
#14071,#14072,#14073,#14074,#14075,#14076,#14077,#14078,#14079,#14080,#14081,
#14082,#14083,#14084,#14085,#14086,#14087,#14088,#14089,#14090,#14091,#14092));
#3203=EDGE_LOOP('',(#14093,#14094,#14095,#14096,#14097));
#3204=EDGE_LOOP('',(#14098,#14099,#14100,#14101,#14102,#14103,#14104,#14105,
#14106,#14107,#14108,#14109,#14110,#14111,#14112,#14113,#14114,#14115,#14116,
#14117,#14118,#14119,#14120,#14121,#14122,#14123,#14124,#14125,#14126,#14127,
#14128,#14129,#14130,#14131,#14132));
#3205=EDGE_LOOP('',(#14133,#14134,#14135,#14136,#14137));
#3206=EDGE_LOOP('',(#14138,#14139,#14140,#14141,#14142,#14143,#14144,#14145,
#14146,#14147,#14148,#14149,#14150,#14151,#14152,#14153,#14154,#14155,#14156,
#14157,#14158,#14159,#14160,#14161,#14162,#14163,#14164,#14165,#14166,#14167,
#14168,#14169,#14170,#14171,#14172,#14173,#14174,#14175,#14176,#14177));
#3207=EDGE_LOOP('',(#14178,#14179,#14180,#14181,#14182,#14183,#14184));
#3208=EDGE_LOOP('',(#14185));
#3209=EDGE_LOOP('',(#14186));
#3210=EDGE_LOOP('',(#14187,#14188,#14189,#14190,#14191));
#3211=EDGE_LOOP('',(#14192,#14193,#14194,#14195,#14196,#14197));
#3212=EDGE_LOOP('',(#14198,#14199,#14200,#14201,#14202,#14203));
#3213=EDGE_LOOP('',(#14204,#14205,#14206,#14207,#14208,#14209,#14210,#14211,
#14212,#14213,#14214,#14215));
#3214=EDGE_LOOP('',(#14216,#14217));
#3215=EDGE_LOOP('',(#14218,#14219));
#3216=EDGE_LOOP('',(#14220,#14221,#14222,#14223));
#3217=EDGE_LOOP('',(#14224));
#3218=EDGE_LOOP('',(#14225,#14226,#14227,#14228,#14229,#14230,#14231,#14232,
#14233));
#3219=EDGE_LOOP('',(#14234,#14235,#14236,#14237));
#4310=LINE('',#71462,#5422);
#4311=LINE('',#71518,#5423);
#4312=LINE('',#71886,#5424);
#4313=LINE('',#72252,#5425);
#4314=LINE('',#72618,#5426);
#4315=LINE('',#72992,#5427);
#4316=LINE('',#73367,#5428);
#4317=LINE('',#73718,#5429);
#4318=LINE('',#73946,#5430);
#4319=LINE('',#74318,#5431);
#4320=LINE('',#74693,#5432);
#4321=LINE('',#75067,#5433);
#4322=LINE('',#80906,#5434);
#4323=LINE('',#80910,#5435);
#4324=LINE('',#80914,#5436);
#4325=LINE('',#80916,#5437);
#4326=LINE('',#80922,#5438);
#4327=LINE('',#80928,#5439);
#4328=LINE('',#80934,#5440);
#4329=LINE('',#80939,#5441);
#4330=LINE('',#80941,#5442);
#4331=LINE('',#80953,#5443);
#5422=VECTOR('',#20328,1.17775);
#5423=VECTOR('',#20333,1.17775);
#5424=VECTOR('',#20338,1.17775);
#5425=VECTOR('',#20341,1.17775);
#5426=VECTOR('',#20344,1.17775);
#5427=VECTOR('',#20347,1.17775);
#5428=VECTOR('',#20350,1.17775);
#5429=VECTOR('',#20353,1.17775);
#5430=VECTOR('',#20356,1.17775);
#5431=VECTOR('',#20359,1.17775);
#5432=VECTOR('',#20362,1.17775);
#5433=VECTOR('',#20365,1.17775);
#5434=VECTOR('',#20396,10.);
#5435=VECTOR('',#20399,10.);
#5436=VECTOR('',#20404,10.);
#5437=VECTOR('',#20405,10.);
#5438=VECTOR('',#20406,10.);
#5439=VECTOR('',#20409,10.);
#5440=VECTOR('',#20410,10.);
#5441=VECTOR('',#20411,10.);
#5442=VECTOR('',#20414,2.75);
#5443=VECTOR('',#20435,1.325);
#6003=CIRCLE('',#16514,1.17775);
#6004=CIRCLE('',#16516,1.17775);
#6005=CIRCLE('',#16528,1.4635);
#6006=CIRCLE('',#16529,1.4635);
#6007=CIRCLE('',#16531,1.17775);
#6008=CIRCLE('',#16533,1.4635);
#6009=CIRCLE('',#16534,1.4635);
#6010=CIRCLE('',#16536,1.5635);
#6011=CIRCLE('',#16537,0.1);
#6012=CIRCLE('',#16539,2.75);
#6013=CIRCLE('',#16541,2.75);
#6014=CIRCLE('',#16542,2.75);
#6015=CIRCLE('',#16543,2.75);
#6016=CIRCLE('',#16547,2.75);
#6017=CIRCLE('',#16548,2.75);
#6018=CIRCLE('',#16550,2.35);
#6019=CIRCLE('',#16552,2.35);
#6020=CIRCLE('',#16555,1.15);
#7461=VERTEX_POINT('',#71460);
#7462=VERTEX_POINT('',#71461);
#7463=VERTEX_POINT('',#71463);
#7464=VERTEX_POINT('',#71516);
#7465=VERTEX_POINT('',#71517);
#7466=VERTEX_POINT('',#71713);
#7467=VERTEX_POINT('',#71715);
#7468=VERTEX_POINT('',#71884);
#7469=VERTEX_POINT('',#71885);
#7470=VERTEX_POINT('',#72075);
#7471=VERTEX_POINT('',#72250);
#7472=VERTEX_POINT('',#72251);
#7473=VERTEX_POINT('',#72441);
#7474=VERTEX_POINT('',#72616);
#7475=VERTEX_POINT('',#72617);
#7476=VERTEX_POINT('',#72815);
#7477=VERTEX_POINT('',#72990);
#7478=VERTEX_POINT('',#72991);
#7479=VERTEX_POINT('',#72993);
#7480=VERTEX_POINT('',#73190);
#7481=VERTEX_POINT('',#73365);
#7482=VERTEX_POINT('',#73366);
#7483=VERTEX_POINT('',#73544);
#7484=VERTEX_POINT('',#73716);
#7485=VERTEX_POINT('',#73717);
#7486=VERTEX_POINT('',#73719);
#7487=VERTEX_POINT('',#73914);
#7488=VERTEX_POINT('',#73944);
#7489=VERTEX_POINT('',#73945);
#7490=VERTEX_POINT('',#74155);
#7491=VERTEX_POINT('',#74316);
#7492=VERTEX_POINT('',#74317);
#7493=VERTEX_POINT('',#74319);
#7494=VERTEX_POINT('',#74516);
#7495=VERTEX_POINT('',#74691);
#7496=VERTEX_POINT('',#74692);
#7497=VERTEX_POINT('',#74890);
#7498=VERTEX_POINT('',#75065);
#7499=VERTEX_POINT('',#75066);
#7500=VERTEX_POINT('',#75068);
#7501=VERTEX_POINT('',#75269);
#7502=VERTEX_POINT('',#75444);
#7503=VERTEX_POINT('',#75445);
#7504=VERTEX_POINT('',#75453);
#7505=VERTEX_POINT('',#75455);
#7506=VERTEX_POINT('',#75461);
#7507=VERTEX_POINT('',#75634);
#7508=VERTEX_POINT('',#75810);
#7509=VERTEX_POINT('',#75983);
#7510=VERTEX_POINT('',#76159);
#7511=VERTEX_POINT('',#76332);
#7512=VERTEX_POINT('',#76505);
#7513=VERTEX_POINT('',#76678);
#7514=VERTEX_POINT('',#76854);
#7515=VERTEX_POINT('',#77027);
#7516=VERTEX_POINT('',#77203);
#7517=VERTEX_POINT('',#77376);
#7518=VERTEX_POINT('',#77552);
#7519=VERTEX_POINT('',#77596);
#7520=VERTEX_POINT('',#77598);
#7521=VERTEX_POINT('',#77618);
#7522=VERTEX_POINT('',#77794);
#7523=VERTEX_POINT('',#77967);
#7524=VERTEX_POINT('',#78143);
#7525=VERTEX_POINT('',#78316);
#7526=VERTEX_POINT('',#78489);
#7527=VERTEX_POINT('',#78665);
#7528=VERTEX_POINT('',#78838);
#7529=VERTEX_POINT('',#79014);
#7530=VERTEX_POINT('',#79187);
#7531=VERTEX_POINT('',#79360);
#7532=VERTEX_POINT('',#79712);
#7533=VERTEX_POINT('',#79732);
#7534=VERTEX_POINT('',#79869);
#7535=VERTEX_POINT('',#80337);
#7536=VERTEX_POINT('',#80366);
#7537=VERTEX_POINT('',#80464);
#7538=VERTEX_POINT('',#80895);
#7539=VERTEX_POINT('',#80899);
#7540=VERTEX_POINT('',#80902);
#7541=VERTEX_POINT('',#80903);
#7542=VERTEX_POINT('',#80905);
#7543=VERTEX_POINT('',#80907);
#7544=VERTEX_POINT('',#80909);
#7545=VERTEX_POINT('',#80913);
#7546=VERTEX_POINT('',#80915);
#7547=VERTEX_POINT('',#80917);
#7548=VERTEX_POINT('',#80921);
#7549=VERTEX_POINT('',#80927);
#7550=VERTEX_POINT('',#80929);
#7551=VERTEX_POINT('',#80933);
#7552=VERTEX_POINT('',#80935);
#7553=VERTEX_POINT('',#80950);
#9663=EDGE_CURVE('',#7461,#7462,#4310,.T.);
#9664=EDGE_CURVE('',#7463,#7461,#736,.F.);
#9665=EDGE_CURVE('',#7462,#7463,#6003,.T.);
#9666=EDGE_CURVE('',#7464,#7465,#4311,.T.);
#9667=EDGE_CURVE('',#7461,#7464,#737,.F.);
#9668=EDGE_CURVE('',#7466,#7462,#6004,.T.);
#9669=EDGE_CURVE('',#7466,#7467,#738,.T.);
#9670=EDGE_CURVE('',#7467,#7465,#739,.T.);
#9671=EDGE_CURVE('',#7468,#7469,#4312,.T.);
#9672=EDGE_CURVE('',#7464,#7468,#740,.F.);
#9673=EDGE_CURVE('',#7465,#7470,#741,.T.);
#9674=EDGE_CURVE('',#7470,#7469,#742,.T.);
#9675=EDGE_CURVE('',#7471,#7472,#4313,.T.);
#9676=EDGE_CURVE('',#7468,#7471,#743,.F.);
#9677=EDGE_CURVE('',#7469,#7473,#744,.T.);
#9678=EDGE_CURVE('',#7473,#7472,#745,.T.);
#9679=EDGE_CURVE('',#7474,#7475,#4314,.T.);
#9680=EDGE_CURVE('',#7471,#7474,#746,.F.);
#9681=EDGE_CURVE('',#7472,#7476,#747,.T.);
#9682=EDGE_CURVE('',#7476,#7475,#748,.T.);
#9683=EDGE_CURVE('',#7477,#7478,#4315,.T.);
#9684=EDGE_CURVE('',#7479,#7477,#749,.F.);
#9685=EDGE_CURVE('',#7474,#7479,#750,.F.);
#9686=EDGE_CURVE('',#7475,#7480,#751,.T.);
#9687=EDGE_CURVE('',#7480,#7478,#752,.T.);
#9688=EDGE_CURVE('',#7481,#7482,#4316,.T.);
#9689=EDGE_CURVE('',#7477,#7481,#753,.F.);
#9690=EDGE_CURVE('',#7478,#7483,#754,.T.);
#9691=EDGE_CURVE('',#7483,#7482,#755,.T.);
#9692=EDGE_CURVE('',#7484,#7485,#4317,.T.);
#9693=EDGE_CURVE('',#7486,#7484,#756,.F.);
#9694=EDGE_CURVE('',#7481,#7486,#757,.F.);
#9695=EDGE_CURVE('',#7482,#7487,#758,.T.);
#9696=EDGE_CURVE('',#7487,#7485,#759,.T.);
#9697=EDGE_CURVE('',#7488,#7489,#4318,.T.);
#9698=EDGE_CURVE('',#7484,#7488,#760,.F.);
#9699=EDGE_CURVE('',#7485,#7490,#761,.T.);
#9700=EDGE_CURVE('',#7490,#7489,#762,.T.);
#9701=EDGE_CURVE('',#7491,#7492,#4319,.T.);
#9702=EDGE_CURVE('',#7493,#7491,#763,.F.);
#9703=EDGE_CURVE('',#7488,#7493,#764,.F.);
#9704=EDGE_CURVE('',#7489,#7494,#765,.T.);
#9705=EDGE_CURVE('',#7494,#7492,#766,.T.);
#9706=EDGE_CURVE('',#7495,#7496,#4320,.T.);
#9707=EDGE_CURVE('',#7491,#7495,#767,.F.);
#9708=EDGE_CURVE('',#7492,#7497,#768,.T.);
#9709=EDGE_CURVE('',#7497,#7496,#769,.T.);
#9710=EDGE_CURVE('',#7498,#7499,#4321,.T.);
#9711=EDGE_CURVE('',#7500,#7498,#770,.F.);
#9712=EDGE_CURVE('',#7495,#7500,#771,.F.);
#9713=EDGE_CURVE('',#7496,#7501,#772,.T.);
#9714=EDGE_CURVE('',#7501,#7499,#773,.T.);
#9715=EDGE_CURVE('',#7502,#7503,#774,.T.);
#9716=EDGE_CURVE('',#7503,#7504,#6005,.T.);
#9717=EDGE_CURVE('',#7504,#7505,#775,.T.);
#9718=EDGE_CURVE('',#7505,#7506,#776,.T.);
#9719=EDGE_CURVE('',#7506,#7507,#777,.T.);
#9720=EDGE_CURVE('',#7507,#7508,#778,.T.);
#9721=EDGE_CURVE('',#7508,#7509,#779,.T.);
#9722=EDGE_CURVE('',#7509,#7510,#780,.T.);
#9723=EDGE_CURVE('',#7510,#7511,#781,.T.);
#9724=EDGE_CURVE('',#7511,#7512,#782,.T.);
#9725=EDGE_CURVE('',#7512,#7513,#783,.T.);
#9726=EDGE_CURVE('',#7513,#7514,#784,.T.);
#9727=EDGE_CURVE('',#7514,#7515,#785,.T.);
#9728=EDGE_CURVE('',#7515,#7516,#786,.T.);
#9729=EDGE_CURVE('',#7516,#7517,#787,.T.);
#9730=EDGE_CURVE('',#7517,#7518,#788,.T.);
#9731=EDGE_CURVE('',#7519,#7518,#6006,.T.);
#9732=EDGE_CURVE('',#7519,#7520,#789,.T.);
#9733=EDGE_CURVE('',#7520,#7521,#790,.T.);
#9734=EDGE_CURVE('',#7521,#7522,#791,.T.);
#9735=EDGE_CURVE('',#7522,#7523,#792,.T.);
#9736=EDGE_CURVE('',#7523,#7524,#793,.T.);
#9737=EDGE_CURVE('',#7524,#7525,#794,.T.);
#9738=EDGE_CURVE('',#7525,#7526,#795,.T.);
#9739=EDGE_CURVE('',#7526,#7527,#796,.T.);
#9740=EDGE_CURVE('',#7527,#7528,#797,.T.);
#9741=EDGE_CURVE('',#7528,#7529,#798,.T.);
#9742=EDGE_CURVE('',#7529,#7530,#799,.T.);
#9743=EDGE_CURVE('',#7530,#7531,#800,.T.);
#9744=EDGE_CURVE('',#7531,#7502,#801,.T.);
#9745=EDGE_CURVE('',#7499,#7532,#802,.T.);
#9746=EDGE_CURVE('',#7532,#7533,#803,.T.);
#9747=EDGE_CURVE('',#7534,#7533,#6007,.T.);
#9748=EDGE_CURVE('',#7498,#7534,#804,.F.);
#9749=EDGE_CURVE('',#7463,#7535,#805,.T.);
#9750=EDGE_CURVE('',#7536,#7534,#806,.T.);
#9751=EDGE_CURVE('',#7518,#7536,#807,.T.);
#9752=EDGE_CURVE('',#7535,#7504,#808,.T.);
#9753=EDGE_CURVE('',#7536,#7537,#6008,.T.);
#9754=EDGE_CURVE('',#7533,#7519,#809,.T.);
#9755=EDGE_CURVE('',#7537,#7519,#6009,.T.);
#9756=EDGE_CURVE('',#7503,#7466,#810,.T.);
#9757=EDGE_CURVE('',#7538,#7538,#6010,.T.);
#9758=EDGE_CURVE('',#7538,#7537,#6011,.T.);
#9759=EDGE_CURVE('',#7539,#7539,#6012,.T.);
#9760=EDGE_CURVE('',#7540,#7541,#6013,.T.);
#9761=EDGE_CURVE('',#7542,#7540,#4322,.T.);
#9762=EDGE_CURVE('',#7543,#7542,#6014,.T.);
#9763=EDGE_CURVE('',#7544,#7543,#4323,.T.);
#9764=EDGE_CURVE('',#7541,#7544,#6015,.T.);
#9765=EDGE_CURVE('',#7544,#7545,#4324,.T.);
#9766=EDGE_CURVE('',#7546,#7543,#4325,.T.);
#9767=EDGE_CURVE('',#7547,#7546,#356,.T.);
#9768=EDGE_CURVE('',#7548,#7547,#4326,.T.);
#9769=EDGE_CURVE('',#7545,#7548,#357,.T.);
#9770=EDGE_CURVE('',#7549,#7540,#4327,.T.);
#9771=EDGE_CURVE('',#7550,#7549,#358,.T.);
#9772=EDGE_CURVE('',#7551,#7550,#4328,.T.);
#9773=EDGE_CURVE('',#7552,#7551,#359,.T.);
#9774=EDGE_CURVE('',#7542,#7552,#4329,.T.);
#9775=EDGE_CURVE('',#7541,#7539,#4330,.T.);
#9776=EDGE_CURVE('',#7546,#7545,#6016,.T.);
#9777=EDGE_CURVE('',#7549,#7552,#6017,.T.);
#9778=EDGE_CURVE('',#7547,#7548,#6018,.T.);
#9779=EDGE_CURVE('',#7550,#7551,#6019,.T.);
#9780=EDGE_CURVE('',#7553,#7553,#6020,.T.);
#9781=EDGE_CURVE('',#7553,#7535,#4331,.T.);
#14000=ORIENTED_EDGE('',*,*,#9663,.F.);
#14001=ORIENTED_EDGE('',*,*,#9664,.F.);
#14002=ORIENTED_EDGE('',*,*,#9665,.F.);
#14003=ORIENTED_EDGE('',*,*,#9666,.F.);
#14004=ORIENTED_EDGE('',*,*,#9667,.F.);
#14005=ORIENTED_EDGE('',*,*,#9663,.T.);
#14006=ORIENTED_EDGE('',*,*,#9668,.F.);
#14007=ORIENTED_EDGE('',*,*,#9669,.T.);
#14008=ORIENTED_EDGE('',*,*,#9670,.T.);
#14009=ORIENTED_EDGE('',*,*,#9671,.F.);
#14010=ORIENTED_EDGE('',*,*,#9672,.F.);
#14011=ORIENTED_EDGE('',*,*,#9666,.T.);
#14012=ORIENTED_EDGE('',*,*,#9673,.T.);
#14013=ORIENTED_EDGE('',*,*,#9674,.T.);
#14014=ORIENTED_EDGE('',*,*,#9675,.F.);
#14015=ORIENTED_EDGE('',*,*,#9676,.F.);
#14016=ORIENTED_EDGE('',*,*,#9671,.T.);
#14017=ORIENTED_EDGE('',*,*,#9677,.T.);
#14018=ORIENTED_EDGE('',*,*,#9678,.T.);
#14019=ORIENTED_EDGE('',*,*,#9679,.F.);
#14020=ORIENTED_EDGE('',*,*,#9680,.F.);
#14021=ORIENTED_EDGE('',*,*,#9675,.T.);
#14022=ORIENTED_EDGE('',*,*,#9681,.T.);
#14023=ORIENTED_EDGE('',*,*,#9682,.T.);
#14024=ORIENTED_EDGE('',*,*,#9683,.F.);
#14025=ORIENTED_EDGE('',*,*,#9684,.F.);
#14026=ORIENTED_EDGE('',*,*,#9685,.F.);
#14027=ORIENTED_EDGE('',*,*,#9679,.T.);
#14028=ORIENTED_EDGE('',*,*,#9686,.T.);
#14029=ORIENTED_EDGE('',*,*,#9687,.T.);
#14030=ORIENTED_EDGE('',*,*,#9688,.F.);
#14031=ORIENTED_EDGE('',*,*,#9689,.F.);
#14032=ORIENTED_EDGE('',*,*,#9683,.T.);
#14033=ORIENTED_EDGE('',*,*,#9690,.T.);
#14034=ORIENTED_EDGE('',*,*,#9691,.T.);
#14035=ORIENTED_EDGE('',*,*,#9692,.F.);
#14036=ORIENTED_EDGE('',*,*,#9693,.F.);
#14037=ORIENTED_EDGE('',*,*,#9694,.F.);
#14038=ORIENTED_EDGE('',*,*,#9688,.T.);
#14039=ORIENTED_EDGE('',*,*,#9695,.T.);
#14040=ORIENTED_EDGE('',*,*,#9696,.T.);
#14041=ORIENTED_EDGE('',*,*,#9697,.F.);
#14042=ORIENTED_EDGE('',*,*,#9698,.F.);
#14043=ORIENTED_EDGE('',*,*,#9692,.T.);
#14044=ORIENTED_EDGE('',*,*,#9699,.T.);
#14045=ORIENTED_EDGE('',*,*,#9700,.T.);
#14046=ORIENTED_EDGE('',*,*,#9701,.F.);
#14047=ORIENTED_EDGE('',*,*,#9702,.F.);
#14048=ORIENTED_EDGE('',*,*,#9703,.F.);
#14049=ORIENTED_EDGE('',*,*,#9697,.T.);
#14050=ORIENTED_EDGE('',*,*,#9704,.T.);
#14051=ORIENTED_EDGE('',*,*,#9705,.T.);
#14052=ORIENTED_EDGE('',*,*,#9706,.F.);
#14053=ORIENTED_EDGE('',*,*,#9707,.F.);
#14054=ORIENTED_EDGE('',*,*,#9701,.T.);
#14055=ORIENTED_EDGE('',*,*,#9708,.T.);
#14056=ORIENTED_EDGE('',*,*,#9709,.T.);
#14057=ORIENTED_EDGE('',*,*,#9710,.F.);
#14058=ORIENTED_EDGE('',*,*,#9711,.F.);
#14059=ORIENTED_EDGE('',*,*,#9712,.F.);
#14060=ORIENTED_EDGE('',*,*,#9706,.T.);
#14061=ORIENTED_EDGE('',*,*,#9713,.T.);
#14062=ORIENTED_EDGE('',*,*,#9714,.T.);
#14063=ORIENTED_EDGE('',*,*,#9715,.T.);
#14064=ORIENTED_EDGE('',*,*,#9716,.T.);
#14065=ORIENTED_EDGE('',*,*,#9717,.T.);
#14066=ORIENTED_EDGE('',*,*,#9718,.T.);
#14067=ORIENTED_EDGE('',*,*,#9719,.T.);
#14068=ORIENTED_EDGE('',*,*,#9720,.T.);
#14069=ORIENTED_EDGE('',*,*,#9721,.T.);
#14070=ORIENTED_EDGE('',*,*,#9722,.T.);
#14071=ORIENTED_EDGE('',*,*,#9723,.T.);
#14072=ORIENTED_EDGE('',*,*,#9724,.T.);
#14073=ORIENTED_EDGE('',*,*,#9725,.T.);
#14074=ORIENTED_EDGE('',*,*,#9726,.T.);
#14075=ORIENTED_EDGE('',*,*,#9727,.T.);
#14076=ORIENTED_EDGE('',*,*,#9728,.T.);
#14077=ORIENTED_EDGE('',*,*,#9729,.T.);
#14078=ORIENTED_EDGE('',*,*,#9730,.T.);
#14079=ORIENTED_EDGE('',*,*,#9731,.F.);
#14080=ORIENTED_EDGE('',*,*,#9732,.T.);
#14081=ORIENTED_EDGE('',*,*,#9733,.T.);
#14082=ORIENTED_EDGE('',*,*,#9734,.T.);
#14083=ORIENTED_EDGE('',*,*,#9735,.T.);
#14084=ORIENTED_EDGE('',*,*,#9736,.T.);
#14085=ORIENTED_EDGE('',*,*,#9737,.T.);
#14086=ORIENTED_EDGE('',*,*,#9738,.T.);
#14087=ORIENTED_EDGE('',*,*,#9739,.T.);
#14088=ORIENTED_EDGE('',*,*,#9740,.T.);
#14089=ORIENTED_EDGE('',*,*,#9741,.T.);
#14090=ORIENTED_EDGE('',*,*,#9742,.T.);
#14091=ORIENTED_EDGE('',*,*,#9743,.T.);
#14092=ORIENTED_EDGE('',*,*,#9744,.T.);
#14093=ORIENTED_EDGE('',*,*,#9710,.T.);
#14094=ORIENTED_EDGE('',*,*,#9745,.T.);
#14095=ORIENTED_EDGE('',*,*,#9746,.T.);
#14096=ORIENTED_EDGE('',*,*,#9747,.F.);
#14097=ORIENTED_EDGE('',*,*,#9748,.F.);
#14098=ORIENTED_EDGE('',*,*,#9749,.F.);
#14099=ORIENTED_EDGE('',*,*,#9664,.T.);
#14100=ORIENTED_EDGE('',*,*,#9667,.T.);
#14101=ORIENTED_EDGE('',*,*,#9672,.T.);
#14102=ORIENTED_EDGE('',*,*,#9676,.T.);
#14103=ORIENTED_EDGE('',*,*,#9680,.T.);
#14104=ORIENTED_EDGE('',*,*,#9685,.T.);
#14105=ORIENTED_EDGE('',*,*,#9684,.T.);
#14106=ORIENTED_EDGE('',*,*,#9689,.T.);
#14107=ORIENTED_EDGE('',*,*,#9694,.T.);
#14108=ORIENTED_EDGE('',*,*,#9693,.T.);
#14109=ORIENTED_EDGE('',*,*,#9698,.T.);
#14110=ORIENTED_EDGE('',*,*,#9703,.T.);
#14111=ORIENTED_EDGE('',*,*,#9702,.T.);
#14112=ORIENTED_EDGE('',*,*,#9707,.T.);
#14113=ORIENTED_EDGE('',*,*,#9712,.T.);
#14114=ORIENTED_EDGE('',*,*,#9711,.T.);
#14115=ORIENTED_EDGE('',*,*,#9748,.T.);
#14116=ORIENTED_EDGE('',*,*,#9750,.F.);
#14117=ORIENTED_EDGE('',*,*,#9751,.F.);
#14118=ORIENTED_EDGE('',*,*,#9730,.F.);
#14119=ORIENTED_EDGE('',*,*,#9729,.F.);
#14120=ORIENTED_EDGE('',*,*,#9728,.F.);
#14121=ORIENTED_EDGE('',*,*,#9727,.F.);
#14122=ORIENTED_EDGE('',*,*,#9726,.F.);
#14123=ORIENTED_EDGE('',*,*,#9725,.F.);
#14124=ORIENTED_EDGE('',*,*,#9724,.F.);
#14125=ORIENTED_EDGE('',*,*,#9723,.F.);
#14126=ORIENTED_EDGE('',*,*,#9722,.F.);
#14127=ORIENTED_EDGE('',*,*,#9721,.F.);
#14128=ORIENTED_EDGE('',*,*,#9720,.F.);
#14129=ORIENTED_EDGE('',*,*,#9719,.F.);
#14130=ORIENTED_EDGE('',*,*,#9718,.F.);
#14131=ORIENTED_EDGE('',*,*,#9717,.F.);
#14132=ORIENTED_EDGE('',*,*,#9752,.F.);
#14133=ORIENTED_EDGE('',*,*,#9753,.F.);
#14134=ORIENTED_EDGE('',*,*,#9750,.T.);
#14135=ORIENTED_EDGE('',*,*,#9747,.T.);
#14136=ORIENTED_EDGE('',*,*,#9754,.T.);
#14137=ORIENTED_EDGE('',*,*,#9755,.F.);
#14138=ORIENTED_EDGE('',*,*,#9756,.F.);
#14139=ORIENTED_EDGE('',*,*,#9715,.F.);
#14140=ORIENTED_EDGE('',*,*,#9744,.F.);
#14141=ORIENTED_EDGE('',*,*,#9743,.F.);
#14142=ORIENTED_EDGE('',*,*,#9742,.F.);
#14143=ORIENTED_EDGE('',*,*,#9741,.F.);
#14144=ORIENTED_EDGE('',*,*,#9740,.F.);
#14145=ORIENTED_EDGE('',*,*,#9739,.F.);
#14146=ORIENTED_EDGE('',*,*,#9738,.F.);
#14147=ORIENTED_EDGE('',*,*,#9737,.F.);
#14148=ORIENTED_EDGE('',*,*,#9736,.F.);
#14149=ORIENTED_EDGE('',*,*,#9735,.F.);
#14150=ORIENTED_EDGE('',*,*,#9734,.F.);
#14151=ORIENTED_EDGE('',*,*,#9733,.F.);
#14152=ORIENTED_EDGE('',*,*,#9732,.F.);
#14153=ORIENTED_EDGE('',*,*,#9754,.F.);
#14154=ORIENTED_EDGE('',*,*,#9746,.F.);
#14155=ORIENTED_EDGE('',*,*,#9745,.F.);
#14156=ORIENTED_EDGE('',*,*,#9714,.F.);
#14157=ORIENTED_EDGE('',*,*,#9713,.F.);
#14158=ORIENTED_EDGE('',*,*,#9709,.F.);
#14159=ORIENTED_EDGE('',*,*,#9708,.F.);
#14160=ORIENTED_EDGE('',*,*,#9705,.F.);
#14161=ORIENTED_EDGE('',*,*,#9704,.F.);
#14162=ORIENTED_EDGE('',*,*,#9700,.F.);
#14163=ORIENTED_EDGE('',*,*,#9699,.F.);
#14164=ORIENTED_EDGE('',*,*,#9696,.F.);
#14165=ORIENTED_EDGE('',*,*,#9695,.F.);
#14166=ORIENTED_EDGE('',*,*,#9691,.F.);
#14167=ORIENTED_EDGE('',*,*,#9690,.F.);
#14168=ORIENTED_EDGE('',*,*,#9687,.F.);
#14169=ORIENTED_EDGE('',*,*,#9686,.F.);
#14170=ORIENTED_EDGE('',*,*,#9682,.F.);
#14171=ORIENTED_EDGE('',*,*,#9681,.F.);
#14172=ORIENTED_EDGE('',*,*,#9678,.F.);
#14173=ORIENTED_EDGE('',*,*,#9677,.F.);
#14174=ORIENTED_EDGE('',*,*,#9674,.F.);
#14175=ORIENTED_EDGE('',*,*,#9673,.F.);
#14176=ORIENTED_EDGE('',*,*,#9670,.F.);
#14177=ORIENTED_EDGE('',*,*,#9669,.F.);
#14178=ORIENTED_EDGE('',*,*,#9757,.T.);
#14179=ORIENTED_EDGE('',*,*,#9758,.T.);
#14180=ORIENTED_EDGE('',*,*,#9755,.T.);
#14181=ORIENTED_EDGE('',*,*,#9731,.T.);
#14182=ORIENTED_EDGE('',*,*,#9751,.T.);
#14183=ORIENTED_EDGE('',*,*,#9753,.T.);
#14184=ORIENTED_EDGE('',*,*,#9758,.F.);
#14185=ORIENTED_EDGE('',*,*,#9759,.F.);
#14186=ORIENTED_EDGE('',*,*,#9757,.F.);
#14187=ORIENTED_EDGE('',*,*,#9760,.F.);
#14188=ORIENTED_EDGE('',*,*,#9761,.F.);
#14189=ORIENTED_EDGE('',*,*,#9762,.F.);
#14190=ORIENTED_EDGE('',*,*,#9763,.F.);
#14191=ORIENTED_EDGE('',*,*,#9764,.F.);
#14192=ORIENTED_EDGE('',*,*,#9765,.F.);
#14193=ORIENTED_EDGE('',*,*,#9763,.T.);
#14194=ORIENTED_EDGE('',*,*,#9766,.F.);
#14195=ORIENTED_EDGE('',*,*,#9767,.F.);
#14196=ORIENTED_EDGE('',*,*,#9768,.F.);
#14197=ORIENTED_EDGE('',*,*,#9769,.F.);
#14198=ORIENTED_EDGE('',*,*,#9770,.F.);
#14199=ORIENTED_EDGE('',*,*,#9771,.F.);
#14200=ORIENTED_EDGE('',*,*,#9772,.F.);
#14201=ORIENTED_EDGE('',*,*,#9773,.F.);
#14202=ORIENTED_EDGE('',*,*,#9774,.F.);
#14203=ORIENTED_EDGE('',*,*,#9761,.T.);
#14204=ORIENTED_EDGE('',*,*,#9760,.T.);
#14205=ORIENTED_EDGE('',*,*,#9775,.T.);
#14206=ORIENTED_EDGE('',*,*,#9759,.T.);
#14207=ORIENTED_EDGE('',*,*,#9775,.F.);
#14208=ORIENTED_EDGE('',*,*,#9764,.T.);
#14209=ORIENTED_EDGE('',*,*,#9765,.T.);
#14210=ORIENTED_EDGE('',*,*,#9776,.F.);
#14211=ORIENTED_EDGE('',*,*,#9766,.T.);
#14212=ORIENTED_EDGE('',*,*,#9762,.T.);
#14213=ORIENTED_EDGE('',*,*,#9774,.T.);
#14214=ORIENTED_EDGE('',*,*,#9777,.F.);
#14215=ORIENTED_EDGE('',*,*,#9770,.T.);
#14216=ORIENTED_EDGE('',*,*,#9768,.T.);
#14217=ORIENTED_EDGE('',*,*,#9778,.T.);
#14218=ORIENTED_EDGE('',*,*,#9772,.T.);
#14219=ORIENTED_EDGE('',*,*,#9779,.T.);
#14220=ORIENTED_EDGE('',*,*,#9769,.T.);
#14221=ORIENTED_EDGE('',*,*,#9778,.F.);
#14222=ORIENTED_EDGE('',*,*,#9767,.T.);
#14223=ORIENTED_EDGE('',*,*,#9776,.T.);
#14224=ORIENTED_EDGE('',*,*,#9780,.F.);
#14225=ORIENTED_EDGE('',*,*,#9780,.T.);
#14226=ORIENTED_EDGE('',*,*,#9781,.T.);
#14227=ORIENTED_EDGE('',*,*,#9752,.T.);
#14228=ORIENTED_EDGE('',*,*,#9716,.F.);
#14229=ORIENTED_EDGE('',*,*,#9756,.T.);
#14230=ORIENTED_EDGE('',*,*,#9668,.T.);
#14231=ORIENTED_EDGE('',*,*,#9665,.T.);
#14232=ORIENTED_EDGE('',*,*,#9749,.T.);
#14233=ORIENTED_EDGE('',*,*,#9781,.F.);
#14234=ORIENTED_EDGE('',*,*,#9771,.T.);
#14235=ORIENTED_EDGE('',*,*,#9777,.T.);
#14236=ORIENTED_EDGE('',*,*,#9773,.T.);
#14237=ORIENTED_EDGE('',*,*,#9779,.F.);
#14338=CONICAL_SURFACE('',#16553,2.55,0.785398163397459);
#14339=CONICAL_SURFACE('',#16556,1.325,0.785398163397496);
#14340=CONICAL_SURFACE('',#16557,2.55,0.785398163397459);
#15055=ADVANCED_FACE('',(#2320),#1068,.T.);
#15056=ADVANCED_FACE('',(#2321),#1069,.T.);
#15057=ADVANCED_FACE('',(#2322),#1070,.T.);
#15058=ADVANCED_FACE('',(#2323),#1071,.T.);
#15059=ADVANCED_FACE('',(#2324),#1072,.T.);
#15060=ADVANCED_FACE('',(#2325),#1073,.T.);
#15061=ADVANCED_FACE('',(#2326),#1074,.T.);
#15062=ADVANCED_FACE('',(#2327),#1075,.T.);
#15063=ADVANCED_FACE('',(#2328),#1076,.T.);
#15064=ADVANCED_FACE('',(#2329),#1077,.T.);
#15065=ADVANCED_FACE('',(#2330),#1078,.T.);
#15066=ADVANCED_FACE('',(#2331),#1079,.T.);
#15067=ADVANCED_FACE('',(#2332),#1080,.T.);
#15068=ADVANCED_FACE('',(#2333),#1081,.T.);
#15069=ADVANCED_FACE('',(#2334),#370,.F.);
#15070=ADVANCED_FACE('',(#2335),#1598,.F.);
#15071=ADVANCED_FACE('',(#2336),#371,.F.);
#15072=ADVANCED_FACE('',(#2337),#363,.F.);
#15073=ADVANCED_FACE('',(#2338,#1210),#1599,.T.);
#15074=ADVANCED_FACE('',(#2339),#1600,.F.);
#15075=ADVANCED_FACE('',(#2340),#1601,.F.);
#15076=ADVANCED_FACE('',(#2341),#1602,.F.);
#15077=ADVANCED_FACE('',(#2342),#1082,.T.);
#15078=ADVANCED_FACE('',(#2343),#1603,.T.);
#15079=ADVANCED_FACE('',(#2344),#1604,.T.);
#15080=ADVANCED_FACE('',(#2345),#14338,.T.);
#15081=ADVANCED_FACE('',(#2346),#1605,.T.);
#15082=ADVANCED_FACE('',(#2347),#14339,.F.);
#15083=ADVANCED_FACE('',(#2348),#14340,.T.);
#15093=CLOSED_SHELL('',(#15055,#15056,#15057,#15058,#15059,#15060,#15061,
#15062,#15063,#15064,#15065,#15066,#15067,#15068,#15069,#15070,#15071,#15072,
#15073,#15074,#15075,#15076,#15077,#15078,#15079,#15080,#15081,#15082,#15083));
#16512=AXIS2_PLACEMENT_3D('',#71458,#20324,#20325);
#16513=AXIS2_PLACEMENT_3D('',#71459,#20326,#20327);
#16514=AXIS2_PLACEMENT_3D('',#71514,#20329,#20330);
#16515=AXIS2_PLACEMENT_3D('',#71515,#20331,#20332);
#16516=AXIS2_PLACEMENT_3D('',#71714,#20334,#20335);
#16517=AXIS2_PLACEMENT_3D('',#71883,#20336,#20337);
#16518=AXIS2_PLACEMENT_3D('',#72249,#20339,#20340);
#16519=AXIS2_PLACEMENT_3D('',#72615,#20342,#20343);
#16520=AXIS2_PLACEMENT_3D('',#72989,#20345,#20346);
#16521=AXIS2_PLACEMENT_3D('',#73364,#20348,#20349);
#16522=AXIS2_PLACEMENT_3D('',#73715,#20351,#20352);
#16523=AXIS2_PLACEMENT_3D('',#73943,#20354,#20355);
#16524=AXIS2_PLACEMENT_3D('',#74315,#20357,#20358);
#16525=AXIS2_PLACEMENT_3D('',#74690,#20360,#20361);
#16526=AXIS2_PLACEMENT_3D('',#75064,#20363,#20364);
#16527=AXIS2_PLACEMENT_3D('',#75443,#20366,#20367);
#16528=AXIS2_PLACEMENT_3D('',#75454,#20368,#20369);
#16529=AXIS2_PLACEMENT_3D('',#77597,#20370,#20371);
#16530=AXIS2_PLACEMENT_3D('',#79711,#20372,#20373);
#16531=AXIS2_PLACEMENT_3D('',#79870,#20374,#20375);
#16532=AXIS2_PLACEMENT_3D('',#80463,#20376,#20377);
#16533=AXIS2_PLACEMENT_3D('',#80465,#20378,#20379);
#16534=AXIS2_PLACEMENT_3D('',#80551,#20380,#20381);
#16535=AXIS2_PLACEMENT_3D('',#80894,#20382,#20383);
#16536=AXIS2_PLACEMENT_3D('',#80896,#20384,#20385);
#16537=AXIS2_PLACEMENT_3D('',#80897,#20386,#20387);
#16538=AXIS2_PLACEMENT_3D('',#80898,#20388,#20389);
#16539=AXIS2_PLACEMENT_3D('',#80900,#20390,#20391);
#16540=AXIS2_PLACEMENT_3D('',#80901,#20392,#20393);
#16541=AXIS2_PLACEMENT_3D('',#80904,#20394,#20395);
#16542=AXIS2_PLACEMENT_3D('',#80908,#20397,#20398);
#16543=AXIS2_PLACEMENT_3D('',#80911,#20400,#20401);
#16544=AXIS2_PLACEMENT_3D('',#80912,#20402,#20403);
#16545=AXIS2_PLACEMENT_3D('',#80926,#20407,#20408);
#16546=AXIS2_PLACEMENT_3D('',#80940,#20412,#20413);
#16547=AXIS2_PLACEMENT_3D('',#80942,#20415,#20416);
#16548=AXIS2_PLACEMENT_3D('',#80943,#20417,#20418);
#16549=AXIS2_PLACEMENT_3D('',#80944,#20419,#20420);
#16550=AXIS2_PLACEMENT_3D('',#80945,#20421,#20422);
#16551=AXIS2_PLACEMENT_3D('',#80946,#20423,#20424);
#16552=AXIS2_PLACEMENT_3D('',#80947,#20425,#20426);
#16553=AXIS2_PLACEMENT_3D('',#80948,#20427,#20428);
#16554=AXIS2_PLACEMENT_3D('',#80949,#20429,#20430);
#16555=AXIS2_PLACEMENT_3D('',#80951,#20431,#20432);
#16556=AXIS2_PLACEMENT_3D('',#80952,#20433,#20434);
#16557=AXIS2_PLACEMENT_3D('',#80954,#20436,#20437);
#20324=DIRECTION('axis',(0.,0.,1.));
#20325=DIRECTION('refdir',(1.,0.,0.));
#20326=DIRECTION('center_axis',(1.,0.,0.));
#20327=DIRECTION('ref_axis',(0.,0.761817798782983,-0.64779135642385));
#20328=DIRECTION('',(-1.,0.,0.));
#20329=DIRECTION('center_axis',(-1.,0.,0.));
#20330=DIRECTION('ref_axis',(0.,1.,6.78718384827097E-14));
#20331=DIRECTION('center_axis',(1.,0.,0.));
#20332=DIRECTION('ref_axis',(0.,0.761817798782983,-0.64779135642385));
#20333=DIRECTION('',(-1.,0.,0.));
#20334=DIRECTION('center_axis',(-1.,0.,0.));
#20335=DIRECTION('ref_axis',(0.,1.,6.78718384827097E-14));
#20336=DIRECTION('center_axis',(1.,0.,0.));
#20337=DIRECTION('ref_axis',(0.,0.761817798782983,-0.64779135642385));
#20338=DIRECTION('',(-1.,0.,0.));
#20339=DIRECTION('center_axis',(1.,0.,0.));
#20340=DIRECTION('ref_axis',(0.,0.761817798782983,-0.64779135642385));
#20341=DIRECTION('',(-1.,0.,0.));
#20342=DIRECTION('center_axis',(1.,0.,0.));
#20343=DIRECTION('ref_axis',(0.,0.761817798782983,-0.64779135642385));
#20344=DIRECTION('',(-1.,0.,0.));
#20345=DIRECTION('center_axis',(1.,0.,0.));
#20346=DIRECTION('ref_axis',(0.,0.761817798782983,-0.64779135642385));
#20347=DIRECTION('',(-1.,0.,0.));
#20348=DIRECTION('center_axis',(1.,0.,0.));
#20349=DIRECTION('ref_axis',(0.,0.761817798782983,-0.64779135642385));
#20350=DIRECTION('',(-1.,0.,0.));
#20351=DIRECTION('center_axis',(1.,0.,0.));
#20352=DIRECTION('ref_axis',(0.,0.761817798782983,-0.64779135642385));
#20353=DIRECTION('',(-1.,0.,0.));
#20354=DIRECTION('center_axis',(1.,0.,0.));
#20355=DIRECTION('ref_axis',(0.,0.761817798782983,-0.64779135642385));
#20356=DIRECTION('',(-1.,0.,0.));
#20357=DIRECTION('center_axis',(1.,0.,0.));
#20358=DIRECTION('ref_axis',(0.,0.761817798782983,-0.64779135642385));
#20359=DIRECTION('',(-1.,0.,0.));
#20360=DIRECTION('center_axis',(1.,0.,0.));
#20361=DIRECTION('ref_axis',(0.,0.761817798782983,-0.64779135642385));
#20362=DIRECTION('',(-1.,0.,0.));
#20363=DIRECTION('center_axis',(1.,0.,0.));
#20364=DIRECTION('ref_axis',(0.,0.761817798782983,-0.64779135642385));
#20365=DIRECTION('',(-1.,0.,0.));
#20366=DIRECTION('center_axis',(1.,0.,0.));
#20367=DIRECTION('ref_axis',(0.,1.,0.));
#20368=DIRECTION('center_axis',(1.,0.,0.));
#20369=DIRECTION('ref_axis',(0.,1.,0.));
#20370=DIRECTION('center_axis',(1.,0.,0.));
#20371=DIRECTION('ref_axis',(0.,1.,0.));
#20372=DIRECTION('center_axis',(1.,0.,0.));
#20373=DIRECTION('ref_axis',(0.,0.761817798782983,-0.64779135642385));
#20374=DIRECTION('center_axis',(1.,0.,0.));
#20375=DIRECTION('ref_axis',(0.,1.,6.78718384827097E-14));
#20376=DIRECTION('center_axis',(1.,0.,0.));
#20377=DIRECTION('ref_axis',(0.,0.,-1.));
#20378=DIRECTION('center_axis',(1.,0.,0.));
#20379=DIRECTION('ref_axis',(0.,1.,0.));
#20380=DIRECTION('center_axis',(1.,0.,0.));
#20381=DIRECTION('ref_axis',(0.,1.,0.));
#20382=DIRECTION('center_axis',(1.,0.,0.));
#20383=DIRECTION('ref_axis',(0.,0.,-1.));
#20384=DIRECTION('center_axis',(-1.,0.,0.));
#20385=DIRECTION('ref_axis',(0.,1.,0.));
#20386=DIRECTION('center_axis',(0.,1.,0.));
#20387=DIRECTION('ref_axis',(0.,0.,1.));
#20388=DIRECTION('center_axis',(-1.,0.,0.));
#20389=DIRECTION('ref_axis',(0.,0.,1.));
#20390=DIRECTION('center_axis',(1.,0.,0.));
#20391=DIRECTION('ref_axis',(0.,0.,-1.));
#20392=DIRECTION('center_axis',(-1.,0.,0.));
#20393=DIRECTION('ref_axis',(0.,0.,1.));
#20394=DIRECTION('center_axis',(-1.,0.,0.));
#20395=DIRECTION('ref_axis',(0.,1.,0.));
#20396=DIRECTION('',(0.,-1.,0.));
#20397=DIRECTION('center_axis',(-1.,0.,0.));
#20398=DIRECTION('ref_axis',(0.,1.,0.));
#20399=DIRECTION('',(0.,1.,0.));
#20400=DIRECTION('center_axis',(-1.,0.,0.));
#20401=DIRECTION('ref_axis',(0.,1.,0.));
#20402=DIRECTION('center_axis',(0.,0.,1.));
#20403=DIRECTION('ref_axis',(0.,1.,0.));
#20404=DIRECTION('',(1.,0.,0.));
#20405=DIRECTION('',(-1.,0.,0.));
#20406=DIRECTION('',(0.,1.,0.));
#20407=DIRECTION('center_axis',(0.,0.,-1.));
#20408=DIRECTION('ref_axis',(0.,-1.,0.));
#20409=DIRECTION('',(-1.,0.,0.));
#20410=DIRECTION('',(0.,-1.,0.));
#20411=DIRECTION('',(1.,0.,0.));
#20412=DIRECTION('center_axis',(1.,0.,0.));
#20413=DIRECTION('ref_axis',(0.,1.,0.));
#20414=DIRECTION('',(-1.,0.,0.));
#20415=DIRECTION('center_axis',(1.,0.,0.));
#20416=DIRECTION('ref_axis',(0.,0.,-1.));
#20417=DIRECTION('center_axis',(1.,0.,0.));
#20418=DIRECTION('ref_axis',(0.,0.,-1.));
#20419=DIRECTION('center_axis',(1.,0.,0.));
#20420=DIRECTION('ref_axis',(0.,0.,-1.));
#20421=DIRECTION('center_axis',(1.,0.,0.));
#20422=DIRECTION('ref_axis',(0.,0.,-1.));
#20423=DIRECTION('center_axis',(1.,0.,0.));
#20424=DIRECTION('ref_axis',(0.,0.,-1.));
#20425=DIRECTION('center_axis',(1.,0.,0.));
#20426=DIRECTION('ref_axis',(0.,0.,-1.));
#20427=DIRECTION('center_axis',(-1.,0.,0.));
#20428=DIRECTION('ref_axis',(0.,1.,0.));
#20429=DIRECTION('center_axis',(-1.,0.,0.));
#20430=DIRECTION('ref_axis',(0.,0.,1.));
#20431=DIRECTION('center_axis',(1.,0.,0.));
#20432=DIRECTION('ref_axis',(0.,0.,-1.));
#20433=DIRECTION('center_axis',(-1.,0.,0.));
#20434=DIRECTION('ref_axis',(0.,1.,0.));
#20435=DIRECTION('',(-0.707106781186514,-0.707106781186581,8.65956056235535E-17));
#20436=DIRECTION('center_axis',(-1.,0.,0.));
#20437=DIRECTION('ref_axis',(0.,1.,0.));
#71458=CARTESIAN_POINT('',(0.,0.,0.));
#71459=CARTESIAN_POINT('Origin',(197.762132885264,11.,29.5));
#71460=CARTESIAN_POINT('',(199.054667040747,10.1027691233085,30.2629363121594));
#71461=CARTESIAN_POINT('',(198.97225,10.1027690874833,30.2629362700282));
#71462=CARTESIAN_POINT('',(197.762132885264,10.1027690874833,30.2629362700282));
#71463=CARTESIAN_POINT('',(198.972408128224,11.1995478642895,30.6605616167741));
#71464=CARTESIAN_POINT('Ctrl Pts',(199.054667040747,10.1027691233085,30.2629363121594));
#71465=CARTESIAN_POINT('Ctrl Pts',(199.050047837914,10.1510957824736,30.3197695891699));
#71466=CARTESIAN_POINT('Ctrl Pts',(199.045424869181,10.2047250125246,30.3718971729035));
#71467=CARTESIAN_POINT('Ctrl Pts',(199.039436061019,10.2767217856396,30.4296642512059));
#71468=CARTESIAN_POINT('Ctrl Pts',(199.038279532795,10.2907436101604,30.4404054001326));
#71469=CARTESIAN_POINT('Ctrl Pts',(199.03642353782,10.313389255642,30.4569580461726));
#71470=CARTESIAN_POINT('Ctrl Pts',(199.035732005111,10.3218579668715,30.4629778750665));
#71471=CARTESIAN_POINT('Ctrl Pts',(199.034482863418,10.3372030929332,30.4735828723269));
#71472=CARTESIAN_POINT('Ctrl Pts',(199.033926842805,10.344050296774,30.4782092466494));
#71473=CARTESIAN_POINT('Ctrl Pts',(199.033263392418,10.3522381752584,30.4836168364151));
#71474=CARTESIAN_POINT('Ctrl Pts',(199.033158553209,10.3535325562788,30.4844680323103));
#71475=CARTESIAN_POINT('Ctrl Pts',(199.032999120303,10.3555017482171,30.4857574312877));
#71476=CARTESIAN_POINT('Ctrl Pts',(199.032944595149,10.3561753388067,30.4861975033045));
#71477=CARTESIAN_POINT('Ctrl Pts',(199.03285671492,10.3572612100683,30.4869053409987));
#71478=CARTESIAN_POINT('Ctrl Pts',(199.0328233757,10.3576732092472,30.4871735399891));
#71479=CARTESIAN_POINT('Ctrl Pts',(199.032768002488,10.3583575840413,30.4876184374311));
#71480=CARTESIAN_POINT('Ctrl Pts',(199.03274597382,10.3586298653129,30.4877952815448));
#71481=CARTESIAN_POINT('Ctrl Pts',(199.032708712138,10.3590904686424,30.4880941683234));
#71482=CARTESIAN_POINT('Ctrl Pts',(199.032693481273,10.3592787526436,30.488216269875));
#71483=CARTESIAN_POINT('Ctrl Pts',(199.032620047558,10.3601865909939,30.4888046315188));
#71484=CARTESIAN_POINT('Ctrl Pts',(199.032561818005,10.360906617924,30.48927015857));
#71485=CARTESIAN_POINT('Ctrl Pts',(199.032446957709,10.3623272003227,30.4901864253755));
#71486=CARTESIAN_POINT('Ctrl Pts',(199.032390328606,10.3630277270215,30.4906372090209));
#71487=CARTESIAN_POINT('Ctrl Pts',(199.032277593615,10.3644225891859,30.4915327010402));
#71488=CARTESIAN_POINT('Ctrl Pts',(199.032221488307,10.3651169146002,30.4919774242575));
#71489=CARTESIAN_POINT('Ctrl Pts',(199.032108839059,10.3665112685847,30.492868460022));
#71490=CARTESIAN_POINT('Ctrl Pts',(199.032052294787,10.3672113031633,30.4933147622412));
#71491=CARTESIAN_POINT('Ctrl Pts',(199.030942145707,10.3809579693864,30.5020584252807));
#71492=CARTESIAN_POINT('Ctrl Pts',(199.029879335722,10.3941657112817,30.5100984600361));
#71493=CARTESIAN_POINT('Ctrl Pts',(199.027494437902,10.4238941369291,30.5274024155019));
#71494=CARTESIAN_POINT('Ctrl Pts',(199.026168124288,10.4404874614061,30.536532363144));
#71495=CARTESIAN_POINT('Ctrl Pts',(199.021981122858,10.4930527493686,30.5638247225895));
#71496=CARTESIAN_POINT('Ctrl Pts',(199.019078689559,10.5297387387927,30.580542636061));
#71497=CARTESIAN_POINT('Ctrl Pts',(199.011211935375,10.6302098477806,30.6202408078014));
#71498=CARTESIAN_POINT('Ctrl Pts',(199.006198748159,10.6952429953544,30.6396523341107));
#71499=CARTESIAN_POINT('Ctrl Pts',(198.999426957925,10.7872455683046,30.6586704711183));
#71500=CARTESIAN_POINT('Ctrl Pts',(198.997560635733,10.8130790418952,30.6631175727641));
#71501=CARTESIAN_POINT('Ctrl Pts',(198.995140521639,10.8474561228168,30.6678602588841));
#71502=CARTESIAN_POINT('Ctrl Pts',(198.994552261683,10.8558835235845,30.6689301392159));
#71503=CARTESIAN_POINT('Ctrl Pts',(198.993631743619,10.8691949353454,30.6704739048081));
#71504=CARTESIAN_POINT('Ctrl Pts',(198.993296352101,10.8740714055189,30.6710085900895));
#71505=CARTESIAN_POINT('Ctrl Pts',(198.992594277158,10.8843380921291,30.6720694152485));
#71506=CARTESIAN_POINT('Ctrl Pts',(198.992227989733,10.8897288660171,30.6725888751746));
#71507=CARTESIAN_POINT('Ctrl Pts',(198.991302989487,10.9034239764498,30.6738132683551));
#71508=CARTESIAN_POINT('Ctrl Pts',(198.990746959212,10.9117327560362,30.6744672922818));
#71509=CARTESIAN_POINT('Ctrl Pts',(198.989536447892,10.9299700761366,30.675708201186));
#71510=CARTESIAN_POINT('Ctrl Pts',(198.988883754879,10.9399005978941,30.6762576421173));
#71511=CARTESIAN_POINT('Ctrl Pts',(198.982788814076,11.0334047119427,30.6802437892237));
#71512=CARTESIAN_POINT('Ctrl Pts',(198.97769936836,11.1171236786616,30.6748943153088));
#71513=CARTESIAN_POINT('Ctrl Pts',(198.972499309319,11.1995770050681,30.6607170549053));
#71514=CARTESIAN_POINT('Origin',(198.97225,11.,29.5));
#71515=CARTESIAN_POINT('Origin',(197.762132885264,11.,29.5));
#71516=CARTESIAN_POINT('',(199.554117165109,10.1027690888331,30.2629362716156));
#71517=CARTESIAN_POINT('',(199.456018641859,10.1027690874833,30.2629362700282));
#71518=CARTESIAN_POINT('',(197.762132885264,10.1027690874833,30.2629362700282));
#71519=CARTESIAN_POINT('Ctrl Pts',(199.554117165109,10.1027690888331,30.2629362716156));
#71520=CARTESIAN_POINT('Ctrl Pts',(199.55397561361,10.104033743,30.2644235345137));
#71521=CARTESIAN_POINT('Ctrl Pts',(199.553834153139,10.1053021670648,30.2659077375468));
#71522=CARTESIAN_POINT('Ctrl Pts',(199.551475140412,10.1265318427489,30.2906241982884));
#71523=CARTESIAN_POINT('Ctrl Pts',(199.549283840494,10.1473900197398,30.3130742890784));
#71524=CARTESIAN_POINT('Ctrl Pts',(199.546521955864,10.1754176750091,30.3409747178614));
#71525=CARTESIAN_POINT('Ctrl Pts',(199.545904047563,10.181805151833,30.3471904680199));
#71526=CARTESIAN_POINT('Ctrl Pts',(199.544911134781,10.1922692472355,30.3571444860382));
#71527=CARTESIAN_POINT('Ctrl Pts',(199.544532969818,10.1963025831272,30.3609274674216));
#71528=CARTESIAN_POINT('Ctrl Pts',(199.543786434426,10.204363322805,30.3683818490507));
#71529=CARTESIAN_POINT('Ctrl Pts',(199.543418020189,10.2083898433213,30.3720539663394));
#71530=CARTESIAN_POINT('Ctrl Pts',(199.542477546404,10.2187890451231,30.3814064782455));
#71531=CARTESIAN_POINT('Ctrl Pts',(199.541908373359,10.2251984015703,30.3870459003836));
#71532=CARTESIAN_POINT('Ctrl Pts',(199.539410509341,10.2538093262097,30.4116731581275));
#71533=CARTESIAN_POINT('Ctrl Pts',(199.537528526823,10.2766533342977,30.4299023454379));
#71534=CARTESIAN_POINT('Ctrl Pts',(199.531582977554,10.3520366351769,30.4855961135881));
#71535=CARTESIAN_POINT('Ctrl Pts',(199.527635449356,10.4069837312913,30.519602292334));
#71536=CARTESIAN_POINT('Ctrl Pts',(199.519886246082,10.5180487324825,30.5763089044829));
#71537=CARTESIAN_POINT('Ctrl Pts',(199.516103624939,10.5736686306426,30.5995263488409));
#71538=CARTESIAN_POINT('Ctrl Pts',(199.511172823979,10.6454805301191,30.6232317315417));
#71539=CARTESIAN_POINT('Ctrl Pts',(199.510157441837,10.6602392917988,30.6277837570737));
#71540=CARTESIAN_POINT('Ctrl Pts',(199.508480393937,10.6845348883537,30.6347570350474));
#71541=CARTESIAN_POINT('Ctrl Pts',(199.507824282064,10.6940203771917,30.6373514082756));
#71542=CARTESIAN_POINT('Ctrl Pts',(199.506537156815,10.7125823251794,30.6421792746344));
#71543=CARTESIAN_POINT('Ctrl Pts',(199.505906557151,10.7216550977296,30.6444241005806));
#71544=CARTESIAN_POINT('Ctrl Pts',(199.504397279835,10.7433129252783,30.6495100035707));
#71545=CARTESIAN_POINT('Ctrl Pts',(199.503515586384,10.7559196062974,30.6522526811813));
#71546=CARTESIAN_POINT('Ctrl Pts',(199.500356291611,10.8009136317413,30.6612699585049));
#71547=CARTESIAN_POINT('Ctrl Pts',(199.49804382135,10.833513999149,30.6663898793413));
#71548=CARTESIAN_POINT('Ctrl Pts',(199.491839879123,10.9200914554552,30.6762834562131));
#71549=CARTESIAN_POINT('Ctrl Pts',(199.48789226576,10.9742545269602,30.6787129927265));
#71550=CARTESIAN_POINT('Ctrl Pts',(199.479087076369,11.0943445212123,30.6758175991903));
#71551=CARTESIAN_POINT('Ctrl Pts',(199.474232457238,11.1600564508388,30.6686878289023));
#71552=CARTESIAN_POINT('Ctrl Pts',(199.468741914828,11.2365650748656,30.6538088907022));
#71553=CARTESIAN_POINT('Ctrl Pts',(199.467907032434,11.2482656166387,30.6513479932067));
#71554=CARTESIAN_POINT('Ctrl Pts',(199.466649765203,11.2660161440091,30.6473314461284));
#71555=CARTESIAN_POINT('Ctrl Pts',(199.466220929688,11.2720942174386,30.6459052218114));
#71556=CARTESIAN_POINT('Ctrl Pts',(199.465441596703,11.2831884789837,30.643208694156));
#71557=CARTESIAN_POINT('Ctrl Pts',(199.465090325176,11.2882078776386,30.6419536129155));
#71558=CARTESIAN_POINT('Ctrl Pts',(199.464278022546,11.2998570672304,30.6389590753402));
#71559=CARTESIAN_POINT('Ctrl Pts',(199.46381837152,11.3064801642162,30.6371947725203));
#71560=CARTESIAN_POINT('Ctrl Pts',(199.462316399564,11.3282090702536,30.6312028609942));
#71561=CARTESIAN_POINT('Ctrl Pts',(199.461286601463,11.343246523321,30.6267311068583));
#71562=CARTESIAN_POINT('Ctrl Pts',(199.458766387683,11.380247954646,30.6149182265592));
#71563=CARTESIAN_POINT('Ctrl Pts',(199.457290554239,11.4020937856794,30.6072271092186));
#71564=CARTESIAN_POINT('Ctrl Pts',(199.449751762245,11.5136303672644,30.5642221185986));
#71565=CARTESIAN_POINT('Ctrl Pts',(199.443939895019,11.598963682996,30.5186404937894));
#71566=CARTESIAN_POINT('Ctrl Pts',(199.435963409052,11.7013279243578,30.4466057868504));
#71567=CARTESIAN_POINT('Ctrl Pts',(199.434105573168,11.7242480082989,30.4291867373441));
#71568=CARTESIAN_POINT('Ctrl Pts',(199.431467814239,11.7553237250241,30.4037207001819));
#71569=CARTESIAN_POINT('Ctrl Pts',(199.430714595171,11.7640359377842,30.3963671706326));
#71570=CARTESIAN_POINT('Ctrl Pts',(199.429333220759,11.7797104000681,30.382742612754));
#71571=CARTESIAN_POINT('Ctrl Pts',(199.428706751116,11.7867072514395,30.3765127040578));
#71572=CARTESIAN_POINT('Ctrl Pts',(199.427429176894,11.8007454544031,30.3637097605538));
#71573=CARTESIAN_POINT('Ctrl Pts',(199.426777924717,11.8077819637742,30.3571325001384));
#71574=CARTESIAN_POINT('Ctrl Pts',(199.425140993212,11.825165755119,30.3404790992798));
#71575=CARTESIAN_POINT('Ctrl Pts',(199.424150887683,11.835409604665,30.330297778095));
#71576=CARTESIAN_POINT('Ctrl Pts',(199.419872076268,11.8785083437364,30.2858569666828));
#71577=CARTESIAN_POINT('Ctrl Pts',(199.416506222358,11.9094591744748,30.2498207000433));
#71578=CARTESIAN_POINT('Ctrl Pts',(199.409635154824,11.9669869414675,30.1740227900945));
#71579=CARTESIAN_POINT('Ctrl Pts',(199.406135604062,11.9934887826076,30.1343107094375));
#71580=CARTESIAN_POINT('Ctrl Pts',(199.398376805358,12.0467882263918,30.0428719803416));
#71581=CARTESIAN_POINT('Ctrl Pts',(199.39412830673,12.0723112674455,29.9905359262447));
#71582=CARTESIAN_POINT('Ctrl Pts',(199.389359185023,12.0975448000005,29.927304354392));
#71583=CARTESIAN_POINT('Ctrl Pts',(199.388669199555,12.1011074520957,29.9180382689772));
#71584=CARTESIAN_POINT('Ctrl Pts',(199.387589670073,12.1065474324464,29.9033371802295));
#71585=CARTESIAN_POINT('Ctrl Pts',(199.387195948245,12.1085027647167,29.8979318098835));
#71586=CARTESIAN_POINT('Ctrl Pts',(199.386443382754,12.1121861300555,29.8875115554209));
#71587=CARTESIAN_POINT('Ctrl Pts',(199.386084243431,12.1139199709967,29.8824990102202));
#71588=CARTESIAN_POINT('Ctrl Pts',(199.385201684437,12.118119594338,29.8700871010029));
#71589=CARTESIAN_POINT('Ctrl Pts',(199.384680467488,12.1205459062477,29.8626744678721));
#71590=CARTESIAN_POINT('Ctrl Pts',(199.382687517735,12.129604921492,29.834039148791));
#71591=CARTESIAN_POINT('Ctrl Pts',(199.381242265404,12.1357102068358,29.8126530083178));
#71592=CARTESIAN_POINT('Ctrl Pts',(199.377308627066,12.1508818761976,29.7531762123979));
#71593=CARTESIAN_POINT('Ctrl Pts',(199.374864624295,12.1586607634217,29.7147857646126));
#71594=CARTESIAN_POINT('Ctrl Pts',(199.366816968299,12.1780431339211,29.5865973098536));
#71595=CARTESIAN_POINT('Ctrl Pts',(199.361276100427,12.1812137671653,29.49586585006));
#71596=CARTESIAN_POINT('Ctrl Pts',(199.354273251435,12.1725773065496,29.3883835085662));
#71597=CARTESIAN_POINT('Ctrl Pts',(199.353136694342,12.1708068367173,29.3711315306429));
#71598=CARTESIAN_POINT('Ctrl Pts',(199.351311542584,12.1673880671735,29.3437799439687));
#71599=CARTESIAN_POINT('Ctrl Pts',(199.350630593516,12.1659878940476,29.3336514944718));
#71600=CARTESIAN_POINT('Ctrl Pts',(199.349328601689,12.1630764969782,29.3144389358177));
#71601=CARTESIAN_POINT('Ctrl Pts',(199.348708379303,12.1615902487833,29.3053517734548));
#71602=CARTESIAN_POINT('Ctrl Pts',(199.347275314284,12.1579301140469,29.2845103534915));
#71603=CARTESIAN_POINT('Ctrl Pts',(199.346460265098,12.1556835535797,29.272770066573));
#71604=CARTESIAN_POINT('Ctrl Pts',(199.34381309581,12.1478615776771,29.2350158073927));
#71605=CARTESIAN_POINT('Ctrl Pts',(199.341959524407,12.1415836765402,29.2091575333803));
#71606=CARTESIAN_POINT('Ctrl Pts',(199.337359809625,12.1240809675592,29.1464152203365));
#71607=CARTESIAN_POINT('Ctrl Pts',(199.334588554984,12.1119109696819,29.1098285599595));
#71608=CARTESIAN_POINT('Ctrl Pts',(199.326289822645,12.0706235272621,29.003437714297));
#71609=CARTESIAN_POINT('Ctrl Pts',(199.320682692828,12.0365563045028,28.9357660878128));
#71610=CARTESIAN_POINT('Ctrl Pts',(199.313658292782,11.9843372787911,28.8529504484375));
#71611=CARTESIAN_POINT('Ctrl Pts',(199.312075774013,11.9719004748141,28.8344155840126));
#71612=CARTESIAN_POINT('Ctrl Pts',(199.309963024472,11.9542842249072,28.809709414937));
#71613=CARTESIAN_POINT('Ctrl Pts',(199.309407969382,11.9495580027044,28.8032223582065));
#71614=CARTESIAN_POINT('Ctrl Pts',(199.308493925471,11.9416053552586,28.7925380346109));
#71615=CARTESIAN_POINT('Ctrl Pts',(199.308132546753,11.9384163405637,28.7883133741403));
#71616=CARTESIAN_POINT('Ctrl Pts',(199.307389348292,11.9317627189889,28.7796214511788));
#71617=CARTESIAN_POINT('Ctrl Pts',(199.307007797144,11.9282942510155,28.7751573929824));
#71618=CARTESIAN_POINT('Ctrl Pts',(199.305991723728,11.9189208614585,28.7632711050602));
#71619=CARTESIAN_POINT('Ctrl Pts',(199.30536103486,11.9129580649776,28.7558947656303));
#71620=CARTESIAN_POINT('Ctrl Pts',(199.30184787498,11.8789721192224,28.7148757239378));
#71621=CARTESIAN_POINT('Ctrl Pts',(199.299072135445,11.8491760198917,28.682740519812));
#71622=CARTESIAN_POINT('Ctrl Pts',(199.290253089337,11.7476566097271,28.5848149072397));
#71623=CARTESIAN_POINT('Ctrl Pts',(199.284360662411,11.6695677452392,28.526227526484));
#71624=CARTESIAN_POINT('Ctrl Pts',(199.276712481297,11.566567284197,28.4672580955822));
#71625=CARTESIAN_POINT('Ctrl Pts',(199.275316604586,11.5476829573531,28.4571205166682));
#71626=CARTESIAN_POINT('Ctrl Pts',(199.273166243126,11.5185496102897,28.4424905777106));
#71627=CARTESIAN_POINT('Ctrl Pts',(199.272424683742,11.5084951992158,28.4376194209032));
#71628=CARTESIAN_POINT('Ctrl Pts',(199.271067281495,11.4900882642366,28.4290227969557));
#71629=CARTESIAN_POINT('Ctrl Pts',(199.270453095659,11.4817586612533,28.4252501404964));
#71630=CARTESIAN_POINT('Ctrl Pts',(199.269109600489,11.4635419101987,28.4172537035204));
#71631=CARTESIAN_POINT('Ctrl Pts',(199.268379095556,11.4536392362692,28.4130675848045));
#71632=CARTESIAN_POINT('Ctrl Pts',(199.266280443305,11.4252063626599,28.4015044972366));
#71633=CARTESIAN_POINT('Ctrl Pts',(199.264901528461,11.4065449772769,28.3944621585162));
#71634=CARTESIAN_POINT('Ctrl Pts',(199.261710920056,11.3634351727307,28.3794326950577));
#71635=CARTESIAN_POINT('Ctrl Pts',(199.259890231092,11.3388865127897,28.3717659901676));
#71636=CARTESIAN_POINT('Ctrl Pts',(199.252974247716,11.2457828587354,28.346001876214));
#71637=CARTESIAN_POINT('Ctrl Pts',(199.247749983417,11.1758942782619,28.333303594154));
#71638=CARTESIAN_POINT('Ctrl Pts',(199.23914984729,11.058738373807,28.3227872028255));
#71639=CARTESIAN_POINT('Ctrl Pts',(199.235761035929,11.0119679081332,28.321383083587));
#71640=CARTESIAN_POINT('Ctrl Pts',(199.231805665549,10.9554979698128,28.3230507673531));
#71641=CARTESIAN_POINT('Ctrl Pts',(199.231128960288,10.9457659216815,28.32345905004));
#71642=CARTESIAN_POINT('Ctrl Pts',(199.230065343891,10.9303399051886,28.3242980321637));
#71643=CARTESIAN_POINT('Ctrl Pts',(199.229674450539,10.92464231264,28.3246494700024));
#71644=CARTESIAN_POINT('Ctrl Pts',(199.228923235393,10.9136335284199,28.3254088940476));
#71645=CARTESIAN_POINT('Ctrl Pts',(199.228562662267,10.9083222189539,28.3258115060541));
#71646=CARTESIAN_POINT('Ctrl Pts',(199.227670957267,10.8951246071276,28.3269020169546));
#71647=CARTESIAN_POINT('Ctrl Pts',(199.227142132131,10.8872419815451,28.3276334346491));
#71648=CARTESIAN_POINT('Ctrl Pts',(199.225079023685,10.8562998910404,28.330819484723));
#71649=CARTESIAN_POINT('Ctrl Pts',(199.223573649349,10.8333061106647,28.3338756030311));
#71650=CARTESIAN_POINT('Ctrl Pts',(199.219404661186,10.7690025087063,28.344363416282));
#71651=CARTESIAN_POINT('Ctrl Pts',(199.216792037532,10.7279768615204,28.353326713131));
#71652=CARTESIAN_POINT('Ctrl Pts',(199.208900253456,10.6052605522628,28.387096607951));
#71653=CARTESIAN_POINT('Ctrl Pts',(199.203659135385,10.5257176221002,28.4185991700282));
#71654=CARTESIAN_POINT('Ctrl Pts',(199.196975301239,10.4345944234358,28.4666916876087));
#71655=CARTESIAN_POINT('Ctrl Pts',(199.195814223083,10.4191009397079,28.4753216292874));
#71656=CARTESIAN_POINT('Ctrl Pts',(199.193952723513,10.3948363773603,28.4895643048852));
#71657=CARTESIAN_POINT('Ctrl Pts',(199.193260322993,10.3859343657315,28.4949494095047));
#71658=CARTESIAN_POINT('Ctrl Pts',(199.192010618432,10.3700953914079,28.5048198834376));
#71659=CARTESIAN_POINT('Ctrl Pts',(199.191454916925,10.363131989357,28.5092616836714));
#71660=CARTESIAN_POINT('Ctrl Pts',(199.190140095822,10.3468470395989,28.51989212098));
#71661=CARTESIAN_POINT('Ctrl Pts',(199.189378800807,10.3375659644616,28.5261409866342));
#71662=CARTESIAN_POINT('Ctrl Pts',(199.187090830196,10.3101218832859,28.5451926805549));
#71663=CARTESIAN_POINT('Ctrl Pts',(199.18555011509,10.2922315858019,28.5583776812938));
#71664=CARTESIAN_POINT('Ctrl Pts',(199.18000145544,10.2299142066744,28.6070846928884));
#71665=CARTESIAN_POINT('Ctrl Pts',(199.175896219152,10.1877039488176,28.6453050043792));
#71666=CARTESIAN_POINT('Ctrl Pts',(199.166391905083,10.0978706245797,28.7393337318908));
#71667=CARTESIAN_POINT('Ctrl Pts',(199.160975857458,10.0523575066952,28.7968462118573));
#71668=CARTESIAN_POINT('Ctrl Pts',(199.154662411959,10.0038886342109,28.8714258066601));
#71669=CARTESIAN_POINT('Ctrl Pts',(199.153555273488,9.99556733653232,28.884810230761));
#71670=CARTESIAN_POINT('Ctrl Pts',(199.151992354998,9.98404652772017,28.9041982287849));
#71671=CARTESIAN_POINT('Ctrl Pts',(199.151524402698,9.98062683725261,28.9100681657741));
#71672=CARTESIAN_POINT('Ctrl Pts',(199.150705305482,9.97469063139452,28.9204634901362));
#71673=CARTESIAN_POINT('Ctrl Pts',(199.150352892367,9.97215288821443,28.9249763604106));
#71674=CARTESIAN_POINT('Ctrl Pts',(199.149582833646,9.9666431554737,28.9349273546286));
#71675=CARTESIAN_POINT('Ctrl Pts',(199.14916597653,9.96368422436451,28.9403723737055));
#71676=CARTESIAN_POINT('Ctrl Pts',(199.147941808949,9.95507060884029,28.9565257454444));
#71677=CARTESIAN_POINT('Ctrl Pts',(199.147141479161,9.94953775244688,28.9672985902588));
#71678=CARTESIAN_POINT('Ctrl Pts',(199.143255866313,9.92322941367611,29.0205272411553));
#71679=CARTESIAN_POINT('Ctrl Pts',(199.140284425323,9.90485440480586,29.0641260633656));
#71680=CARTESIAN_POINT('Ctrl Pts',(199.131786683405,9.85948500349734,29.1929292189662));
#71681=CARTESIAN_POINT('Ctrl Pts',(199.126343070861,9.83949586739486,29.2802362381936));
#71682=CARTESIAN_POINT('Ctrl Pts',(199.119210658951,9.82718122709295,29.39023097704));
#71683=CARTESIAN_POINT('Ctrl Pts',(199.117816625471,9.82538031996532,29.411560020899));
#71684=CARTESIAN_POINT('Ctrl Pts',(199.115668765839,9.82352582812475,29.4440697822466));
#71685=CARTESIAN_POINT('Ctrl Pts',(199.114927834619,9.82304859034161,29.4552224209926));
#71686=CARTESIAN_POINT('Ctrl Pts',(199.113571434148,9.8224690885387,29.4755147200795));
#71687=CARTESIAN_POINT('Ctrl Pts',(199.112957618516,9.82231455385527,29.4846520900297));
#71688=CARTESIAN_POINT('Ctrl Pts',(199.111614777694,9.82220970707052,29.5045367853038));
#71689=CARTESIAN_POINT('Ctrl Pts',(199.110884555625,9.82230013971825,29.5152834051855));
#71690=CARTESIAN_POINT('Ctrl Pts',(199.108786305008,9.822978319842,29.5459643163472));
#71691=CARTESIAN_POINT('Ctrl Pts',(199.10740750139,9.8239253045106,29.565886126029));
#71692=CARTESIAN_POINT('Ctrl Pts',(199.104216934179,9.8272501695058,29.6114184925363));
#71693=CARTESIAN_POINT('Ctrl Pts',(199.102396165509,9.82996205894455,29.6369938012734));
#71694=CARTESIAN_POINT('Ctrl Pts',(199.095478606081,9.8432901161763,29.7326925542547));
#71695=CARTESIAN_POINT('Ctrl Pts',(199.090252674016,9.85939438164621,29.8018953761779));
#71696=CARTESIAN_POINT('Ctrl Pts',(199.081651486936,9.89627324953134,29.9136019429219));
#71697=CARTESIAN_POINT('Ctrl Pts',(199.078263233059,9.91355511673502,29.9570751827318));
#71698=CARTESIAN_POINT('Ctrl Pts',(199.074308650384,9.93750565007133,30.0082279215158));
#71699=CARTESIAN_POINT('Ctrl Pts',(199.073632156896,9.9417436892029,30.0169946419011));
#71700=CARTESIAN_POINT('Ctrl Pts',(199.07256892404,9.94863690912871,30.0308137783448));
#71701=CARTESIAN_POINT('Ctrl Pts',(199.072178202638,9.95122082324698,30.0359009777559));
#71702=CARTESIAN_POINT('Ctrl Pts',(199.071427261538,9.95628750092329,30.0456992172214));
#71703=CARTESIAN_POINT('Ctrl Pts',(199.071066790771,9.9587653940781,30.0504124935947));
#71704=CARTESIAN_POINT('Ctrl Pts',(199.070175449316,9.96500435338885,30.0620868911616));
#71705=CARTESIAN_POINT('Ctrl Pts',(199.069646882718,9.96880384738301,30.0690273850704));
#71706=CARTESIAN_POINT('Ctrl Pts',(199.067586009318,9.98399792850531,30.0961301702344));
#71707=CARTESIAN_POINT('Ctrl Pts',(199.066082538199,9.99591697761888,30.1159941851323));
#71708=CARTESIAN_POINT('Ctrl Pts',(199.061921643895,10.0310027292842,30.170739690745));
#71709=CARTESIAN_POINT('Ctrl Pts',(199.059314989865,10.0554550527729,30.2047572237535));
#71710=CARTESIAN_POINT('Ctrl Pts',(199.056034177674,10.088584320814,30.2460151023313));
#71711=CARTESIAN_POINT('Ctrl Pts',(199.055350501907,10.0956186699298,30.2545272124069));
#71712=CARTESIAN_POINT('Ctrl Pts',(199.054667040747,10.1027691233085,30.2629363121594));
#71713=CARTESIAN_POINT('',(198.971545633483,9.96489439058431,30.0635599336052));
#71714=CARTESIAN_POINT('Origin',(198.97225,11.,29.5));
#71715=CARTESIAN_POINT('',(199.01213292537,9.82225003050404,29.500268052058));
#71716=CARTESIAN_POINT('Ctrl Pts',(198.972443712976,9.96565131904446,30.0632209767982));
#71717=CARTESIAN_POINT('Ctrl Pts',(198.975807610355,9.94171007452878,30.0192531636212));
#71718=CARTESIAN_POINT('Ctrl Pts',(198.979171507734,9.92061433691864,29.9738270716902));
#71719=CARTESIAN_POINT('Ctrl Pts',(198.982535405113,9.9025075342917,29.927323472575));
#71720=CARTESIAN_POINT('Ctrl Pts',(198.98590663962,9.884361238206,29.8807184426323));
#71721=CARTESIAN_POINT('Ctrl Pts',(198.989277874128,9.86921700580483,29.8330316474283));
#71722=CARTESIAN_POINT('Ctrl Pts',(198.992649108635,9.85716802120539,29.7846579188155));
#71723=CARTESIAN_POINT('Ctrl Pts',(198.996032930337,9.84507404925335,29.7361035769762));
#71724=CARTESIAN_POINT('Ctrl Pts',(198.99941675204,9.83609851197747,29.6868576152335));
#71725=CARTESIAN_POINT('Ctrl Pts',(199.002800573742,9.83028330893629,29.6373241608274));
#71726=CARTESIAN_POINT('Ctrl Pts',(199.004794261458,9.82685709447019,29.6081399282495));
#71727=CARTESIAN_POINT('Ctrl Pts',(199.006787949173,9.82452695210034,29.5788559541146));
#71728=CARTESIAN_POINT('Ctrl Pts',(199.008781636889,9.82329298769148,29.5495547140438));
#71729=CARTESIAN_POINT('Ctrl Pts',(199.00989871968,9.82260158532406,29.5331369416932));
#71730=CARTESIAN_POINT('Ctrl Pts',(199.011015802472,9.82225377973876,29.5167050154579));
#71731=CARTESIAN_POINT('Ctrl Pts',(199.012132885264,9.82225003063834,29.5002686421649));
#71732=CARTESIAN_POINT('Ctrl Pts',(199.012132965476,9.82225003036973,29.500267461951));
#71733=CARTESIAN_POINT('Ctrl Pts',(199.015290203676,9.82223948074753,29.4538129394526));
#71734=CARTESIAN_POINT('Ctrl Pts',(199.018447441875,9.82498170507075,29.4072497693987));
#71735=CARTESIAN_POINT('Ctrl Pts',(199.021604680075,9.83048918351974,29.3609334237292));
#71736=CARTESIAN_POINT('Ctrl Pts',(199.024757398053,9.83598877690527,29.3146833892271));
#71737=CARTESIAN_POINT('Ctrl Pts',(199.027910116031,9.84424573011089,29.2686800365615));
#71738=CARTESIAN_POINT('Ctrl Pts',(199.031062834009,9.85522055611645,29.2232779601086));
#71739=CARTESIAN_POINT('Ctrl Pts',(199.034212471243,9.86618465784211,29.1779202492406));
#71740=CARTESIAN_POINT('Ctrl Pts',(199.037362108477,9.87986124591711,29.1331631992053));
#71741=CARTESIAN_POINT('Ctrl Pts',(199.040511745711,9.89615953926772,29.0893525846296));
#71742=CARTESIAN_POINT('Ctrl Pts',(199.043659736592,9.91244931331107,29.0455648703711));
#71743=CARTESIAN_POINT('Ctrl Pts',(199.046807727474,9.93135788183305,29.0027231407691));
#71744=CARTESIAN_POINT('Ctrl Pts',(199.049955718356,9.95274508255928,28.961156608655));
#71745=CARTESIAN_POINT('Ctrl Pts',(199.053105823233,9.97414664559549,28.9195621630506));
#71746=CARTESIAN_POINT('Ctrl Pts',(199.056255928109,9.99802991680388,28.8792451344006));
#71747=CARTESIAN_POINT('Ctrl Pts',(199.059406032985,10.0242080271693,28.8405114949757));
#71748=CARTESIAN_POINT('Ctrl Pts',(199.062556987811,10.0503932008154,28.8017674045838));
#71749=CARTESIAN_POINT('Ctrl Pts',(199.065707942637,10.0788741100446,28.7646080098553));
#71750=CARTESIAN_POINT('Ctrl Pts',(199.068858897463,10.1094217892156,28.7293084190313));
#71751=CARTESIAN_POINT('Ctrl Pts',(199.072016018166,10.1400292449474,28.6939397529716));
#71752=CARTESIAN_POINT('Ctrl Pts',(199.075173138869,10.1727111597207,28.6604385732073));
#71753=CARTESIAN_POINT('Ctrl Pts',(199.078330259573,10.2072007417723,28.6290439743284));
#71754=CARTESIAN_POINT('Ctrl Pts',(199.081364684923,10.2403499533278,28.5988694654469));
#71755=CARTESIAN_POINT('Ctrl Pts',(199.084399110273,10.2751684678066,28.5706409972311));
#71756=CARTESIAN_POINT('Ctrl Pts',(199.087433535623,10.3113934224206,28.544533598804));
#71757=CARTESIAN_POINT('Ctrl Pts',(199.090710698071,10.3505161712813,28.5163377541728));
#71758=CARTESIAN_POINT('Ctrl Pts',(199.093987860518,10.391458684281,28.4904873589618));
#71759=CARTESIAN_POINT('Ctrl Pts',(199.097265022965,10.433907274098,28.4672202131234));
#71760=CARTESIAN_POINT('Ctrl Pts',(199.100443805193,10.4750815598006,28.4446515456043));
#71761=CARTESIAN_POINT('Ctrl Pts',(199.103622587421,10.5176722408203,28.4245134947446));
#71762=CARTESIAN_POINT('Ctrl Pts',(199.106801369648,10.5613622420152,28.4069803387999));
#71763=CARTESIAN_POINT('Ctrl Pts',(199.109977113254,10.6050104796088,28.389463942931));
#71764=CARTESIAN_POINT('Ctrl Pts',(199.11315285686,10.6497554441766,28.3745477182844));
#71765=CARTESIAN_POINT('Ctrl Pts',(199.116328600465,10.6952577315414,28.3623589264119));
#71766=CARTESIAN_POINT('Ctrl Pts',(199.119502689493,10.7407363119845,28.3501764849615));
#71767=CARTESIAN_POINT('Ctrl Pts',(199.12267677852,10.7869708982647,28.3407188040294));
#71768=CARTESIAN_POINT('Ctrl Pts',(199.125850867547,10.8336070530522,28.3340632737125));
#71769=CARTESIAN_POINT('Ctrl Pts',(199.129024683154,10.8802391905317,28.3274083167129));
#71770=CARTESIAN_POINT('Ctrl Pts',(199.13219849876,10.9272722784719,28.3235551068591));
#71771=CARTESIAN_POINT('Ctrl Pts',(199.135372314367,10.9743444957301,28.3225294663557));
#71772=CARTESIAN_POINT('Ctrl Pts',(199.138549374687,11.0214648367325,28.3215027773004));
#71773=CARTESIAN_POINT('Ctrl Pts',(199.141726435008,11.0686238312664,28.3233094351217));
#71774=CARTESIAN_POINT('Ctrl Pts',(199.144903495329,11.1154593631351,28.3279231262565));
#71775=CARTESIAN_POINT('Ctrl Pts',(199.1480825397,11.1623241434446,28.332539698607));
#71776=CARTESIAN_POINT('Ctrl Pts',(199.151261584071,11.2088645111085,28.3399667052858));
#71777=CARTESIAN_POINT('Ctrl Pts',(199.154440628442,11.2547267752472,28.3501263841308));
#71778=CARTESIAN_POINT('Ctrl Pts',(199.157625293964,11.3006701325216,28.3603040272048));
#71779=CARTESIAN_POINT('Ctrl Pts',(199.160809959485,11.3459324626995,28.3732238252956));
#71780=CARTESIAN_POINT('Ctrl Pts',(199.163994625007,11.3901753816714,28.3887582468079));
#71781=CARTESIAN_POINT('Ctrl Pts',(199.164691561457,11.3998575610712,28.3921578203317));
#71782=CARTESIAN_POINT('Ctrl Pts',(199.165388497907,11.4094910014412,28.3956824317297));
#71783=CARTESIAN_POINT('Ctrl Pts',(199.166085434358,11.4190723032271,28.3993304459703));
#71784=CARTESIAN_POINT('Ctrl Pts',(199.169362596805,11.4641258836326,28.4164842844135));
#71785=CARTESIAN_POINT('Ctrl Pts',(199.172639759252,11.5082278906805,28.4364483183434));
#71786=CARTESIAN_POINT('Ctrl Pts',(199.1759169217,11.551005627053,28.459092770005));
#71787=CARTESIAN_POINT('Ctrl Pts',(199.179088162373,11.592400736286,28.4810053261508));
#71788=CARTESIAN_POINT('Ctrl Pts',(199.182259403045,11.6325553428388,28.5054273755897));
#71789=CARTESIAN_POINT('Ctrl Pts',(199.185430643718,11.6711502036526,28.5321919267556));
#71790=CARTESIAN_POINT('Ctrl Pts',(199.18859872715,11.7097066399855,28.5589298315245));
#71791=CARTESIAN_POINT('Ctrl Pts',(199.191766810582,11.7467059475697,28.5880053056637));
#71792=CARTESIAN_POINT('Ctrl Pts',(199.194934894014,11.7818556691029,28.6192067352712));
#71793=CARTESIAN_POINT('Ctrl Pts',(199.198101220393,11.8169858962251,28.6503908602325));
#71794=CARTESIAN_POINT('Ctrl Pts',(199.201267546772,11.8502681527442,28.6836982352638));
#71795=CARTESIAN_POINT('Ctrl Pts',(199.204433873151,11.8814432170039,28.7188771430192));
#71796=CARTESIAN_POINT('Ctrl Pts',(199.207599839623,11.9126147376819,28.7540520520874));
#71797=CARTESIAN_POINT('Ctrl Pts',(199.210765806094,11.9416791734333,28.7910976527551));
#71798=CARTESIAN_POINT('Ctrl Pts',(199.213931772566,11.9684162106679,28.829727588651));
#71799=CARTESIAN_POINT('Ctrl Pts',(199.217100915189,11.9951800709576,28.8683962787622));
#71800=CARTESIAN_POINT('Ctrl Pts',(199.220270057813,12.0196115576936,28.9086520148148));
#71801=CARTESIAN_POINT('Ctrl Pts',(199.223439200436,12.0415336788053,28.9501794307101));
#71802=CARTESIAN_POINT('Ctrl Pts',(199.226610278997,12.0634691915029,28.9917322144954));
#71803=CARTESIAN_POINT('Ctrl Pts',(199.229781357558,12.0828920580106,29.0345577156462));
#71804=CARTESIAN_POINT('Ctrl Pts',(199.232952436118,12.0996728621035,29.078319245337));
#71805=CARTESIAN_POINT('Ctrl Pts',(199.236129144687,12.116483459233,29.1221584702831));
#71806=CARTESIAN_POINT('Ctrl Pts',(199.239305853255,12.1306424730576,29.1669365062241));
#71807=CARTESIAN_POINT('Ctrl Pts',(199.242482561824,12.1420704636969,29.2123020360671));
#71808=CARTESIAN_POINT('Ctrl Pts',(199.243234152246,12.1447742585622,29.223035251601));
#71809=CARTESIAN_POINT('Ctrl Pts',(199.243985742669,12.147325406606,29.2338013173809));
#71810=CARTESIAN_POINT('Ctrl Pts',(199.244737333092,12.1497232789299,29.2445955278646));
#71811=CARTESIAN_POINT('Ctrl Pts',(199.248014495539,12.1601787303235,29.2916615629988));
#71812=CARTESIAN_POINT('Ctrl Pts',(199.251291657987,12.1677628892916,29.3394767473395));
#71813=CARTESIAN_POINT('Ctrl Pts',(199.254568820434,12.1723798432976,29.387658709597));
#71814=CARTESIAN_POINT('Ctrl Pts',(199.257743090611,12.1768518399255,29.4343279145435));
#71815=CARTESIAN_POINT('Ctrl Pts',(199.260917360789,12.1785401531388,29.4813406030709));
#71816=CARTESIAN_POINT('Ctrl Pts',(199.264091630967,12.1774090365302,29.5283376639313));
#71817=CARTESIAN_POINT('Ctrl Pts',(199.267262773696,12.1762790343537,29.5752884209544));
#71818=CARTESIAN_POINT('Ctrl Pts',(199.270433916425,12.1723351141447,29.6222230266559));
#71819=CARTESIAN_POINT('Ctrl Pts',(199.273605059154,12.1655935328295,29.6687802675847));
#71820=CARTESIAN_POINT('Ctrl Pts',(199.276774468309,12.1588556369463,29.7153120569865));
#71821=CARTESIAN_POINT('Ctrl Pts',(199.279943877464,12.1493231894927,29.761466340247));
#71822=CARTESIAN_POINT('Ctrl Pts',(199.283113286619,12.1370642147272,29.8068876571105));
#71823=CARTESIAN_POINT('Ctrl Pts',(199.286282353072,12.1248065654992,29.8523040626613));
#71824=CARTESIAN_POINT('Ctrl Pts',(199.289451419526,12.1098231214598,29.8969871225891));
#71825=CARTESIAN_POINT('Ctrl Pts',(199.292620485979,12.092232226292,29.9405948551098));
#71826=CARTESIAN_POINT('Ctrl Pts',(199.295792730805,12.0746236885721,29.9842463234201));
#71827=CARTESIAN_POINT('Ctrl Pts',(199.298964975631,12.0544026923683,30.0268197961744));
#71828=CARTESIAN_POINT('Ctrl Pts',(199.302137220457,12.0317356270029,30.0679935373513));
#71829=CARTESIAN_POINT('Ctrl Pts',(199.305311405725,12.0090546963434,30.1091924642338));
#71830=CARTESIAN_POINT('Ctrl Pts',(199.308485590992,11.9839250163396,30.1489894849433));
#71831=CARTESIAN_POINT('Ctrl Pts',(199.311659776259,11.956556948554,30.1870908722091));
#71832=CARTESIAN_POINT('Ctrl Pts',(199.314839567394,11.9291405465495,30.2252595496031));
#71833=CARTESIAN_POINT('Ctrl Pts',(199.318019358529,11.8994782249642,30.2617261911537));
#71834=CARTESIAN_POINT('Ctrl Pts',(199.321199149664,11.8678200524929,30.2962307573757));
#71835=CARTESIAN_POINT('Ctrl Pts',(199.321929177051,11.8605518603507,30.304152434387));
#71836=CARTESIAN_POINT('Ctrl Pts',(199.322659204439,11.8531786159839,30.311970853757));
#71837=CARTESIAN_POINT('Ctrl Pts',(199.323389231826,11.8457035972358,30.3196831632542));
#71838=CARTESIAN_POINT('Ctrl Pts',(199.326666394273,11.812147526388,30.354304454867));
#71839=CARTESIAN_POINT('Ctrl Pts',(199.329943556721,11.7763865406103,30.3869396180561));
#71840=CARTESIAN_POINT('Ctrl Pts',(199.333220719168,11.7386872767217,30.4172982991969));
#71841=CARTESIAN_POINT('Ctrl Pts',(199.336395134308,11.7021699798263,30.4467051591251));
#71842=CARTESIAN_POINT('Ctrl Pts',(199.339569549448,11.6638346296527,30.4739758072547));
#71843=CARTESIAN_POINT('Ctrl Pts',(199.342743964588,11.62396154616,30.4988829017526));
#71844=CARTESIAN_POINT('Ctrl Pts',(199.345915263681,11.5841276026118,30.5237655471181));
#71845=CARTESIAN_POINT('Ctrl Pts',(199.349086562773,11.5427593836559,30.5462889376308));
#71846=CARTESIAN_POINT('Ctrl Pts',(199.352257861865,11.5001675582563,30.5662680132912));
#71847=CARTESIAN_POINT('Ctrl Pts',(199.355427438465,11.4575988666251,30.586236237308));
#71848=CARTESIAN_POINT('Ctrl Pts',(199.358597015065,11.4138083883404,30.603662648244));
#71849=CARTESIAN_POINT('Ctrl Pts',(199.361766591665,11.3691304507295,30.6184085894003));
#71850=CARTESIAN_POINT('Ctrl Pts',(199.364935836341,11.3244571918726,30.633152986335));
#71851=CARTESIAN_POINT('Ctrl Pts',(199.368105081018,11.2788971872386,30.6452172986398));
#71852=CARTESIAN_POINT('Ctrl Pts',(199.371274325694,11.2328011743626,30.6545123107682));
#71853=CARTESIAN_POINT('Ctrl Pts',(199.37444676338,11.1866587198106,30.6638166876098));
#71854=CARTESIAN_POINT('Ctrl Pts',(199.377619201066,11.1399797264185,30.6703460892419));
#71855=CARTESIAN_POINT('Ctrl Pts',(199.380791638752,11.0931244413613,30.6740625626095));
#71856=CARTESIAN_POINT('Ctrl Pts',(199.383966025666,11.0462403672166,30.6777813194735));
#71857=CARTESIAN_POINT('Ctrl Pts',(199.387140412579,10.9991803424814,30.6786836981663));
#71858=CARTESIAN_POINT('Ctrl Pts',(199.390314799492,10.9523053989409,30.6767838746048));
#71859=CARTESIAN_POINT('Ctrl Pts',(199.393494803093,10.9053475159529,30.6748806895391));
#71860=CARTESIAN_POINT('Ctrl Pts',(199.396674806693,10.8585759200923,30.6701654715798));
#71861=CARTESIAN_POINT('Ctrl Pts',(199.399854810294,10.8123453406177,30.6627040858757));
#71862=CARTESIAN_POINT('Ctrl Pts',(199.400583583716,10.8017505043074,30.6609941319647));
#71863=CARTESIAN_POINT('Ctrl Pts',(199.401312357138,10.7911840289986,30.6591401572854));
#71864=CARTESIAN_POINT('Ctrl Pts',(199.40204113056,10.7806500773883,30.6571433247227));
#71865=CARTESIAN_POINT('Ctrl Pts',(199.40522003876,10.7347010016762,30.6484331451052));
#71866=CARTESIAN_POINT('Ctrl Pts',(199.40839894696,10.6891707968276,30.6369627383111));
#71867=CARTESIAN_POINT('Ctrl Pts',(199.41157785516,10.6444148634672,30.6227886146452));
#71868=CARTESIAN_POINT('Ctrl Pts',(199.41475187707,10.5997277243165,30.6086362779819));
#71869=CARTESIAN_POINT('Ctrl Pts',(199.41792589898,10.5558130271195,30.5917886189121));
#71870=CARTESIAN_POINT('Ctrl Pts',(199.42109992089,10.5130152595534,30.5723529852955));
#71871=CARTESIAN_POINT('Ctrl Pts',(199.424270708434,10.4702611034214,30.5529371568207));
#71872=CARTESIAN_POINT('Ctrl Pts',(199.427441495977,10.4286221287092,30.5309388040667));
#71873=CARTESIAN_POINT('Ctrl Pts',(199.430612283521,10.388424431426,30.5065139772618));
#71874=CARTESIAN_POINT('Ctrl Pts',(199.433781106762,10.3482516366209,30.4821042816399));
#71875=CARTESIAN_POINT('Ctrl Pts',(199.436949930002,10.3095188239599,30.4552713815384));
#71876=CARTESIAN_POINT('Ctrl Pts',(199.440118753243,10.2725265199744,30.4262167124164));
#71877=CARTESIAN_POINT('Ctrl Pts',(199.443288375647,10.2355248866845,30.3971547158284));
#71878=CARTESIAN_POINT('Ctrl Pts',(199.446457998052,10.2002650822288,30.3658701688511));
#71879=CARTESIAN_POINT('Ctrl Pts',(199.449627620456,10.1670158662807,30.3326058464075));
#71880=CARTESIAN_POINT('Ctrl Pts',(199.451757960924,10.1446686774975,30.310248504371));
#71881=CARTESIAN_POINT('Ctrl Pts',(199.453888301391,10.1232290655337,30.2869976831466));
#71882=CARTESIAN_POINT('Ctrl Pts',(199.456018641859,10.1027690874833,30.2629362700282));
#71883=CARTESIAN_POINT('Origin',(197.762132885264,11.,29.5));
#71884=CARTESIAN_POINT('',(200.055837189155,10.1027690874889,30.2629362700347));
#71885=CARTESIAN_POINT('',(199.956073744839,10.1027690874833,30.2629362700282));
#71886=CARTESIAN_POINT('',(197.762132885264,10.1027690874833,30.2629362700282));
#71887=CARTESIAN_POINT('Ctrl Pts',(200.055837189155,10.1027690874889,30.2629362700347));
#71888=CARTESIAN_POINT('Ctrl Pts',(200.054854794923,10.1121144588561,30.2739266455208));
#71889=CARTESIAN_POINT('Ctrl Pts',(200.053864348436,10.1216606349857,30.2847439824393));
#71890=CARTESIAN_POINT('Ctrl Pts',(200.049365182412,10.1655617649195,30.3326861750602));
#71891=CARTESIAN_POINT('Ctrl Pts',(200.045767937199,10.2020837943372,30.3677453333879));
#71892=CARTESIAN_POINT('Ctrl Pts',(200.038837688901,10.2752457687659,30.4294426115047));
#71893=CARTESIAN_POINT('Ctrl Pts',(200.035524082849,10.311392956766,30.4565313859838));
#71894=CARTESIAN_POINT('Ctrl Pts',(200.028401485108,10.3923792699774,30.5102481303646));
#71895=CARTESIAN_POINT('Ctrl Pts',(200.024601530178,10.437618439397,30.5361139813143));
#71896=CARTESIAN_POINT('Ctrl Pts',(200.020053351931,10.4956200767861,30.5643547433665));
#71897=CARTESIAN_POINT('Ctrl Pts',(200.019183258542,10.5069022843358,30.5696283465646));
#71898=CARTESIAN_POINT('Ctrl Pts',(200.01788982428,10.523984981196,30.5772854937322));
#71899=CARTESIAN_POINT('Ctrl Pts',(200.017459306931,10.5297239443401,30.5798031158698));
#71900=CARTESIAN_POINT('Ctrl Pts',(200.016678444491,10.5402351998181,30.5843145926775));
#71901=CARTESIAN_POINT('Ctrl Pts',(200.016327303062,10.5450007634233,30.586322928013));
#71902=CARTESIAN_POINT('Ctrl Pts',(200.015517248391,10.556083244364,30.5909076549117));
#71903=CARTESIAN_POINT('Ctrl Pts',(200.015059687144,10.5624095210276,30.5934606420703));
#71904=CARTESIAN_POINT('Ctrl Pts',(200.013572223532,10.5831782529244,30.6016328061134));
#71905=CARTESIAN_POINT('Ctrl Pts',(200.012554514343,10.5977101074211,30.6070221791975));
#71906=CARTESIAN_POINT('Ctrl Pts',(200.01007103355,10.6338376718621,30.6196152364247));
#71907=CARTESIAN_POINT('Ctrl Pts',(200.008619299216,10.655544375205,30.6264828319304));
#71908=CARTESIAN_POINT('Ctrl Pts',(200.001418939159,10.7652834656862,30.657733078677));
#71909=CARTESIAN_POINT('Ctrl Pts',(199.995901338364,10.8557410487224,30.6724453887902));
#71910=CARTESIAN_POINT('Ctrl Pts',(199.988014458571,10.9800048981241,30.6780438333142));
#71911=CARTESIAN_POINT('Ctrl Pts',(199.985890150566,11.0130624903483,30.6781409738603));
#71912=CARTESIAN_POINT('Ctrl Pts',(199.982855920796,11.0593177374628,30.6763298932124));
#71913=CARTESIAN_POINT('Ctrl Pts',(199.981981093508,11.072546943092,30.6755881632937));
#71914=CARTESIAN_POINT('Ctrl Pts',(199.980479725469,11.09504845619,30.673945305938));
#71915=CARTESIAN_POINT('Ctrl Pts',(199.979856690601,11.1043279112443,30.6731570521162));
#71916=CARTESIAN_POINT('Ctrl Pts',(199.978577114593,11.123260700138,30.6713223850789));
#71917=CARTESIAN_POINT('Ctrl Pts',(199.977920326972,11.1329123703985,30.6702664748319));
#71918=CARTESIAN_POINT('Ctrl Pts',(199.976250878958,11.1572712990166,30.6672963421513));
#71919=CARTESIAN_POINT('Ctrl Pts',(199.975233413792,11.1719571299483,30.6652234647745));
#71920=CARTESIAN_POINT('Ctrl Pts',(199.970562150302,11.2386281239938,30.6545251734251));
#71921=CARTESIAN_POINT('Ctrl Pts',(199.966811735006,11.2900308322721,30.6426952886861));
#71922=CARTESIAN_POINT('Ctrl Pts',(199.961855259039,11.355487901505,30.6229290907532));
#71923=CARTESIAN_POINT('Ctrl Pts',(199.960712321334,11.3704201569733,30.6180922494444));
#71924=CARTESIAN_POINT('Ctrl Pts',(199.95443149541,11.4516779504175,30.5899648359673));
#71925=CARTESIAN_POINT('Ctrl Pts',(199.949230212179,11.5159144819989,30.5610698425288));
#71926=CARTESIAN_POINT('Ctrl Pts',(199.942877184629,11.5935008907672,30.5174486727657));
#71927=CARTESIAN_POINT('Ctrl Pts',(199.941556307287,11.6095898585085,30.5078915642802));
#71928=CARTESIAN_POINT('Ctrl Pts',(199.939733840326,11.6318116889657,30.4939645384128));
#71929=CARTESIAN_POINT('Ctrl Pts',(199.939215068181,11.6381399898413,30.4899135692938));
#71930=CARTESIAN_POINT('Ctrl Pts',(199.93833985133,11.648828040544,30.4829266777494));
#71931=CARTESIAN_POINT('Ctrl Pts',(199.937981505076,11.6532076212099,30.4800216773532));
#71932=CARTESIAN_POINT('Ctrl Pts',(199.937227483164,11.6624325651079,30.4738134026796));
#71933=CARTESIAN_POINT('Ctrl Pts',(199.936832263503,11.667272907289,30.4705031259178));
#71934=CARTESIAN_POINT('Ctrl Pts',(199.935737450634,11.6806881675051,30.4611807058516));
#71935=CARTESIAN_POINT('Ctrl Pts',(199.935042781223,11.689208156398,30.455089978089));
#71936=CARTESIAN_POINT('Ctrl Pts',(199.930451061393,11.745476315257,30.4137201443066));
#71937=CARTESIAN_POINT('Ctrl Pts',(199.926748257664,11.7905854465486,30.3749833486178));
#71938=CARTESIAN_POINT('Ctrl Pts',(199.917708597861,11.8936836504557,30.271937123872));
#71939=CARTESIAN_POINT('Ctrl Pts',(199.912405460425,11.947872198007,30.2043394197111));
#71940=CARTESIAN_POINT('Ctrl Pts',(199.905657626896,12.0036306981697,30.1165477964377));
#71941=CARTESIAN_POINT('Ctrl Pts',(199.904503353043,12.0127452620131,30.1014588480852));
#71942=CARTESIAN_POINT('Ctrl Pts',(199.902650331012,12.0266834851289,30.0771687997558));
#71943=CARTESIAN_POINT('Ctrl Pts',(199.90195948037,12.0317301592159,30.0680982918493));
#71944=CARTESIAN_POINT('Ctrl Pts',(199.900649718098,12.041012559231,30.0508830813142));
#71945=CARTESIAN_POINT('Ctrl Pts',(199.9000317723,12.0452742518778,30.0427532109555));
#71946=CARTESIAN_POINT('Ctrl Pts',(199.898619773821,12.054742987249,30.0241648339521));
#71947=CARTESIAN_POINT('Ctrl Pts',(199.897823741306,12.0598902430807,30.0136771340245));
#71948=CARTESIAN_POINT('Ctrl Pts',(199.895308197414,12.0755551712255,29.9805211379587));
#71949=CARTESIAN_POINT('Ctrl Pts',(199.893570135963,12.0855073505922,29.9575949316584));
#71950=CARTESIAN_POINT('Ctrl Pts',(199.889332081664,12.1076935040541,29.9016803379145));
#71951=CARTESIAN_POINT('Ctrl Pts',(199.886812016899,12.1191928487818,29.8684277315629));
#71952=CARTESIAN_POINT('Ctrl Pts',(199.883165679721,12.1334893397921,29.8201971280844));
#71953=CARTESIAN_POINT('Ctrl Pts',(199.882063362434,12.1375117107615,29.8056000228924));
#71954=CARTESIAN_POINT('Ctrl Pts',(199.875902082689,12.1583532616546,29.7238433338055));
#71955=CARTESIAN_POINT('Ctrl Pts',(199.870779935361,12.1695068147498,29.655378487046));
#71956=CARTESIAN_POINT('Ctrl Pts',(199.864401991586,12.1760441257028,29.566432527908));
#71957=CARTESIAN_POINT('Ctrl Pts',(199.862991203876,12.1770007859915,29.5465008095379));
#71958=CARTESIAN_POINT('Ctrl Pts',(199.861067296549,12.1776244839142,29.5188440315771));
#71959=CARTESIAN_POINT('Ctrl Pts',(199.860534530294,12.1777226257001,29.511133170358));
#71960=CARTESIAN_POINT('Ctrl Pts',(199.85964663371,12.1777602419313,29.4981855146602));
#71961=CARTESIAN_POINT('Ctrl Pts',(199.859289391478,12.1777405359075,29.4929491661793));
#71962=CARTESIAN_POINT('Ctrl Pts',(199.858543090051,12.1776257827794,29.4819504014819));
#71963=CARTESIAN_POINT('Ctrl Pts',(199.858154423026,12.1775233663272,29.4761882902396));
#71964=CARTESIAN_POINT('Ctrl Pts',(199.857097505559,12.177127651999,29.4604338590818));
#71965=CARTESIAN_POINT('Ctrl Pts',(199.856433639937,12.176749420163,29.4504439012595));
#71966=CARTESIAN_POINT('Ctrl Pts',(199.851545895265,12.1729965837153,29.3763051770765));
#71967=CARTESIAN_POINT('Ctrl Pts',(199.847553950856,12.1645054653802,29.3125150579678));
#71968=CARTESIAN_POINT('Ctrl Pts',(199.838517384869,12.1335135283684,29.1700010745316));
#71969=CARTESIAN_POINT('Ctrl Pts',(199.833492592613,12.1079397550879,29.092299040243));
#71970=CARTESIAN_POINT('Ctrl Pts',(199.827033682706,12.0671543785838,29.0013996059917));
#71971=CARTESIAN_POINT('Ctrl Pts',(199.825852529094,12.059388569559,28.985105230375));
#71972=CARTESIAN_POINT('Ctrl Pts',(199.823966332002,12.046531021037,28.9596505628223));
#71973=CARTESIAN_POINT('Ctrl Pts',(199.823269690646,12.0416860091204,28.9503683606677));
#71974=CARTESIAN_POINT('Ctrl Pts',(199.821960937804,12.0324099275392,28.9331603097828));
#71975=CARTESIAN_POINT('Ctrl Pts',(199.821349936308,12.028009681516,28.9252186678836));
#71976=CARTESIAN_POINT('Ctrl Pts',(199.819957867093,12.017830520482,28.9073379873598));
#71977=CARTESIAN_POINT('Ctrl Pts',(199.819174914375,12.011997079214,28.8974312278221));
#71978=CARTESIAN_POINT('Ctrl Pts',(199.816746720231,11.9935806748748,28.8671771107269));
#71979=CARTESIAN_POINT('Ctrl Pts',(199.815084732947,11.9805227365437,28.8471275865045));
#71980=CARTESIAN_POINT('Ctrl Pts',(199.811077678076,11.9479938742955,28.8003609578919));
#71981=CARTESIAN_POINT('Ctrl Pts',(199.808715417237,11.9279915437114,28.7740395622481));
#71982=CARTESIAN_POINT('Ctrl Pts',(199.802960947675,11.8772233166769,28.7127646414821));
#71983=CARTESIAN_POINT('Ctrl Pts',(199.799545741574,11.8454399328425,28.678725862665));
#71984=CARTESIAN_POINT('Ctrl Pts',(199.792272262698,11.7735420299162,28.610334106438));
#71985=CARTESIAN_POINT('Ctrl Pts',(199.788422908465,11.7329572433049,28.5766109492801));
#71986=CARTESIAN_POINT('Ctrl Pts',(199.783825097849,11.6801211500669,28.5383938194425));
#71987=CARTESIAN_POINT('Ctrl Pts',(199.782951856447,11.6698793142148,28.531231214252));
#71988=CARTESIAN_POINT('Ctrl Pts',(199.781654723862,11.6543258983543,28.520718600387));
#71989=CARTESIAN_POINT('Ctrl Pts',(199.781223597971,11.6490987206393,28.5172460652825));
#71990=CARTESIAN_POINT('Ctrl Pts',(199.780445546479,11.6395555313057,28.511015665795));
#71991=CARTESIAN_POINT('Ctrl Pts',(199.780097779787,11.635249068207,28.5082440249216));
#71992=CARTESIAN_POINT('Ctrl Pts',(199.779293790955,11.625199002952,28.5018681235561));
#71993=CARTESIAN_POINT('Ctrl Pts',(199.778838918562,11.6194421755478,28.4982852538323));
#71994=CARTESIAN_POINT('Ctrl Pts',(199.777370032423,11.6006342194411,28.4868039176794));
#71995=CARTESIAN_POINT('Ctrl Pts',(199.77636779531,11.5874599505852,28.479108906149));
#71996=CARTESIAN_POINT('Ctrl Pts',(199.769774328673,11.4988182136531,28.4296182046935));
#71997=CARTESIAN_POINT('Ctrl Pts',(199.764541619873,11.4190965963708,28.3959627259269));
#71998=CARTESIAN_POINT('Ctrl Pts',(199.755646199711,11.2821190671527,28.3551363638869));
#71999=CARTESIAN_POINT('Ctrl Pts',(199.752076847629,11.2267418117348,28.3428954407303));
#72000=CARTESIAN_POINT('Ctrl Pts',(199.747382107985,11.1555138718028,28.332461497422));
#72001=CARTESIAN_POINT('Ctrl Pts',(199.746372662018,11.1402834036833,28.3305337752308));
#72002=CARTESIAN_POINT('Ctrl Pts',(199.744702847601,11.1152608433243,28.3278624951988));
#72003=CARTESIAN_POINT('Ctrl Pts',(199.744047937266,11.1054891427547,28.3269427025056));
#72004=CARTESIAN_POINT('Ctrl Pts',(199.742761300309,11.086381992349,28.3253848486058));
#72005=CARTESIAN_POINT('Ctrl Pts',(199.742129965509,11.0770481642694,28.3247357002585));
#72006=CARTESIAN_POINT('Ctrl Pts',(199.740615801925,11.0547682943337,28.3234527281501));
#72007=CARTESIAN_POINT('Ctrl Pts',(199.739729905026,11.041817818214,28.3229212872685));
#72008=CARTESIAN_POINT('Ctrl Pts',(199.736535022065,10.9954336900868,28.3217842681858));
#72009=CARTESIAN_POINT('Ctrl Pts',(199.73419010338,10.961989098956,28.3223888759115));
#72010=CARTESIAN_POINT('Ctrl Pts',(199.727859480885,10.8732788271546,28.3277753887231));
#72011=CARTESIAN_POINT('Ctrl Pts',(199.723814512345,10.8182506426103,28.335038660732));
#72012=CARTESIAN_POINT('Ctrl Pts',(199.715064151226,10.701318257272,28.3589608407561));
#72013=CARTESIAN_POINT('Ctrl Pts',(199.710365728278,10.6398347666837,28.3768510827219));
#72014=CARTESIAN_POINT('Ctrl Pts',(199.705011044746,10.5688344197503,28.4039449013017));
#72015=CARTESIAN_POINT('Ctrl Pts',(199.704168586191,10.5576319123567,28.4084181021858));
#72016=CARTESIAN_POINT('Ctrl Pts',(199.702902311584,10.5407176843702,28.4154751884102));
#72017=CARTESIAN_POINT('Ctrl Pts',(199.702471911415,10.53495495981,28.4179337231796));
#72018=CARTESIAN_POINT('Ctrl Pts',(199.701691155641,10.5244714138408,28.4225055114323));
#72019=CARTESIAN_POINT('Ctrl Pts',(199.701340005253,10.5197446566767,28.4246039723967));
#72020=CARTESIAN_POINT('Ctrl Pts',(199.700529794802,10.5088130857615,28.4295435351708));
#72021=CARTESIAN_POINT('Ctrl Pts',(199.700072088676,10.5026189374618,28.4324075159445));
#72022=CARTESIAN_POINT('Ctrl Pts',(199.698583625748,10.4824292699813,28.4419564511522));
#72023=CARTESIAN_POINT('Ctrl Pts',(199.697565084639,10.4685402440131,28.448864331169));
#72024=CARTESIAN_POINT('Ctrl Pts',(199.695079082979,10.4345917577724,28.4665940423286));
#72025=CARTESIAN_POINT('Ctrl Pts',(199.693625696691,10.4147017799682,28.4777277918263));
#72026=CARTESIAN_POINT('Ctrl Pts',(199.68640322336,10.3164917610084,28.5365092977627));
#72027=CARTESIAN_POINT('Ctrl Pts',(199.680866458342,10.243601968728,28.5926076013548));
#72028=CARTESIAN_POINT('Ctrl Pts',(199.672973748462,10.1544869445651,28.6794656843314));
#72029=CARTESIAN_POINT('Ctrl Pts',(199.670866626089,10.1319868811555,28.7033056873993));
#72030=CARTESIAN_POINT('Ctrl Pts',(199.667852870047,10.1018539577391,28.7380267647443));
#72031=CARTESIAN_POINT('Ctrl Pts',(199.666980677835,10.093365314467,28.7481469234929));
#72032=CARTESIAN_POINT('Ctrl Pts',(199.665482419578,10.0791894484271,28.7656366117744));
#72033=CARTESIAN_POINT('Ctrl Pts',(199.66485982243,10.0734159930168,28.7729348533236));
#72034=CARTESIAN_POINT('Ctrl Pts',(199.663579900077,10.0617898714637,28.7879948723523));
#72035=CARTESIAN_POINT('Ctrl Pts',(199.662922314758,10.0559456202391,28.7957622095911));
#72036=CARTESIAN_POINT('Ctrl Pts',(199.661248224565,10.041396265763,28.8156057149122));
#72037=CARTESIAN_POINT('Ctrl Pts',(199.660226860244,10.0328229620318,28.8277759308807));
#72038=CARTESIAN_POINT('Ctrl Pts',(199.655493041924,9.99448745120509,28.8844469754947));
#72039=CARTESIAN_POINT('Ctrl Pts',(199.651680627031,9.96755429819227,28.9307764298256));
#72040=CARTESIAN_POINT('Ctrl Pts',(199.646579384302,9.93642719480184,28.9938472524547));
#72041=CARTESIAN_POINT('Ctrl Pts',(199.645354115873,9.92931052038818,29.00908072912));
#72042=CARTESIAN_POINT('Ctrl Pts',(199.638720905804,9.89266968857507,29.0921016198844));
#72043=CARTESIAN_POINT('Ctrl Pts',(199.633248825515,9.86925131248244,29.1624056170936));
#72044=CARTESIAN_POINT('Ctrl Pts',(199.626948458616,9.84920719905091,29.2490127335935));
#72045=CARTESIAN_POINT('Ctrl Pts',(199.625899112991,9.84611303482275,29.2636451809904));
#72046=CARTESIAN_POINT('Ctrl Pts',(199.624402282262,9.84204523038445,29.2848718169007));
#72047=CARTESIAN_POINT('Ctrl Pts',(199.623943932103,9.84084765031514,29.2914209524009));
#72048=CARTESIAN_POINT('Ctrl Pts',(199.623135117246,9.83881914602302,29.3030715961609));
#72049=CARTESIAN_POINT('Ctrl Pts',(199.622783503396,9.83796617913246,29.30816889108));
#72050=CARTESIAN_POINT('Ctrl Pts',(199.622007021387,9.83614694049944,29.3194982418318));
#72051=CARTESIAN_POINT('Ctrl Pts',(199.621583042447,9.83519713262357,29.3257326380603));
#72052=CARTESIAN_POINT('Ctrl Pts',(199.620315836725,9.83249193071049,29.3445003938163));
#72053=CARTESIAN_POINT('Ctrl Pts',(199.619480336357,9.83088836259479,29.3570551510618));
#72054=CARTESIAN_POINT('Ctrl Pts',(199.61752747636,9.82758058984638,29.3867545145573));
#72055=CARTESIAN_POINT('Ctrl Pts',(199.616417514124,9.82604953525392,29.4039157677796));
#72056=CARTESIAN_POINT('Ctrl Pts',(199.612204174843,9.82162415768627,29.4698299452879));
#72057=CARTESIAN_POINT('Ctrl Pts',(199.609182308378,9.82138630290501,29.5187140941237));
#72058=CARTESIAN_POINT('Ctrl Pts',(199.601527794205,9.82846865458007,29.6421317640584));
#72059=CARTESIAN_POINT('Ctrl Pts',(199.596900409197,9.83985272435551,29.7162033669141));
#72060=CARTESIAN_POINT('Ctrl Pts',(199.590869040678,9.86266910193541,29.8064454557614));
#72061=CARTESIAN_POINT('Ctrl Pts',(199.589671136954,9.86757098146807,29.8240908039078));
#72062=CARTESIAN_POINT('Ctrl Pts',(199.587764275473,9.8759353353345,29.8516880753779));
#72063=CARTESIAN_POINT('Ctrl Pts',(199.587064041173,9.87912349578678,29.861720504168));
#72064=CARTESIAN_POINT('Ctrl Pts',(199.585746348149,9.88533658157581,29.8804003556873));
#72065=CARTESIAN_POINT('Ctrl Pts',(199.585129988859,9.88832877135777,29.8890578855812));
#72066=CARTESIAN_POINT('Ctrl Pts',(199.583735050144,9.89529106062368,29.9084660901051));
#72067=CARTESIAN_POINT('Ctrl Pts',(199.582954676595,9.89931765584436,29.9191953587669));
#72068=CARTESIAN_POINT('Ctrl Pts',(199.580543419739,9.91215639220565,29.9519445045687));
#72069=CARTESIAN_POINT('Ctrl Pts',(199.578896129357,9.92147714930142,29.9737571875917));
#72070=CARTESIAN_POINT('Ctrl Pts',(199.57493308673,9.94517747832428,30.0248906673563));
#72071=CARTESIAN_POINT('Ctrl Pts',(199.572600660517,9.96012997004526,30.0539230839233));
#72072=CARTESIAN_POINT('Ctrl Pts',(199.564915632292,10.0126960117582,30.1463393717559));
#72073=CARTESIAN_POINT('Ctrl Pts',(199.559458413844,10.0550491246193,30.206816476863));
#72074=CARTESIAN_POINT('Ctrl Pts',(199.554117165109,10.1027690888331,30.2629362716156));
#72075=CARTESIAN_POINT('',(199.512132885214,9.82225014354375,29.5005814785295));
#72076=CARTESIAN_POINT('Ctrl Pts',(199.456018641859,10.1027690874833,30.2629362700282));
#72077=CARTESIAN_POINT('Ctrl Pts',(199.459191357844,10.0722980428734,30.2271016082947));
#72078=CARTESIAN_POINT('Ctrl Pts',(199.462364073829,10.0440019616846,30.1894679089783));
#72079=CARTESIAN_POINT('Ctrl Pts',(199.465536789815,10.018083504747,30.150334574546));
#72080=CARTESIAN_POINT('Ctrl Pts',(199.468715460125,9.99211640591272,30.1111277974852));
#72081=CARTESIAN_POINT('Ctrl Pts',(199.471894130436,9.96853612074149,30.0704162483886));
#72082=CARTESIAN_POINT('Ctrl Pts',(199.475072800746,9.94750007695886,30.0285252827428));
#72083=CARTESIAN_POINT('Ctrl Pts',(199.476946210262,9.93510208636799,30.0038360491928));
#72084=CARTESIAN_POINT('Ctrl Pts',(199.478819619778,9.92358695319116,29.9787375612637));
#72085=CARTESIAN_POINT('Ctrl Pts',(199.480693029294,9.91297891505301,29.9532992647034));
#72086=CARTESIAN_POINT('Ctrl Pts',(199.484218641163,9.8930154074229,29.9054263573039));
#72087=CARTESIAN_POINT('Ctrl Pts',(199.487744253032,9.87619275675429,29.8561715335063));
#72088=CARTESIAN_POINT('Ctrl Pts',(199.491269864901,9.86268036845629,29.805939729694));
#72089=CARTESIAN_POINT('Ctrl Pts',(199.494773776819,9.8492511481827,29.7560170999371));
#72090=CARTESIAN_POINT('Ctrl Pts',(199.498277688736,9.83909172096559,29.70512978883));
#72091=CARTESIAN_POINT('Ctrl Pts',(199.501781600653,9.83232178947454,29.6536966465609));
#72092=CARTESIAN_POINT('Ctrl Pts',(199.50523202884,9.82565519425427,29.6030485800527));
#72093=CARTESIAN_POINT('Ctrl Pts',(199.508682457027,9.82227546647417,29.5518715540156));
#72094=CARTESIAN_POINT('Ctrl Pts',(199.512132885214,9.82225014354375,29.5005814785295));
#72095=CARTESIAN_POINT('Ctrl Pts',(199.512132885264,9.82225014354338,29.5005814777886));
#72096=CARTESIAN_POINT('Ctrl Pts',(199.515343406687,9.82222658133527,29.4528575788382));
#72097=CARTESIAN_POINT('Ctrl Pts',(199.518553928109,9.82510810646364,29.4051355189712));
#72098=CARTESIAN_POINT('Ctrl Pts',(199.521764449532,9.83086776361372,29.3577858082243));
#72099=CARTESIAN_POINT('Ctrl Pts',(199.524979232366,9.83663506571088,29.3103732489391));
#72100=CARTESIAN_POINT('Ctrl Pts',(199.5281940152,9.84528806402763,29.2633345593417));
#72101=CARTESIAN_POINT('Ctrl Pts',(199.531408798033,9.85674805959125,29.2170334591306));
#72102=CARTESIAN_POINT('Ctrl Pts',(199.534625630782,9.86821536265037,29.1707028349044));
#72103=CARTESIAN_POINT('Ctrl Pts',(199.53784246353,9.8824930695955,29.1251112500719));
#72104=CARTESIAN_POINT('Ctrl Pts',(199.541059296278,9.89945259428958,29.0806070216562));
#72105=CARTESIAN_POINT('Ctrl Pts',(199.544283566842,9.91645133203196,29.0359998925703));
#72106=CARTESIAN_POINT('Ctrl Pts',(199.547507837406,9.93614405904267,28.9924856352886));
#72107=CARTESIAN_POINT('Ctrl Pts',(199.55073210797,9.95835447491095,28.950391355088));
#72108=CARTESIAN_POINT('Ctrl Pts',(199.553603047989,9.97813097024559,28.9129099616311));
#72109=CARTESIAN_POINT('Ctrl Pts',(199.556473988009,9.99990278314456,28.8765542520836));
#72110=CARTESIAN_POINT('Ctrl Pts',(199.559344928028,10.0235170635946,28.8415350142877));
#72111=CARTESIAN_POINT('Ctrl Pts',(199.562622090476,10.0504726365378,28.8015607444461));
#72112=CARTESIAN_POINT('Ctrl Pts',(199.565899252923,10.0799476785143,28.7631542676721));
#72113=CARTESIAN_POINT('Ctrl Pts',(199.56917641537,10.1117307368903,28.7266483473124));
#72114=CARTESIAN_POINT('Ctrl Pts',(199.572350409119,10.1425132294368,28.691291673701));
#72115=CARTESIAN_POINT('Ctrl Pts',(199.575524402868,10.1754601677577,28.6577181154801));
#72116=CARTESIAN_POINT('Ctrl Pts',(199.578698396617,10.2103356226518,28.6262006902914));
#72117=CARTESIAN_POINT('Ctrl Pts',(199.581869266297,10.245176750663,28.5947142867759));
#72118=CARTESIAN_POINT('Ctrl Pts',(199.585040135978,10.2819422266949,28.5652803821609));
#72119=CARTESIAN_POINT('Ctrl Pts',(199.588211005658,10.3203588108115,28.5381357078785));
#72120=CARTESIAN_POINT('Ctrl Pts',(199.591380145721,10.3587544398008,28.5110058402249));
#72121=CARTESIAN_POINT('Ctrl Pts',(199.594549285785,10.3987989386431,28.486163049911));
#72122=CARTESIAN_POINT('Ctrl Pts',(199.597718425848,10.4401876200514,28.4638025469264));
#72123=CARTESIAN_POINT('Ctrl Pts',(199.600887227748,10.4815718850841,28.4414444299173));
#72124=CARTESIAN_POINT('Ctrl Pts',(199.604056029649,10.5242995572051,28.4215683368624));
#72125=CARTESIAN_POINT('Ctrl Pts',(199.60722483155,10.5680411049611,28.4043236903644));
#72126=CARTESIAN_POINT('Ctrl Pts',(199.610396820559,10.6118266469678,28.3870616995943));
#72127=CARTESIAN_POINT('Ctrl Pts',(199.613568809568,10.6566275796872,28.3724366387231));
#72128=CARTESIAN_POINT('Ctrl Pts',(199.616740798577,10.702096002898,28.3605491362017));
#72129=CARTESIAN_POINT('Ctrl Pts',(199.619914732898,10.7475923109004,28.3486543433345));
#72130=CARTESIAN_POINT('Ctrl Pts',(199.623088667219,10.7937563777182,28.3395005579516));
#72131=CARTESIAN_POINT('Ctrl Pts',(199.62626260154,10.8402303732158,28.3331372279239));
#72132=CARTESIAN_POINT('Ctrl Pts',(199.629442151318,10.8867865924598,28.3267626396251));
#72133=CARTESIAN_POINT('Ctrl Pts',(199.632621701097,10.933653279433,28.3231883931202));
#72134=CARTESIAN_POINT('Ctrl Pts',(199.635801250876,10.9804697299899,28.3224119433973));
#72135=CARTESIAN_POINT('Ctrl Pts',(199.636533109505,10.9912457912878,28.3222332226761));
#72136=CARTESIAN_POINT('Ctrl Pts',(199.637264968134,11.0020192069751,28.3222025154569));
#72137=CARTESIAN_POINT('Ctrl Pts',(199.637996826763,11.0127856191094,28.322319402196));
#72138=CARTESIAN_POINT('Ctrl Pts',(199.64127398921,11.0609961342868,28.3228428049635));
#72139=CARTESIAN_POINT('Ctrl Pts',(199.644551151657,11.1092832441449,28.3263326393911));
#72140=CARTESIAN_POINT('Ctrl Pts',(199.647828314105,11.1572527280681,28.3327953726895));
#72141=CARTESIAN_POINT('Ctrl Pts',(199.651002230128,11.2037109418765,28.3390544987172));
#72142=CARTESIAN_POINT('Ctrl Pts',(199.654176146152,11.2498706479703,28.3481018880395));
#72143=CARTESIAN_POINT('Ctrl Pts',(199.657350062175,11.2953740813938,28.3598907006165));
#72144=CARTESIAN_POINT('Ctrl Pts',(199.660520852732,11.340832705984,28.3716679043346));
#72145=CARTESIAN_POINT('Ctrl Pts',(199.663691643288,11.3856358003685,28.3861810487819));
#72146=CARTESIAN_POINT('Ctrl Pts',(199.666862433845,11.4294353779103,28.4033321748592));
#72147=CARTESIAN_POINT('Ctrl Pts',(199.670031493551,11.4732110464232,28.4204739385913));
#72148=CARTESIAN_POINT('Ctrl Pts',(199.673200553257,11.5159837656456,28.4402506284899));
#72149=CARTESIAN_POINT('Ctrl Pts',(199.676369612963,11.5574229250327,28.4625151831723));
#72150=CARTESIAN_POINT('Ctrl Pts',(199.679538333435,11.598857648546,28.4847773545353));
#72151=CARTESIAN_POINT('Ctrl Pts',(199.682707053908,11.6389586064701,28.5095265965194));
#72152=CARTESIAN_POINT('Ctrl Pts',(199.68587577438,11.6774197595813,28.5365699133674));
#72153=CARTESIAN_POINT('Ctrl Pts',(199.689047680989,11.7159195852349,28.5636404221673));
#72154=CARTESIAN_POINT('Ctrl Pts',(199.692219587598,11.7527758612525,28.5930092857949));
#72155=CARTESIAN_POINT('Ctrl Pts',(199.695391494207,11.7877131930823,28.6244413280973));
#72156=CARTESIAN_POINT('Ctrl Pts',(199.698565345474,11.822671944569,28.6558926410058));
#72157=CARTESIAN_POINT('Ctrl Pts',(199.70173919674,11.8557090198283,28.6894092530028));
#72158=CARTESIAN_POINT('Ctrl Pts',(199.704913048007,11.8865863041646,28.7247195425088));
#72159=CARTESIAN_POINT('Ctrl Pts',(199.7080925146,11.9175182180377,28.7600923046319));
#72160=CARTESIAN_POINT('Ctrl Pts',(199.711271981192,11.9462823814283,28.7972646323191));
#72161=CARTESIAN_POINT('Ctrl Pts',(199.714451447785,11.9726825192878,28.8359339045155));
#72162=CARTESIAN_POINT('Ctrl Pts',(199.715183873689,11.9787640880893,28.8448418064598));
#72163=CARTESIAN_POINT('Ctrl Pts',(199.715916299593,11.9847203975814,28.8538290392186));
#72164=CARTESIAN_POINT('Ctrl Pts',(199.716648725497,11.9905493962399,28.8628917234028));
#72165=CARTESIAN_POINT('Ctrl Pts',(199.719925887944,12.0166306358653,28.9034417478069));
#72166=CARTESIAN_POINT('Ctrl Pts',(199.723203050392,12.0402766244894,28.9456874097543));
#72167=CARTESIAN_POINT('Ctrl Pts',(199.726480212839,12.061265130975,28.9893030406625));
#72168=CARTESIAN_POINT('Ctrl Pts',(199.729654174801,12.0815926924885,29.031545180228));
#72169=CARTESIAN_POINT('Ctrl Pts',(199.732828136764,12.0994274112475,29.0750717343834));
#72170=CARTESIAN_POINT('Ctrl Pts',(199.736002098726,12.1146116179335,29.119558146798));
#72171=CARTESIAN_POINT('Ctrl Pts',(199.739172935786,12.1297808751082,29.1640007604066));
#72172=CARTESIAN_POINT('Ctrl Pts',(199.742343772845,12.1423046063959,29.2094008370208));
#72173=CARTESIAN_POINT('Ctrl Pts',(199.745514609904,12.1520732126151,29.2554138694147));
#72174=CARTESIAN_POINT('Ctrl Pts',(199.748683716579,12.1618364879259,29.301401791649));
#72175=CARTESIAN_POINT('Ctrl Pts',(199.751852823253,12.1688475013121,29.3480014631884));
#72176=CARTESIAN_POINT('Ctrl Pts',(199.755021929928,12.1730472183889,29.3948558801923));
#72177=CARTESIAN_POINT('Ctrl Pts',(199.75819069774,12.1772464864021,29.4417052871888));
#72178=CARTESIAN_POINT('Ctrl Pts',(199.761359465551,12.1786350075224,29.4888088310685));
#72179=CARTESIAN_POINT('Ctrl Pts',(199.764528233363,12.1772056241259,29.5358047626201));
#72180=CARTESIAN_POINT('Ctrl Pts',(199.767700187501,12.1757748034253,29.5828479505267));
#72181=CARTESIAN_POINT('Ctrl Pts',(199.77087214164,12.1715204436319,29.6297827528572));
#72182=CARTESIAN_POINT('Ctrl Pts',(199.774044095779,12.1644874693901,29.6762498117257));
#72183=CARTESIAN_POINT('Ctrl Pts',(199.777217994735,12.1574501830264,29.7227453609058));
#72184=CARTESIAN_POINT('Ctrl Pts',(199.780391893692,12.147631008309,29.7687720512951));
#72185=CARTESIAN_POINT('Ctrl Pts',(199.783565792648,12.1351258123785,29.8139816118375));
#72186=CARTESIAN_POINT('Ctrl Pts',(199.786745306692,12.1225984929426,29.8592711546497));
#72187=CARTESIAN_POINT('Ctrl Pts',(199.789924820736,12.1073758571237,29.9037401591285));
#72188=CARTESIAN_POINT('Ctrl Pts',(199.793104334781,12.0896026746266,29.9470582444677));
#72189=CARTESIAN_POINT('Ctrl Pts',(199.793836431264,12.0855103245924,29.9570324158379));
#72190=CARTESIAN_POINT('Ctrl Pts',(199.794568527748,12.0812829459443,29.9669456695963));
#72191=CARTESIAN_POINT('Ctrl Pts',(199.795300624231,12.0769226471017,29.976794163827));
#72192=CARTESIAN_POINT('Ctrl Pts',(199.798577786678,12.0574041711255,30.0208800407323));
#72193=CARTESIAN_POINT('Ctrl Pts',(199.801854949126,12.0351300999337,30.0638648594177));
#72194=CARTESIAN_POINT('Ctrl Pts',(199.805132111573,12.0102501699625,30.1053838919155));
#72195=CARTESIAN_POINT('Ctrl Pts',(199.808306067234,11.9861537768636,30.1455953768076));
#72196=CARTESIAN_POINT('Ctrl Pts',(199.811480022895,11.9596135441534,30.1844315167418));
#72197=CARTESIAN_POINT('Ctrl Pts',(199.814653978556,11.9308137911021,30.2215821150736));
#72198=CARTESIAN_POINT('Ctrl Pts',(199.81782480934,11.9020423924787,30.2586961372598));
#72199=CARTESIAN_POINT('Ctrl Pts',(199.820995640123,11.8710162164852,30.2941274644022));
#72200=CARTESIAN_POINT('Ctrl Pts',(199.824166470907,11.8379626851255,30.3275950705733));
#72201=CARTESIAN_POINT('Ctrl Pts',(199.827335571346,11.8049271913131,30.3610444132335));
#72202=CARTESIAN_POINT('Ctrl Pts',(199.830504671784,11.7698669245265,30.3925317623392));
#72203=CARTESIAN_POINT('Ctrl Pts',(199.833673772223,11.7330475563883,30.4218114463236));
#72204=CARTESIAN_POINT('Ctrl Pts',(199.836842533851,11.6962321246362,30.451087999995));
#72205=CARTESIAN_POINT('Ctrl Pts',(199.840011295479,11.6576584019286,30.4781570125518));
#72206=CARTESIAN_POINT('Ctrl Pts',(199.843180057106,11.6176245578356,30.5028135260648));
#72207=CARTESIAN_POINT('Ctrl Pts',(199.846352005186,11.5775504564012,30.5274948337414));
#72208=CARTESIAN_POINT('Ctrl Pts',(199.849523953266,11.5360137799205,30.5497585112635));
#72209=CARTESIAN_POINT('Ctrl Pts',(199.852695901346,11.4933393488691,30.5694444115322));
#72210=CARTESIAN_POINT('Ctrl Pts',(199.85586979431,11.450638751925,30.5891423822407));
#72211=CARTESIAN_POINT('Ctrl Pts',(199.859043687275,11.40679953099,30.6062592279677));
#72212=CARTESIAN_POINT('Ctrl Pts',(199.862217580239,11.3621652685777,30.6206834435897));
#72213=CARTESIAN_POINT('Ctrl Pts',(199.865397088449,11.3174520393221,30.6351331785037));
#72214=CARTESIAN_POINT('Ctrl Pts',(199.868576596658,11.2719415022112,30.6468806455459));
#72215=CARTESIAN_POINT('Ctrl Pts',(199.871756104867,11.2259891979731,30.6558650201903));
#72216=CARTESIAN_POINT('Ctrl Pts',(199.872488244233,11.2154078474385,30.6579338352154));
#72217=CARTESIAN_POINT('Ctrl Pts',(199.873220383599,11.204803095393,30.6598563588498));
#72218=CARTESIAN_POINT('Ctrl Pts',(199.873952522965,11.194179310854,30.661632238592));
#72219=CARTESIAN_POINT('Ctrl Pts',(199.877229685412,11.1466257037727,30.669581334997));
#72220=CARTESIAN_POINT('Ctrl Pts',(199.88050684786,11.0984758947224,30.6746235145448));
#72221=CARTESIAN_POINT('Ctrl Pts',(199.883784010307,11.0501168424284,30.6766832048623));
#72222=CARTESIAN_POINT('Ctrl Pts',(199.886957958635,11.00328085683,30.6786780253038));
#72223=CARTESIAN_POINT('Ctrl Pts',(199.890131906963,10.9562492181484,30.6778754238886));
#72224=CARTESIAN_POINT('Ctrl Pts',(199.893305855292,10.909382364626,30.6742587051665));
#72225=CARTESIAN_POINT('Ctrl Pts',(199.896476678598,10.8625616555079,30.6706455474116));
#72226=CARTESIAN_POINT('Ctrl Pts',(199.899647501904,10.8159059631852,30.6642237993453));
#72227=CARTESIAN_POINT('Ctrl Pts',(199.90281832521,10.7697750735935,30.6550288073295));
#72228=CARTESIAN_POINT('Ctrl Pts',(199.905987418042,10.7236693598957,30.6458388334729));
#72229=CARTESIAN_POINT('Ctrl Pts',(199.909156510874,10.6780884267301,30.6338787226884));
#72230=CARTESIAN_POINT('Ctrl Pts',(199.912325603706,10.6333835740681,30.6192352115337));
#72231=CARTESIAN_POINT('Ctrl Pts',(199.915494357613,10.5886835024526,30.6045932664576));
#72232=CARTESIAN_POINT('Ctrl Pts',(199.91866311152,10.5448598534815,30.5872686661981));
#72233=CARTESIAN_POINT('Ctrl Pts',(199.921831865428,10.5022478017002,30.5673976820228));
#72234=CARTESIAN_POINT('Ctrl Pts',(199.925003805676,10.4595929013577,30.5475067165736));
#72235=CARTESIAN_POINT('Ctrl Pts',(199.928175745925,10.4181525336127,30.5250644958841));
#72236=CARTESIAN_POINT('Ctrl Pts',(199.931347686174,10.3782391096656,30.5002541965673));
#72237=CARTESIAN_POINT('Ctrl Pts',(199.934521571235,10.3383012135965,30.4754286853091));
#72238=CARTESIAN_POINT('Ctrl Pts',(199.937695456295,10.2998925788117,30.4482325280295));
#72239=CARTESIAN_POINT('Ctrl Pts',(199.940869341356,10.2632953143319,30.4188913257914));
#72240=CARTESIAN_POINT('Ctrl Pts',(199.944048841634,10.226633302209,30.3894982132885));
#72241=CARTESIAN_POINT('Ctrl Pts',(199.947228341911,10.1917894624995,30.3579528618704));
#72242=CARTESIAN_POINT('Ctrl Pts',(199.950407842189,10.1590101570364,30.3245187363136));
#72243=CARTESIAN_POINT('Ctrl Pts',(199.951140035359,10.1514615545856,30.316819338216));
#72244=CARTESIAN_POINT('Ctrl Pts',(199.951872228529,10.1440222683806,30.3090199139201));
#72245=CARTESIAN_POINT('Ctrl Pts',(199.9526044217,10.1366949965981,30.3011239190046));
#72246=CARTESIAN_POINT('Ctrl Pts',(199.953760862746,10.1251221519025,30.2886528212227));
#72247=CARTESIAN_POINT('Ctrl Pts',(199.954917303793,10.1138091790481,30.275919676137));
#72248=CARTESIAN_POINT('Ctrl Pts',(199.956073744839,10.1027690874833,30.2629362700282));
#72249=CARTESIAN_POINT('Origin',(197.762132885264,11.,29.5));
#72250=CARTESIAN_POINT('',(200.554352848915,10.1027690892854,30.2629362721474));
#72251=CARTESIAN_POINT('',(200.456078305605,10.1027690874833,30.2629362700282));
#72252=CARTESIAN_POINT('',(197.762132885264,10.1027690874833,30.2629362700282));
#72253=CARTESIAN_POINT('Ctrl Pts',(200.554352848915,10.1027690892854,30.2629362721474));
#72254=CARTESIAN_POINT('Ctrl Pts',(200.554059484652,10.1058259895353,30.2665312583807));
#72255=CARTESIAN_POINT('Ctrl Pts',(200.553766388138,10.1089048112609,30.2701082428271));
#72256=CARTESIAN_POINT('Ctrl Pts',(200.550536613393,10.1430933772254,30.3093489769809));
#72257=CARTESIAN_POINT('Ctrl Pts',(200.547622714416,10.1763032051018,30.3431240866796));
#72258=CARTESIAN_POINT('Ctrl Pts',(200.541663360381,10.2470316592398,30.4068780928422));
#72259=CARTESIAN_POINT('Ctrl Pts',(200.538622129452,10.284528158526,30.4367435503193));
#72260=CARTESIAN_POINT('Ctrl Pts',(200.534546714256,10.3355883625495,30.4725542788059));
#72261=CARTESIAN_POINT('Ctrl Pts',(200.533593209763,10.3475928104203,30.4806474792247));
#72262=CARTESIAN_POINT('Ctrl Pts',(200.531991325723,10.3678328268368,30.4937568255723));
#72263=CARTESIAN_POINT('Ctrl Pts',(200.531347530803,10.3759864869471,30.4988969363709));
#72264=CARTESIAN_POINT('Ctrl Pts',(200.530071145571,10.3921830518015,30.508831641037));
#72265=CARTESIAN_POINT('Ctrl Pts',(200.529438807578,10.4002218725936,30.5136315463267));
#72266=CARTESIAN_POINT('Ctrl Pts',(200.528030316431,10.4181551439961,30.5240513141878));
#72267=CARTESIAN_POINT('Ctrl Pts',(200.52725259088,10.4280754301327,30.5296245924175));
#72268=CARTESIAN_POINT('Ctrl Pts',(200.524500533615,10.4632316690618,30.5487107465772));
#72269=CARTESIAN_POINT('Ctrl Pts',(200.522500074167,10.4888762817245,30.5614456076251));
#72270=CARTESIAN_POINT('Ctrl Pts',(200.51362607943,10.6029782446479,30.6130134453149));
#72271=CARTESIAN_POINT('Ctrl Pts',(200.506454714688,10.6955531740712,30.6418111902866));
#72272=CARTESIAN_POINT('Ctrl Pts',(200.497762726127,10.8133827237603,30.663101814847));
#72273=CARTESIAN_POINT('Ctrl Pts',(200.496094212026,10.836299920532,30.6665480040363));
#72274=CARTESIAN_POINT('Ctrl Pts',(200.49333594951,10.8748854424783,30.6711907070014));
#72275=CARTESIAN_POINT('Ctrl Pts',(200.492233486018,10.8905026494745,30.6727539009854));
#72276=CARTESIAN_POINT('Ctrl Pts',(200.490670876236,10.9129802633747,30.67455081439));
#72277=CARTESIAN_POINT('Ctrl Pts',(200.490198725757,10.9198180654875,30.675037409287));
#72278=CARTESIAN_POINT('Ctrl Pts',(200.489375793352,10.9318237647191,30.6757864739942));
#72279=CARTESIAN_POINT('Ctrl Pts',(200.489023685301,10.9369896891018,30.6760746301657));
#72280=CARTESIAN_POINT('Ctrl Pts',(200.488250947651,10.9483919839721,30.6766353028671));
#72281=CARTESIAN_POINT('Ctrl Pts',(200.487831147444,10.9546288206082,30.6768922991092));
#72282=CARTESIAN_POINT('Ctrl Pts',(200.486614880884,10.972811447002,30.6774967765295));
#72283=CARTESIAN_POINT('Ctrl Pts',(200.485825096764,10.9847612236144,30.6777120540833));
#72284=CARTESIAN_POINT('Ctrl Pts',(200.480719847098,11.0627675401348,30.6779297803596));
#72285=CARTESIAN_POINT('Ctrl Pts',(200.476634144649,11.1287292116464,30.6725567207702));
#72286=CARTESIAN_POINT('Ctrl Pts',(200.469192564894,11.2472661142624,30.6527714160568));
#72287=CARTESIAN_POINT('Ctrl Pts',(200.465847611633,11.2999541125762,30.6401971514624));
#72288=CARTESIAN_POINT('Ctrl Pts',(200.460322517995,11.3830554103551,30.6142040462825));
#72289=CARTESIAN_POINT('Ctrl Pts',(200.458201079678,11.4140927250099,30.6030453409429));
#72290=CARTESIAN_POINT('Ctrl Pts',(200.455191934823,11.4565635036614,30.5857307253838));
#72291=CARTESIAN_POINT('Ctrl Pts',(200.454339602688,11.4684266073093,30.5806655047578));
#72292=CARTESIAN_POINT('Ctrl Pts',(200.452858523142,11.4887374945339,30.5715960382333));
#72293=CARTESIAN_POINT('Ctrl Pts',(200.452232903481,11.4972253560091,30.5676841033738));
#72294=CARTESIAN_POINT('Ctrl Pts',(200.450941877531,11.5145474960536,30.5594492222673));
#72295=CARTESIAN_POINT('Ctrl Pts',(200.450276154236,11.5233759557368,30.5551158131519));
#72296=CARTESIAN_POINT('Ctrl Pts',(200.448554912339,11.5459297889911,30.5436926553971));
#72297=CARTESIAN_POINT('Ctrl Pts',(200.447493967628,11.5595714393206,30.5364426944096));
#72298=CARTESIAN_POINT('Ctrl Pts',(200.442242538002,11.6257974752286,30.499557767425));
#72299=CARTESIAN_POINT('Ctrl Pts',(200.437923038594,11.6761853521179,30.4661830165368));
#72300=CARTESIAN_POINT('Ctrl Pts',(200.42883944463,11.7745687285331,30.3895403135794));
#72301=CARTESIAN_POINT('Ctrl Pts',(200.424079664168,11.8220201767396,30.3458850447106));
#72302=CARTESIAN_POINT('Ctrl Pts',(200.417318014235,11.8854544436937,30.2771210679906));
#72303=CARTESIAN_POINT('Ctrl Pts',(200.415234360185,11.9044398138961,30.2549408238497));
#72304=CARTESIAN_POINT('Ctrl Pts',(200.412603185226,11.9278875828418,30.2253912902484));
#72305=CARTESIAN_POINT('Ctrl Pts',(200.412012102161,11.9331195537026,30.2186485924263));
#72306=CARTESIAN_POINT('Ctrl Pts',(200.411051445604,11.9415712626843,30.2075085220035));
#72307=CARTESIAN_POINT('Ctrl Pts',(200.410679063302,11.9448345036043,30.2031447331425));
#72308=CARTESIAN_POINT('Ctrl Pts',(200.409932988339,11.95134854785,30.1943065511501));
#72309=CARTESIAN_POINT('Ctrl Pts',(200.409559361796,11.9545983451369,30.1898316092028));
#72310=CARTESIAN_POINT('Ctrl Pts',(200.408588722835,11.9630042886497,30.1780835358305));
#72311=CARTESIAN_POINT('Ctrl Pts',(200.407994964603,11.9681096962672,30.1707743057543));
#72312=CARTESIAN_POINT('Ctrl Pts',(200.405379478221,11.9904053376091,30.1380695258264));
#72313=CARTESIAN_POINT('Ctrl Pts',(200.403408726568,12.006684276264,30.1120641797077));
#72314=CARTESIAN_POINT('Ctrl Pts',(200.394470734778,12.0768877995601,29.9895207559541));
#72315=CARTESIAN_POINT('Ctrl Pts',(200.387850735577,12.1180639048314,29.8863326711703));
#72316=CARTESIAN_POINT('Ctrl Pts',(200.379297611381,12.1495271515814,29.7572534919568));
#72317=CARTESIAN_POINT('Ctrl Pts',(200.377846476518,12.1541901879936,29.7354505049964));
#72318=CARTESIAN_POINT('Ctrl Pts',(200.375637595656,12.1602622130009,29.7025144725542));
#72319=CARTESIAN_POINT('Ctrl Pts',(200.37489421003,12.1621356091211,29.691471476532));
#72320=CARTESIAN_POINT('Ctrl Pts',(200.373594121891,12.1651162827878,29.6722420502311));
#72321=CARTESIAN_POINT('Ctrl Pts',(200.373039692123,12.1662954775799,29.6640674537552));
#72322=CARTESIAN_POINT('Ctrl Pts',(200.371781597606,12.168763960336,29.6455810895301));
#72323=CARTESIAN_POINT('Ctrl Pts',(200.371076423746,12.1700029250846,29.6352634171583));
#72324=CARTESIAN_POINT('Ctrl Pts',(200.369159853748,12.172980790786,29.6073488522191));
#72325=CARTESIAN_POINT('Ctrl Pts',(200.367940642929,12.1744601372346,29.5897275853987));
#72326=CARTESIAN_POINT('Ctrl Pts',(200.360731285625,12.180797446691,29.4863740249201));
#72327=CARTESIAN_POINT('Ctrl Pts',(200.354469390862,12.176663075435,29.4003635248952));
#72328=CARTESIAN_POINT('Ctrl Pts',(200.345119803961,12.1566965847986,29.2744234408662));
#72329=CARTESIAN_POINT('Ctrl Pts',(200.342068171672,12.1479907756377,29.233636905313));
#72330=CARTESIAN_POINT('Ctrl Pts',(200.337418516003,12.1311286470107,29.1710982197427));
#72331=CARTESIAN_POINT('Ctrl Pts',(200.335780275352,12.124461550279,29.148980368489));
#72332=CARTESIAN_POINT('Ctrl Pts',(200.33362271666,12.1146452335006,29.1195745401375));
#72333=CARTESIAN_POINT('Ctrl Pts',(200.333076321423,12.1120671593705,29.1121028891281));
#72334=CARTESIAN_POINT('Ctrl Pts',(200.3321688592,12.1076271853072,29.0996433903741));
#72335=CARTESIAN_POINT('Ctrl Pts',(200.331805548495,12.1058063585852,29.0946412721472));
#72336=CARTESIAN_POINT('Ctrl Pts',(200.331056641145,12.1019617983021,29.0842983368615));
#72337=CARTESIAN_POINT('Ctrl Pts',(200.330671332666,12.0999330360039,29.0789596250113));
#72338=CARTESIAN_POINT('Ctrl Pts',(200.329633725258,12.0943343148585,29.0645432134544));
#72339=CARTESIAN_POINT('Ctrl Pts',(200.328985546667,12.0906902022097,29.0554945404971));
#72340=CARTESIAN_POINT('Ctrl Pts',(200.325227415945,12.0687286541792,29.0028587695539));
#72341=CARTESIAN_POINT('Ctrl Pts',(200.322241596036,12.0479103028067,28.9603562586247));
#72342=CARTESIAN_POINT('Ctrl Pts',(200.314897515568,11.989840621697,28.8579125337905));
#72343=CARTESIAN_POINT('Ctrl Pts',(200.310592231576,11.9496600333001,28.7998524987611));
#72344=CARTESIAN_POINT('Ctrl Pts',(200.30374911846,11.8802257868761,28.7165857522622));
#72345=CARTESIAN_POINT('Ctrl Pts',(200.301318596926,11.8545285084103,28.6886333006805));
#72346=CARTESIAN_POINT('Ctrl Pts',(200.29794784292,11.8179118032228,28.6524753631909));
#72347=CARTESIAN_POINT('Ctrl Pts',(200.297055966734,11.808132521011,28.6431455596391));
#72348=CARTESIAN_POINT('Ctrl Pts',(200.295528130128,11.7912434285482,28.6275790694907));
#72349=CARTESIAN_POINT('Ctrl Pts',(200.294895849588,11.7842149666841,28.6212558276166));
#72350=CARTESIAN_POINT('Ctrl Pts',(200.293686178161,11.7706993722206,28.609387652039));
#72351=CARTESIAN_POINT('Ctrl Pts',(200.293109475068,11.7642265823042,28.603827248224));
#72352=CARTESIAN_POINT('Ctrl Pts',(200.291750832384,11.7489128106895,28.5909586217059));
#72353=CARTESIAN_POINT('Ctrl Pts',(200.290966653219,11.7400244840577,28.5837083584018));
#72354=CARTESIAN_POINT('Ctrl Pts',(200.288154721767,11.7079870230235,28.5583454217735));
#72355=CARTESIAN_POINT('Ctrl Pts',(200.286099247846,11.6842691113827,28.5409721088688));
#72356=CARTESIAN_POINT('Ctrl Pts',(200.277227087328,11.5806778014099,28.4708919783731));
#72357=CARTESIAN_POINT('Ctrl Pts',(200.270123378105,11.4951940370528,28.4271399972699));
#72358=CARTESIAN_POINT('Ctrl Pts',(200.261503013554,11.3836905564679,28.3862629228289));
#72359=CARTESIAN_POINT('Ctrl Pts',(200.259839497397,11.3617705403745,28.3789509744218));
#72360=CARTESIAN_POINT('Ctrl Pts',(200.257088480645,11.3246534169226,28.3677719003788));
#72361=CARTESIAN_POINT('Ctrl Pts',(200.255988343416,11.3095688863985,28.3635548969176));
#72362=CARTESIAN_POINT('Ctrl Pts',(200.254428391087,11.2877720155653,28.3579276543517));
#72363=CARTESIAN_POINT('Ctrl Pts',(200.253956625392,11.2811251306517,28.3562733533575));
#72364=CARTESIAN_POINT('Ctrl Pts',(200.253134107645,11.2694329730628,28.3534714568621));
#72365=CARTESIAN_POINT('Ctrl Pts',(200.252782034253,11.2643940425422,28.352298984503));
#72366=CARTESIAN_POINT('Ctrl Pts',(200.252009065786,11.2532546789339,28.349784306714));
#72367=CARTESIAN_POINT('Ctrl Pts',(200.251589003871,11.2471511015586,28.348457377758));
#72368=CARTESIAN_POINT('Ctrl Pts',(200.250346021303,11.2289519220059,28.3446522099588));
#72369=CARTESIAN_POINT('Ctrl Pts',(200.249530397407,11.216827190396,28.3423154587035));
#72370=CARTESIAN_POINT('Ctrl Pts',(200.24474517768,11.1447748205305,28.3296008657922));
#72371=CARTESIAN_POINT('Ctrl Pts',(200.240967562845,11.0841462033348,28.3236858254642));
#72372=CARTESIAN_POINT('Ctrl Pts',(200.233641070254,10.9659126413207,28.3213436918574));
#72373=CARTESIAN_POINT('Ctrl Pts',(200.230100217233,10.9084959559439,28.3244068691112));
#72374=CARTESIAN_POINT('Ctrl Pts',(200.224299513255,10.8176931991688,28.3359454746302));
#72375=CARTESIAN_POINT('Ctrl Pts',(200.222107010803,10.7840585707041,28.3417134707805));
#72376=CARTESIAN_POINT('Ctrl Pts',(200.219014367408,10.7379703431451,28.3516943787717));
#72377=CARTESIAN_POINT('Ctrl Pts',(200.218152394453,10.7252641177713,28.3546679460517));
#72378=CARTESIAN_POINT('Ctrl Pts',(200.216659989514,10.7035223417987,28.3601386570273));
#72379=CARTESIAN_POINT('Ctrl Pts',(200.216032818041,10.6944622083917,28.3625337225281));
#72380=CARTESIAN_POINT('Ctrl Pts',(200.214743513993,10.6759996462505,28.3676508340052));
#72381=CARTESIAN_POINT('Ctrl Pts',(200.214081118694,10.6666006641002,28.3703824824861));
#72382=CARTESIAN_POINT('Ctrl Pts',(200.212379103596,10.6426770114188,28.3776600529432));
#72383=CARTESIAN_POINT('Ctrl Pts',(200.211334291144,10.6282048007064,28.3823708273934));
#72384=CARTESIAN_POINT('Ctrl Pts',(200.206574812341,10.5632664386439,28.4049094352874));
#72385=CARTESIAN_POINT('Ctrl Pts',(200.202760872884,10.5139663428851,28.4258820225373));
#72386=CARTESIAN_POINT('Ctrl Pts',(200.193779476257,10.4036238081094,28.4819778498239));
#72387=CARTESIAN_POINT('Ctrl Pts',(200.188575777683,10.3439576472968,28.5193666753786));
#72388=CARTESIAN_POINT('Ctrl Pts',(200.181293474657,10.2637880328199,28.5802122679365));
#72389=CARTESIAN_POINT('Ctrl Pts',(200.179122409607,10.2403118078168,28.5995047399878));
#72390=CARTESIAN_POINT('Ctrl Pts',(200.176400085364,10.2111494432358,28.6254232593247));
#72391=CARTESIAN_POINT('Ctrl Pts',(200.175801625845,10.2047560700298,28.6312326093909));
#72392=CARTESIAN_POINT('Ctrl Pts',(200.174832111417,10.1944187612633,28.6408353710791));
#72393=CARTESIAN_POINT('Ctrl Pts',(200.174458152519,10.1904364411046,28.6445867436218));
#72394=CARTESIAN_POINT('Ctrl Pts',(200.173712081496,10.1824987047159,28.6521692305461));
#72395=CARTESIAN_POINT('Ctrl Pts',(200.173340003177,10.178543732005,28.6560006017263));
#72396=CARTESIAN_POINT('Ctrl Pts',(200.172378268231,10.1683357528672,28.6660292905499));
#72397=CARTESIAN_POINT('Ctrl Pts',(200.171791756353,10.1621249731353,28.6722693585008));
#72398=CARTESIAN_POINT('Ctrl Pts',(200.169251112088,10.1353193300328,28.6998123232013));
#72399=CARTESIAN_POINT('Ctrl Pts',(200.167344514041,10.115460908333,28.7218201460967));
#72400=CARTESIAN_POINT('Ctrl Pts',(200.158495843839,10.0258960167594,28.8289440453364));
#72401=CARTESIAN_POINT('Ctrl Pts',(200.151911736535,9.96750968453955,28.9227993651366));
#72402=CARTESIAN_POINT('Ctrl Pts',(200.143335232086,9.91350019737522,29.0448478671892));
#72403=CARTESIAN_POINT('Ctrl Pts',(200.141810497993,9.90465136893458,29.0665757907962));
#72404=CARTESIAN_POINT('Ctrl Pts',(200.139512529176,9.89247036635523,29.0992464166315));
#72405=CARTESIAN_POINT('Ctrl Pts',(200.138755506463,9.8886389324939,29.1099975812545));
#72406=CARTESIAN_POINT('Ctrl Pts',(200.13738194268,9.88201630167086,29.1294715159846));
#72407=CARTESIAN_POINT('Ctrl Pts',(200.136767261903,9.87916941976998,29.1381744762926));
#72408=CARTESIAN_POINT('Ctrl Pts',(200.135436551814,9.87325844172585,29.1569839081087));
#72409=CARTESIAN_POINT('Ctrl Pts',(200.134719493643,9.87022824179993,29.1671001046275));
#72410=CARTESIAN_POINT('Ctrl Pts',(200.132736268906,9.86227345488839,29.1950172635262));
#72411=CARTESIAN_POINT('Ctrl Pts',(200.131461340337,9.85763110275377,29.2128947970965));
#72412=CARTESIAN_POINT('Ctrl Pts',(200.125622547261,9.83849657413298,29.2944156284368));
#72413=CARTESIAN_POINT('Ctrl Pts',(200.120913255013,9.82889197068187,29.3590786040561));
#72414=CARTESIAN_POINT('Ctrl Pts',(200.112060591604,9.82110196841747,29.4798577113642));
#72415=CARTESIAN_POINT('Ctrl Pts',(200.107947611176,9.82147055730096,29.5357060292933));
#72416=CARTESIAN_POINT('Ctrl Pts',(200.101963292659,9.82790357899108,29.6184235878555));
#72417=CARTESIAN_POINT('Ctrl Pts',(200.100026127748,9.83094958728436,29.6454494678802));
#72418=CARTESIAN_POINT('Ctrl Pts',(200.097548956439,9.8361499669536,29.6806040431663));
#72419=CARTESIAN_POINT('Ctrl Pts',(200.096971191821,9.83745907640505,29.6888473740811));
#72420=CARTESIAN_POINT('Ctrl Pts',(200.096026483028,9.83976098287463,29.7024098591719));
#72421=CARTESIAN_POINT('Ctrl Pts',(200.095656900399,9.84070297915671,29.7077372121524));
#72422=CARTESIAN_POINT('Ctrl Pts',(200.094910526453,9.84269063863739,29.7185433854436));
#72423=CARTESIAN_POINT('Ctrl Pts',(200.09453386237,9.8437385715646,29.7240216095159));
#72424=CARTESIAN_POINT('Ctrl Pts',(200.093545795538,9.84660512033182,29.7384506948196));
#72425=CARTESIAN_POINT('Ctrl Pts',(200.092937864968,9.84848904711843,29.7473883996157));
#72426=CARTESIAN_POINT('Ctrl Pts',(200.09012203995,9.85776962934379,29.7890118634204));
#72427=CARTESIAN_POINT('Ctrl Pts',(200.087975361377,9.86645583806898,29.8213971653031));
#72428=CARTESIAN_POINT('Ctrl Pts',(200.080242527498,9.90323524412609,29.9383316047272));
#72429=CARTESIAN_POINT('Ctrl Pts',(200.074856723675,9.93950879472617,30.0199874612024));
#72430=CARTESIAN_POINT('Ctrl Pts',(200.066994980489,10.0024382620207,30.1270559970883));
#72431=CARTESIAN_POINT('Ctrl Pts',(200.064739712808,10.0215791908949,30.1565219082427));
#72432=CARTESIAN_POINT('Ctrl Pts',(200.061573506326,10.0496719137213,30.19580545931));
#72433=CARTESIAN_POINT('Ctrl Pts',(200.060703296898,10.0575162334201,30.2063943911513));
#72434=CARTESIAN_POINT('Ctrl Pts',(200.059201175609,10.0712537717106,30.2243022462663));
#72435=CARTESIAN_POINT('Ctrl Pts',(200.058572638595,10.0770600415176,30.2316864936288));
#72436=CARTESIAN_POINT('Ctrl Pts',(200.057284588891,10.0890719337397,30.2465923858502));
#72437=CARTESIAN_POINT('Ctrl Pts',(200.056624858235,10.0952838682443,30.2541079787803));
#72438=CARTESIAN_POINT('Ctrl Pts',(200.055920004199,10.101981501335,30.2620093230676));
#72439=CARTESIAN_POINT('Ctrl Pts',(200.055878603811,10.1023751159753,30.2624729503126));
#72440=CARTESIAN_POINT('Ctrl Pts',(200.055837189155,10.1027690874889,30.2629362700347));
#72441=CARTESIAN_POINT('',(200.012132885299,9.82225044682022,29.498974093169));
#72442=CARTESIAN_POINT('Ctrl Pts',(199.956073744839,10.1027690874833,30.2629362700282));
#72443=CARTESIAN_POINT('Ctrl Pts',(199.959213054861,10.0727993192846,30.2276911210882));
#72444=CARTESIAN_POINT('Ctrl Pts',(199.962352364883,10.0448431166944,30.1905990782524));
#72445=CARTESIAN_POINT('Ctrl Pts',(199.965491674906,10.0191369550365,30.1519223493062));
#72446=CARTESIAN_POINT('Ctrl Pts',(199.968626810549,9.99346497517818,30.1132970492826));
#72447=CARTESIAN_POINT('Ctrl Pts',(199.971761946192,9.97003743285672,30.0730917033196));
#72448=CARTESIAN_POINT('Ctrl Pts',(199.974897081835,9.94905028793591,30.0316011335695));
#72449=CARTESIAN_POINT('Ctrl Pts',(199.978030461699,9.92807489650514,29.9901337999004));
#72450=CARTESIAN_POINT('Ctrl Pts',(199.981163841563,9.90953747036862,29.9473831675551));
#72451=CARTESIAN_POINT('Ctrl Pts',(199.984297221427,9.89358899406756,29.9036703462623));
#72452=CARTESIAN_POINT('Ctrl Pts',(199.987429333019,9.87764697310161,29.859975218253));
#72453=CARTESIAN_POINT('Ctrl Pts',(199.99056144461,9.86429201741278,29.8153192114746));
#72454=CARTESIAN_POINT('Ctrl Pts',(199.993693556202,9.85362646241936,29.7700421723266));
#72455=CARTESIAN_POINT('Ctrl Pts',(199.996828401406,9.84295159885049,29.7247256167412));
#72456=CARTESIAN_POINT('Ctrl Pts',(199.99996324661,9.83497095675816,29.6787875038758));
#72457=CARTESIAN_POINT('Ctrl Pts',(200.003098091814,9.82973604293946,29.63257953577));
#72458=CARTESIAN_POINT('Ctrl Pts',(200.006109689631,9.82470694134145,29.5881882479113));
#72459=CARTESIAN_POINT('Ctrl Pts',(200.009121287447,9.82221161931003,29.5435484194516));
#72460=CARTESIAN_POINT('Ctrl Pts',(200.012132885264,9.82225044681977,29.498974093686));
#72461=CARTESIAN_POINT('Ctrl Pts',(200.012132885299,9.82225044682022,29.498974093169));
#72462=CARTESIAN_POINT('Ctrl Pts',(200.016268643754,9.82230376777885,29.4377611902899));
#72463=CARTESIAN_POINT('Ctrl Pts',(200.020404402209,9.82713317339624,29.3767546330056));
#72464=CARTESIAN_POINT('Ctrl Pts',(200.024540160664,9.83662031468082,29.3165803437833));
#72465=CARTESIAN_POINT('Ctrl Pts',(200.026778880587,9.84175578195748,29.2840075082022));
#72466=CARTESIAN_POINT('Ctrl Pts',(200.029017600511,9.84825520947371,29.2516780823027));
#72467=CARTESIAN_POINT('Ctrl Pts',(200.031256320434,9.85609415083642,29.2196886182308));
#72468=CARTESIAN_POINT('Ctrl Pts',(200.034533482881,9.86756922817513,29.1728606656714));
#72469=CARTESIAN_POINT('Ctrl Pts',(200.037810645328,9.88195041103549,29.1266328620673));
#72470=CARTESIAN_POINT('Ctrl Pts',(200.041087807776,9.89915432543894,29.0813905599485));
#72471=CARTESIAN_POINT('Ctrl Pts',(200.044261760322,9.91581642529061,29.0375731043542));
#72472=CARTESIAN_POINT('Ctrl Pts',(200.047435712868,9.93512587009885,28.9946805581051));
#72473=CARTESIAN_POINT('Ctrl Pts',(200.050609665414,9.95695566619216,28.953050660288));
#72474=CARTESIAN_POINT('Ctrl Pts',(200.053780493005,9.97876396948248,28.9114617497156));
#72475=CARTESIAN_POINT('Ctrl Pts',(200.056951320596,10.0030874548671,28.8711335179084));
#72476=CARTESIAN_POINT('Ctrl Pts',(200.060122148187,10.0297515738821,28.8323825540658));
#72477=CARTESIAN_POINT('Ctrl Pts',(200.063291245362,10.0564011414834,28.7936527377924));
#72478=CARTESIAN_POINT('Ctrl Pts',(200.066460342537,10.0853884970476,28.7564989422275));
#72479=CARTESIAN_POINT('Ctrl Pts',(200.069629439712,10.1164952293694,28.7212096670008));
#72480=CARTESIAN_POINT('Ctrl Pts',(200.072798198011,10.1475986354081,28.685924165302));
#72481=CARTESIAN_POINT('Ctrl Pts',(200.07596695631,10.1808205985382,28.6525032040694));
#72482=CARTESIAN_POINT('Ctrl Pts',(200.079135714609,10.2159035662049,28.6212009074824));
#72483=CARTESIAN_POINT('Ctrl Pts',(200.082307659289,10.2510218119494,28.5898671345144));
#72484=CARTESIAN_POINT('Ctrl Pts',(200.085479603969,10.2880043785701,28.5606566467084));
#72485=CARTESIAN_POINT('Ctrl Pts',(200.088651548649,10.3265596090397,28.5337841326478));
#72486=CARTESIAN_POINT('Ctrl Pts',(200.091825438169,10.3651384791857,28.506895142028));
#72487=CARTESIAN_POINT('Ctrl Pts',(200.094999327689,10.4052914568156,28.4823472681669));
#72488=CARTESIAN_POINT('Ctrl Pts',(200.098173217209,10.4466998741197,28.4603106073443));
#72489=CARTESIAN_POINT('Ctrl Pts',(200.101352721942,10.4881815507756,28.4382349594849));
#72490=CARTESIAN_POINT('Ctrl Pts',(200.104532226675,10.5309225903706,28.4186796147557));
#72491=CARTESIAN_POINT('Ctrl Pts',(200.107711731408,10.5745836545359,28.4017668756079));
#72492=CARTESIAN_POINT('Ctrl Pts',(200.108443893994,10.5846377353961,28.3978722832472));
#72493=CARTESIAN_POINT('Ctrl Pts',(200.109176056581,10.5947405420219,28.3941176101592));
#72494=CARTESIAN_POINT('Ctrl Pts',(200.109908219168,10.6048878347393,28.390503970551));
#72495=CARTESIAN_POINT('Ctrl Pts',(200.113185381615,10.6503071544851,28.3743293062953));
#72496=CARTESIAN_POINT('Ctrl Pts',(200.116462544063,10.6968237837432,28.3609117308587));
#72497=CARTESIAN_POINT('Ctrl Pts',(200.11973970651,10.744070042996,28.3503935805642));
#72498=CARTESIAN_POINT('Ctrl Pts',(200.122913658414,10.7898283344861,28.3402066875758));
#72499=CARTESIAN_POINT('Ctrl Pts',(200.126087610318,10.8362703860954,28.3327394191828));
#72500=CARTESIAN_POINT('Ctrl Pts',(200.129261562222,10.8830442887541,28.3280714936025));
#72501=CARTESIAN_POINT('Ctrl Pts',(200.132432389157,10.9297721393517,28.3234081639098));
#72502=CARTESIAN_POINT('Ctrl Pts',(200.135603216091,10.9768306425947,28.3215387766397));
#72503=CARTESIAN_POINT('Ctrl Pts',(200.138774043026,11.0238593946484,28.3224917020305));
#72504=CARTESIAN_POINT('Ctrl Pts',(200.141943139531,11.0708624814957,28.3234441073772));
#72505=CARTESIAN_POINT('Ctrl Pts',(200.145112236037,11.1178352935069,28.3272157628039));
#72506=CARTESIAN_POINT('Ctrl Pts',(200.148281332542,11.1644167584438,28.3337829567174));
#72507=CARTESIAN_POINT('Ctrl Pts',(200.15145009016,11.2109932421918,28.340349448368));
#72508=CARTESIAN_POINT('Ctrl Pts',(200.154618847778,11.2571779111989,28.3497108050288));
#72509=CARTESIAN_POINT('Ctrl Pts',(200.157787605396,11.3026168713695,28.3617917186813));
#72510=CARTESIAN_POINT('Ctrl Pts',(200.160959549383,11.3481015230396,28.3738847803903));
#72511=CARTESIAN_POINT('Ctrl Pts',(200.164131493369,11.3928384313099,28.3887027101717));
#72512=CARTESIAN_POINT('Ctrl Pts',(200.167303437356,11.4364878766585,28.4061200266802));
#72513=CARTESIAN_POINT('Ctrl Pts',(200.170477326175,11.4801640850382,28.4235480223663));
#72514=CARTESIAN_POINT('Ctrl Pts',(200.173651214994,11.5227509997531,28.4435783392123));
#72515=CARTESIAN_POINT('Ctrl Pts',(200.176825103812,11.5639312842824,28.4660384102359));
#72516=CARTESIAN_POINT('Ctrl Pts',(200.18000460784,11.6051844245113,28.4885382173663));
#72517=CARTESIAN_POINT('Ctrl Pts',(200.183184111867,11.6450255011556,28.5134760551328));
#72518=CARTESIAN_POINT('Ctrl Pts',(200.186363615895,11.6831657218461,28.5406358048194));
#72519=CARTESIAN_POINT('Ctrl Pts',(200.18709578323,11.691948545686,28.5468900763657));
#72520=CARTESIAN_POINT('Ctrl Pts',(200.187827950566,11.7006413193404,28.5532620047846));
#72521=CARTESIAN_POINT('Ctrl Pts',(200.188560117902,11.7092407801928,28.5597486622123));
#72522=CARTESIAN_POINT('Ctrl Pts',(200.191837280349,11.747731749119,28.5887827765331));
#72523=CARTESIAN_POINT('Ctrl Pts',(200.195114442797,11.7845237684032,28.6202498310047));
#72524=CARTESIAN_POINT('Ctrl Pts',(200.198391605244,11.8192957257391,28.6539210578878));
#72525=CARTESIAN_POINT('Ctrl Pts',(200.201565557752,11.852972585822,28.6865318535819));
#72526=CARTESIAN_POINT('Ctrl Pts',(200.20473951026,11.8847543092152,28.7212096153979));
#72527=CARTESIAN_POINT('Ctrl Pts',(200.207913462769,11.9143807522802,28.7577043026129));
#72528=CARTESIAN_POINT('Ctrl Pts',(200.211084290316,11.9439780261994,28.7941630584522));
#72529=CARTESIAN_POINT('Ctrl Pts',(200.214255117863,11.9714238706224,28.8324347683777));
#72530=CARTESIAN_POINT('Ctrl Pts',(200.21742594541,11.9964963515863,28.8722340533485));
#72531=CARTESIAN_POINT('Ctrl Pts',(200.220595042535,12.0215551496956,28.9120116185769));
#72532=CARTESIAN_POINT('Ctrl Pts',(200.22376413966,12.0442428539556,28.9533146369634));
#72533=CARTESIAN_POINT('Ctrl Pts',(200.226933236786,12.0643806578495,28.9958285235201));
#72534=CARTESIAN_POINT('Ctrl Pts',(200.230101995029,12.0845163083457,29.0383378639354));
#72535=CARTESIAN_POINT('Ctrl Pts',(200.233270753273,12.1021023636656,29.0820573115153));
#72536=CARTESIAN_POINT('Ctrl Pts',(200.236439511517,12.1170070553719,29.1266498952064));
#72537=CARTESIAN_POINT('Ctrl Pts',(200.239611456134,12.1319267346233,29.1712873193659));
#72538=CARTESIAN_POINT('Ctrl Pts',(200.242783400751,12.1441594956936,29.2167991018886));
#72539=CARTESIAN_POINT('Ctrl Pts',(200.245955345367,12.1536232681568,29.2628325113615));
#72540=CARTESIAN_POINT('Ctrl Pts',(200.249129234819,12.1630928432044,29.3088941455976));
#72541=CARTESIAN_POINT('Ctrl Pts',(200.252303124271,12.1697899720009,29.3554774919692));
#72542=CARTESIAN_POINT('Ctrl Pts',(200.255477013723,12.173684218576,29.4022226121963));
#72543=CARTESIAN_POINT('Ctrl Pts',(200.258656518381,12.177585354805,29.4490504333251));
#72544=CARTESIAN_POINT('Ctrl Pts',(200.26183602304,12.1786737082398,29.4960400432032));
#72545=CARTESIAN_POINT('Ctrl Pts',(200.265015527699,12.1769709150544,29.5428313858755));
#72546=CARTESIAN_POINT('Ctrl Pts',(200.265747690678,12.1765788029913,29.5536062997454));
#72547=CARTESIAN_POINT('Ctrl Pts',(200.266479853657,12.1760389015659,29.5643707276121));
#72548=CARTESIAN_POINT('Ctrl Pts',(200.267212016636,12.1753518613014,29.5751203343657));
#72549=CARTESIAN_POINT('Ctrl Pts',(200.270489179083,12.1722766681835,29.6232355881859));
#72550=CARTESIAN_POINT('Ctrl Pts',(200.27376634153,12.1662351420622,29.671270243921));
#72551=CARTESIAN_POINT('Ctrl Pts',(200.277043503978,12.1572417049752,29.7188302967281));
#72552=CARTESIAN_POINT('Ctrl Pts',(200.280217456315,12.1485315048796,29.7648925054809));
#72553=CARTESIAN_POINT('Ctrl Pts',(200.283391408652,12.1370526946772,29.8105089694688));
#72554=CARTESIAN_POINT('Ctrl Pts',(200.286565360989,12.1228709980971,29.8553248993983));
#72555=CARTESIAN_POINT('Ctrl Pts',(200.289736188364,12.1087032643188,29.9000967051325));
#72556=CARTESIAN_POINT('Ctrl Pts',(200.292907015739,12.0918380788874,29.944069008322));
#72557=CARTESIAN_POINT('Ctrl Pts',(200.296077843114,12.0723916949562,29.9868994917732));
#72558=CARTESIAN_POINT('Ctrl Pts',(200.299246940066,12.0529559235441,30.0297066012477));
#72559=CARTESIAN_POINT('Ctrl Pts',(200.302416037018,12.0309419740899,30.0713726192533));
#72560=CARTESIAN_POINT('Ctrl Pts',(200.30558513397,12.0065142128789,30.1115751808018));
#72561=CARTESIAN_POINT('Ctrl Pts',(200.30875389204,11.9820890638076,30.15177344336));
#72562=CARTESIAN_POINT('Ctrl Pts',(200.31192265011,11.9552509063891,30.1905080857414));
#72563=CARTESIAN_POINT('Ctrl Pts',(200.31509140818,11.9262086756078,30.2274837123461));
#72564=CARTESIAN_POINT('Ctrl Pts',(200.318263352624,11.8971372411461,30.2644965201297));
#72565=CARTESIAN_POINT('Ctrl Pts',(200.321435297068,11.8658576572764,30.2997463456538));
#72566=CARTESIAN_POINT('Ctrl Pts',(200.324607241512,11.83261935746,30.3329706285836));
#72567=CARTESIAN_POINT('Ctrl Pts',(200.327781130791,11.7993606780257,30.3662152825369));
#72568=CARTESIAN_POINT('Ctrl Pts',(200.33095502007,11.7641413096171,30.3974315531704));
#72569=CARTESIAN_POINT('Ctrl Pts',(200.334128909349,11.7272451060402,30.4263960374703));
#72570=CARTESIAN_POINT('Ctrl Pts',(200.337308413836,11.6902836261191,30.4554117654067));
#72571=CARTESIAN_POINT('Ctrl Pts',(200.340487918324,11.6516398527521,30.4821674469353));
#72572=CARTESIAN_POINT('Ctrl Pts',(200.343667422812,11.6116263804457,30.5064831013201));
#72573=CARTESIAN_POINT('Ctrl Pts',(200.344399586998,11.6024122304139,30.512082417618));
#72574=CARTESIAN_POINT('Ctrl Pts',(200.345131751184,11.5931255453682,30.5175525423206));
#72575=CARTESIAN_POINT('Ctrl Pts',(200.34586391537,11.5837703035305,30.5228916341509));
#72576=CARTESIAN_POINT('Ctrl Pts',(200.349141077817,11.5418962979124,30.5467893767402));
#72577=CARTESIAN_POINT('Ctrl Pts',(200.352418240265,11.4984579624634,30.5681655127757));
#72578=CARTESIAN_POINT('Ctrl Pts',(200.355695402712,11.4537922752884,30.5868153630625));
#72579=CARTESIAN_POINT('Ctrl Pts',(200.358869354999,11.410533278438,30.6048778594851));
#72580=CARTESIAN_POINT('Ctrl Pts',(200.362043307287,11.3661236547293,30.6203830237787));
#72581=CARTESIAN_POINT('Ctrl Pts',(200.365217259574,11.3208958508152,30.6331905909553));
#72582=CARTESIAN_POINT('Ctrl Pts',(200.368388086898,11.275712576633,30.6459855482441));
#72583=CARTESIAN_POINT('Ctrl Pts',(200.371558914222,11.2297132501836,30.656088014506));
#72584=CARTESIAN_POINT('Ctrl Pts',(200.374729741546,11.1832476961478,30.6634067836989));
#72585=CARTESIAN_POINT('Ctrl Pts',(200.377898838446,11.1368074998827,30.6707215588003));
#72586=CARTESIAN_POINT('Ctrl Pts',(200.381067935346,11.0899021292431,30.675255559896));
#72587=CARTESIAN_POINT('Ctrl Pts',(200.384237032245,11.0428912109895,30.6769687364241));
#72588=CARTESIAN_POINT('Ctrl Pts',(200.387405790262,10.995885319783,30.6786817297562));
#72589=CARTESIAN_POINT('Ctrl Pts',(200.390574548279,10.9487744596074,30.6775744794197));
#72590=CARTESIAN_POINT('Ctrl Pts',(200.393743306296,10.9019202494185,30.6736589900929));
#72591=CARTESIAN_POINT('Ctrl Pts',(200.396915250685,10.8550189245692,30.6697395635116));
#72592=CARTESIAN_POINT('Ctrl Pts',(200.400087195074,10.8083753201946,30.6630063121403));
#72593=CARTESIAN_POINT('Ctrl Pts',(200.403259139463,10.762345909839,30.6535231232748));
#72594=CARTESIAN_POINT('Ctrl Pts',(200.406433028687,10.7162882771791,30.6440341199216));
#72595=CARTESIAN_POINT('Ctrl Pts',(200.409606917911,10.6708461256432,30.6317919687924));
#72596=CARTESIAN_POINT('Ctrl Pts',(200.412780807134,10.6263621603328,30.6169108412353));
#72597=CARTESIAN_POINT('Ctrl Pts',(200.415960311566,10.581799494504,30.6020033861588));
#72598=CARTESIAN_POINT('Ctrl Pts',(200.419139815998,10.5381989107945,30.5844478528081));
#72599=CARTESIAN_POINT('Ctrl Pts',(200.422319320429,10.4958826599652,30.5644062992938));
#72600=CARTESIAN_POINT('Ctrl Pts',(200.423051484988,10.4861382297368,30.5597912042402));
#72601=CARTESIAN_POINT('Ctrl Pts',(200.423783649546,10.4764617932563,30.5550444706976));
#72602=CARTESIAN_POINT('Ctrl Pts',(200.424515814104,10.4668570764666,30.5501684082024));
#72603=CARTESIAN_POINT('Ctrl Pts',(200.427694743764,10.4251550864809,30.5289974029764));
#72604=CARTESIAN_POINT('Ctrl Pts',(200.430873673424,10.3846248526976,30.5052922646991));
#72605=CARTESIAN_POINT('Ctrl Pts',(200.434052603084,10.3455918892627,30.4792063557296));
#72606=CARTESIAN_POINT('Ctrl Pts',(200.437226952187,10.306615168875,30.4531580342472));
#72607=CARTESIAN_POINT('Ctrl Pts',(200.440401301291,10.2691319095204,30.4247360359438));
#72608=CARTESIAN_POINT('Ctrl Pts',(200.443575650394,10.233443060636,30.3941395423606));
#72609=CARTESIAN_POINT('Ctrl Pts',(200.446746459659,10.1977940097517,30.3635771680975));
#72610=CARTESIAN_POINT('Ctrl Pts',(200.449917268925,10.1639358250307,30.3308454645624));
#72611=CARTESIAN_POINT('Ctrl Pts',(200.45308807819,10.1321381353714,30.2961851834991));
#72612=CARTESIAN_POINT('Ctrl Pts',(200.454084820662,10.1221425458748,30.2852897396772));
#72613=CARTESIAN_POINT('Ctrl Pts',(200.455081563134,10.1123503133646,30.2742040159438));
#72614=CARTESIAN_POINT('Ctrl Pts',(200.456078305605,10.1027690874833,30.2629362700282));
#72615=CARTESIAN_POINT('Origin',(197.762132885264,11.,29.5));
#72616=CARTESIAN_POINT('',(201.054417864302,10.1027692940023,30.2629365128992));
#72617=CARTESIAN_POINT('',(200.956011803843,10.1027690874833,30.2629362700282));
#72618=CARTESIAN_POINT('',(197.762132885264,10.1027690874833,30.2629362700282));
#72619=CARTESIAN_POINT('Ctrl Pts',(201.054417864302,10.1027692940023,30.2629365128992));
#72620=CARTESIAN_POINT('Ctrl Pts',(201.05141890073,10.1293141722984,30.2941538940201));
#72621=CARTESIAN_POINT('Ctrl Pts',(201.048436058869,10.1574897561157,30.3239877180485));
#72622=CARTESIAN_POINT('Ctrl Pts',(201.044447884818,10.1981927710927,30.3628044051238));
#72623=CARTESIAN_POINT('Ctrl Pts',(201.043380444452,10.2093995741434,30.3730849289079));
#72624=CARTESIAN_POINT('Ctrl Pts',(201.041857920987,10.2258809677539,30.387626411253));
#72625=CARTESIAN_POINT('Ctrl Pts',(201.041391629439,10.2309976879275,30.3920629863274));
#72626=CARTESIAN_POINT('Ctrl Pts',(201.040608655144,10.2397114783181,30.3994877921686));
#72627=CARTESIAN_POINT('Ctrl Pts',(201.040290374247,10.2432884733418,30.402499081806));
#72628=CARTESIAN_POINT('Ctrl Pts',(201.039562110351,10.2515541690651,30.4093738542067));
#72629=CARTESIAN_POINT('Ctrl Pts',(201.039153163814,10.2562549515858,30.4132224677239));
#72630=CARTESIAN_POINT('Ctrl Pts',(201.037999407172,10.2696786500102,30.4240402801249));
#72631=CARTESIAN_POINT('Ctrl Pts',(201.037260282136,10.2784714300278,30.4309222621592));
#72632=CARTESIAN_POINT('Ctrl Pts',(201.03153824864,10.3479287880017,30.4837100942689));
#72633=CARTESIAN_POINT('Ctrl Pts',(201.026869315461,10.4128222971946,30.5237713871246));
#72634=CARTESIAN_POINT('Ctrl Pts',(201.019162536663,10.5245155795484,30.5785846089263));
#72635=CARTESIAN_POINT('Ctrl Pts',(201.016160481788,10.569163570506,30.5971826343835));
#72636=CARTESIAN_POINT('Ctrl Pts',(201.011745153561,10.6347514312984,30.6198808655372));
#72637=CARTESIAN_POINT('Ctrl Pts',(201.010391259537,10.6548583048927,30.626240118351));
#72638=CARTESIAN_POINT('Ctrl Pts',(201.007905342958,10.6916391657401,30.6367954364878));
#72639=CARTESIAN_POINT('Ctrl Pts',(201.006778967143,10.7082551327778,30.6411727093527));
#72640=CARTESIAN_POINT('Ctrl Pts',(201.004966253194,10.7348705325665,30.647564946707));
#72641=CARTESIAN_POINT('Ctrl Pts',(201.004287373938,10.7448110284203,30.6498162980962));
#72642=CARTESIAN_POINT('Ctrl Pts',(201.002986846657,10.7637933712409,30.6538571955829));
#72643=CARTESIAN_POINT('Ctrl Pts',(201.00236598706,10.7728294918616,30.6556701740891));
#72644=CARTESIAN_POINT('Ctrl Pts',(201.000941441793,10.7934975173951,30.659565181058));
#72645=CARTESIAN_POINT('Ctrl Pts',(201.000135681691,10.805141185382,30.661578542035));
#72646=CARTESIAN_POINT('Ctrl Pts',(200.997501904897,10.8430363755375,30.6675453769099));
#72647=CARTESIAN_POINT('Ctrl Pts',(200.995652425535,10.8693900937279,30.6707863371429));
#72648=CARTESIAN_POINT('Ctrl Pts',(200.987854904254,10.9793891975865,30.6805539392231));
#72649=CARTESIAN_POINT('Ctrl Pts',(200.98168349618,11.0634939303877,30.6790238877709));
#72650=CARTESIAN_POINT('Ctrl Pts',(200.973090014501,11.1800188967315,30.6643948450842));
#72651=CARTESIAN_POINT('Ctrl Pts',(200.970646080825,11.2131376043149,30.6587902219369));
#72652=CARTESIAN_POINT('Ctrl Pts',(200.967253722702,11.2595372161782,30.648881137232));
#72653=CARTESIAN_POINT('Ctrl Pts',(200.966269732865,11.2730495631276,30.6457449127133));
#72654=CARTESIAN_POINT('Ctrl Pts',(200.964540836263,11.2969346345543,30.6397545911496));
#72655=CARTESIAN_POINT('Ctrl Pts',(200.963791973521,11.3073294689082,30.6369957444613));
#72656=CARTESIAN_POINT('Ctrl Pts',(200.962642048408,11.3233888242212,30.6324971572702));
#72657=CARTESIAN_POINT('Ctrl Pts',(200.962235899982,11.3290801733011,30.6308564834628));
#72658=CARTESIAN_POINT('Ctrl Pts',(200.961475318814,11.3397790003519,30.6276846669657));
#72659=CARTESIAN_POINT('Ctrl Pts',(200.961120420838,11.3447887920779,30.6261630286523));
#72660=CARTESIAN_POINT('Ctrl Pts',(200.960269321222,11.3568417623379,30.6224141747818));
#72661=CARTESIAN_POINT('Ctrl Pts',(200.959774966841,11.3638744156748,30.6201540249725));
#72662=CARTESIAN_POINT('Ctrl Pts',(200.958100545071,11.38778267967,30.6122214704124));
#72663=CARTESIAN_POINT('Ctrl Pts',(200.956936697517,11.4045515759021,30.6062323930871));
#72664=CARTESIAN_POINT('Ctrl Pts',(200.95120058265,11.4875288311721,30.5744573147878));
#72665=CARTESIAN_POINT('Ctrl Pts',(200.946848776718,11.5514496693805,30.5430954445361));
#72666=CARTESIAN_POINT('Ctrl Pts',(200.94144643856,11.6258878993012,30.4978064342095));
#72667=CARTESIAN_POINT('Ctrl Pts',(200.940448230259,11.6394449639331,30.4891731237403));
#72668=CARTESIAN_POINT('Ctrl Pts',(200.937246351682,11.6821638592468,30.4607238940268));
#72669=CARTESIAN_POINT('Ctrl Pts',(200.935027189226,11.7106127823508,30.4398761332686));
#72670=CARTESIAN_POINT('Ctrl Pts',(200.931162614273,11.7575878965633,30.4020987506594));
#72671=CARTESIAN_POINT('Ctrl Pts',(200.92953860289,11.7765870220306,30.3857957071283));
#72672=CARTESIAN_POINT('Ctrl Pts',(200.927120954748,11.803675566543,30.3610094621293));
#72673=CARTESIAN_POINT('Ctrl Pts',(200.926346201202,11.8121815244313,30.3529905424156));
#72674=CARTESIAN_POINT('Ctrl Pts',(200.924953498105,11.827151474094,30.3384508151227));
#72675=CARTESIAN_POINT('Ctrl Pts',(200.924337640988,11.8336613139201,30.3319784468883));
#72676=CARTESIAN_POINT('Ctrl Pts',(200.923018622269,11.8473662778599,30.3180300125284));
#72677=CARTESIAN_POINT('Ctrl Pts',(200.922314598505,11.8545395587158,30.31053367667));
#72678=CARTESIAN_POINT('Ctrl Pts',(200.920404443354,11.8736159068938,30.2900634714575));
#72679=CARTESIAN_POINT('Ctrl Pts',(200.919190585993,11.8853282214557,30.276916291916));
#72680=CARTESIAN_POINT('Ctrl Pts',(200.911937578125,11.9528725414347,30.1975858463982));
#72681=CARTESIAN_POINT('Ctrl Pts',(200.905621309079,12.0015539060369,30.125681142446));
#72682=CARTESIAN_POINT('Ctrl Pts',(200.896249242902,12.0611497923409,30.0126003882821));
#72683=CARTESIAN_POINT('Ctrl Pts',(200.893228169189,12.0784588816488,29.9751050653797));
#72684=CARTESIAN_POINT('Ctrl Pts',(200.888618226564,12.1022790188109,29.9154553264129));
#72685=CARTESIAN_POINT('Ctrl Pts',(200.886989841909,12.1101688017286,29.8938877445873));
#72686=CARTESIAN_POINT('Ctrl Pts',(200.884842954916,12.1199154875853,29.8646183942858));
#72687=CARTESIAN_POINT('Ctrl Pts',(200.884297700493,12.122332288692,29.8571099480436));
#72688=CARTESIAN_POINT('Ctrl Pts',(200.883391582071,12.1262526233699,29.8444973048884));
#72689=CARTESIAN_POINT('Ctrl Pts',(200.883028488564,12.1277973052589,29.8394062571825));
#72690=CARTESIAN_POINT('Ctrl Pts',(200.882279430934,12.1309301447227,29.8288232794494));
#72691=CARTESIAN_POINT('Ctrl Pts',(200.881893761361,12.1325128993987,29.8233299823168));
#72692=CARTESIAN_POINT('Ctrl Pts',(200.880854080684,12.1366948794347,29.8084079512948));
#72693=CARTESIAN_POINT('Ctrl Pts',(200.880204217992,12.1392168244339,29.7989577821247));
#72694=CARTESIAN_POINT('Ctrl Pts',(200.876366233717,12.1535340615244,29.7424943641798));
#72695=CARTESIAN_POINT('Ctrl Pts',(200.873308747182,12.1625370502276,29.6948154306466));
#72696=CARTESIAN_POINT('Ctrl Pts',(200.865953751255,12.1772382088655,29.577719425106));
#72697=CARTESIAN_POINT('Ctrl Pts',(200.861702868868,12.1797730434681,29.5080968219526));
#72698=CARTESIAN_POINT('Ctrl Pts',(200.854932337871,12.1741873925625,29.4010001848339));
#72699=CARTESIAN_POINT('Ctrl Pts',(200.852516794904,12.1704161585616,29.3634621222647));
#72700=CARTESIAN_POINT('Ctrl Pts',(200.849163476261,12.1628607691475,29.3128321317298));
#72701=CARTESIAN_POINT('Ctrl Pts',(200.848273377335,12.1606411451323,29.2995278389988));
#72702=CARTESIAN_POINT('Ctrl Pts',(200.846747657742,12.1564788131757,29.2769728672643));
#72703=CARTESIAN_POINT('Ctrl Pts',(200.846115691693,12.1546523018101,29.2677019146527));
#72704=CARTESIAN_POINT('Ctrl Pts',(200.844905998779,12.1509634418492,29.2500977929029));
#72705=CARTESIAN_POINT('Ctrl Pts',(200.844328952811,12.1491216296573,29.2417609028978));
#72706=CARTESIAN_POINT('Ctrl Pts',(200.842968538324,12.1445887612333,29.2222525173519));
#72707=CARTESIAN_POINT('Ctrl Pts',(200.842182915249,12.1418245680834,29.2110990894847));
#72708=CARTESIAN_POINT('Ctrl Pts',(200.839352682281,12.1313486659258,29.1713307142085));
#72709=CARTESIAN_POINT('Ctrl Pts',(200.837279827866,12.1227213002895,29.1429706983062));
#72710=CARTESIAN_POINT('Ctrl Pts',(200.828406912823,12.0818411706136,29.0247960786888));
#72711=CARTESIAN_POINT('Ctrl Pts',(200.821323007916,12.0398068727197,28.9387545017789));
#72712=CARTESIAN_POINT('Ctrl Pts',(200.812723621565,11.9753005273021,28.8393815938006));
#72713=CARTESIAN_POINT('Ctrl Pts',(200.811061587052,11.9621662765048,28.8203942505181));
#72714=CARTESIAN_POINT('Ctrl Pts',(200.808312718992,11.9392036366574,28.7892000709783));
#72715=CARTESIAN_POINT('Ctrl Pts',(200.807213272026,11.9296746287227,28.7767813941304));
#72716=CARTESIAN_POINT('Ctrl Pts',(200.805654108371,11.9156243313504,28.7592071562465));
#72717=CARTESIAN_POINT('Ctrl Pts',(200.805182456969,11.9113015981471,28.7538958809825));
#72718=CARTESIAN_POINT('Ctrl Pts',(200.804360062312,11.9036321841737,28.7446386946175));
#72719=CARTESIAN_POINT('Ctrl Pts',(200.804007999141,11.9003054865297,28.7406767089274));
#72720=CARTESIAN_POINT('Ctrl Pts',(200.803234961785,11.8929040484637,28.7319788748419));
#72721=CARTESIAN_POINT('Ctrl Pts',(200.802814821885,11.8888176087104,28.7272533718877));
#72722=CARTESIAN_POINT('Ctrl Pts',(200.801571359817,11.8765396228386,28.7132815376905));
#72723=CARTESIAN_POINT('Ctrl Pts',(200.800755342794,11.8682397300543,28.7041310097451));
#72724=CARTESIAN_POINT('Ctrl Pts',(200.796671911984,11.825570053211,28.6585504123285));
#72725=CARTESIAN_POINT('Ctrl Pts',(200.793532094047,11.7890419363471,28.6242048058001));
#72726=CARTESIAN_POINT('Ctrl Pts',(200.787750698132,11.7173389934812,28.564925816093));
#72727=CARTESIAN_POINT('Ctrl Pts',(200.78510637674,11.6827724458304,28.5393956354292));
#72728=CARTESIAN_POINT('Ctrl Pts',(200.780141790337,11.6161848625346,28.4956289004162));
#72729=CARTESIAN_POINT('Ctrl Pts',(200.777832840778,11.5845550194756,28.4768967607829));
#72730=CARTESIAN_POINT('Ctrl Pts',(200.773830606244,11.5293536503388,28.4476012797737));
#72731=CARTESIAN_POINT('Ctrl Pts',(200.772160983206,11.5062158812604,28.436278380319));
#72732=CARTESIAN_POINT('Ctrl Pts',(200.769688539792,11.4719520432726,28.4208819022617));
#72733=CARTESIAN_POINT('Ctrl Pts',(200.768905897474,11.4611053651756,28.4162027746508));
#72734=CARTESIAN_POINT('Ctrl Pts',(200.767504513069,11.4416961464602,28.4081739715416));
#72735=CARTESIAN_POINT('Ctrl Pts',(200.766887966837,11.433161201807,28.404759876842));
#72736=CARTESIAN_POINT('Ctrl Pts',(200.76557332907,11.4149775618981,28.3977319613854));
#72737=CARTESIAN_POINT('Ctrl Pts',(200.764874442856,11.4053197065782,28.3941441641362));
#72738=CARTESIAN_POINT('Ctrl Pts',(200.76296219031,11.378927012748,28.3847317190714));
#72739=CARTESIAN_POINT('Ctrl Pts',(200.761740882735,11.3621063783595,28.3791574902337));
#72740=CARTESIAN_POINT('Ctrl Pts',(200.754422247733,11.2615715573451,28.3483402238901));
#72741=CARTESIAN_POINT('Ctrl Pts',(200.748041631359,11.1753957457005,28.3321082519489));
#72742=CARTESIAN_POINT('Ctrl Pts',(200.738642497543,11.0475570248609,28.3225037183181));
#72743=CARTESIAN_POINT('Ctrl Pts',(200.735657013185,11.0067448321476,28.3215628951638));
#72744=CARTESIAN_POINT('Ctrl Pts',(200.731093422795,10.9431741770112,28.3234007848732));
#72745=CARTESIAN_POINT('Ctrl Pts',(200.729476614283,10.9204061893324,28.3247213650817));
#72746=CARTESIAN_POINT('Ctrl Pts',(200.727342273112,10.8898507229845,28.3273857797826));
#72747=CARTESIAN_POINT('Ctrl Pts',(200.726798367985,10.8820189432541,28.3281478543253));
#72748=CARTESIAN_POINT('Ctrl Pts',(200.725893837773,10.8689090761659,28.3295562819846));
#72749=CARTESIAN_POINT('Ctrl Pts',(200.72553099998,10.8636267494636,28.3301599817313));
#72750=CARTESIAN_POINT('Ctrl Pts',(200.724781758562,10.8526667944155,28.3314878074478));
#72751=CARTESIAN_POINT('Ctrl Pts',(200.724395657091,10.846990076168,28.3322175783778));
#72752=CARTESIAN_POINT('Ctrl Pts',(200.723353495824,10.8315969876953,28.3343106125086));
#72753=CARTESIAN_POINT('Ctrl Pts',(200.722701618129,10.8218917288532,28.3357539857233));
#72754=CARTESIAN_POINT('Ctrl Pts',(200.718611872454,10.7606084148588,28.3456523838812));
#72755=CARTESIAN_POINT('Ctrl Pts',(200.715326672411,10.7096169660092,28.357412686223));
#72756=CARTESIAN_POINT('Ctrl Pts',(200.707928337667,10.5957520297336,28.3917930172262));
#72757=CARTESIAN_POINT('Ctrl Pts',(200.703845070844,10.533687095696,28.4164451230236));
#72758=CARTESIAN_POINT('Ctrl Pts',(200.697299644535,10.4409956962848,28.4627086610199));
#72759=CARTESIAN_POINT('Ctrl Pts',(200.694932082059,10.4087467309301,28.4807462007063));
#72760=CARTESIAN_POINT('Ctrl Pts',(200.691634671177,10.3660280718114,28.5073499369256));
#72761=CARTESIAN_POINT('Ctrl Pts',(200.69075035783,10.3547777471873,28.5146255665149));
#72762=CARTESIAN_POINT('Ctrl Pts',(200.689231520821,10.3358222235394,28.5273479970769));
#72763=CARTESIAN_POINT('Ctrl Pts',(200.688600569845,10.3280537367478,28.5326984709259));
#72764=CARTESIAN_POINT('Ctrl Pts',(200.687314248257,10.3124357137779,28.543734170488));
#72765=CARTESIAN_POINT('Ctrl Pts',(200.6866587332,10.3045904275246,28.5494241212406));
#72766=CARTESIAN_POINT('Ctrl Pts',(200.684996715318,10.2849904036469,28.5640119299813));
#72767=CARTESIAN_POINT('Ctrl Pts',(200.683985494923,10.2733311455468,28.5730346650608));
#72768=CARTESIAN_POINT('Ctrl Pts',(200.679833388212,10.2265532601005,28.6106595374539));
#72769=CARTESIAN_POINT('Ctrl Pts',(200.676623568423,10.1929327596224,28.6410541879715));
#72770=CARTESIAN_POINT('Ctrl Pts',(200.667735793441,10.106444254334,28.728814537637));
#72771=CARTESIAN_POINT('Ctrl Pts',(200.661957287503,10.0573884775016,28.7896118735937));
#72772=CARTESIAN_POINT('Ctrl Pts',(200.654014115923,9.99732215424863,28.8813415542616));
#72773=CARTESIAN_POINT('Ctrl Pts',(200.651743890046,9.98102347763466,28.9085709260413));
#72774=CARTESIAN_POINT('Ctrl Pts',(200.648918802115,9.96165623380376,28.9441098738704));
#72775=CARTESIAN_POINT('Ctrl Pts',(200.648312456098,9.95755522895397,28.9518389654976));
#72776=CARTESIAN_POINT('Ctrl Pts',(200.647333455453,9.95101951748242,28.9644953780907));
#72777=CARTESIAN_POINT('Ctrl Pts',(200.646957794093,9.9485325764679,28.969395144078));
#72778=CARTESIAN_POINT('Ctrl Pts',(200.646256139448,9.94392541077959,28.9786317762011));
#72779=CARTESIAN_POINT('Ctrl Pts',(200.645929666482,9.94179739581556,28.9829645918203));
#72780=CARTESIAN_POINT('Ctrl Pts',(200.645060668794,9.93617730397211,28.9945876214244));
#72781=CARTESIAN_POINT('Ctrl Pts',(200.644520970184,9.93273346461972,29.0019010616437));
#72782=CARTESIAN_POINT('Ctrl Pts',(200.642476888394,9.91988313897022,29.0299356962415));
#72783=CARTESIAN_POINT('Ctrl Pts',(200.640999905714,9.9110019965769,29.0508937924601));
#72784=CARTESIAN_POINT('Ctrl Pts',(200.634735062853,9.8754324491238,29.1421045074596));
#72785=CARTESIAN_POINT('Ctrl Pts',(200.630156885762,9.854892181428,29.2145684187275));
#72786=CARTESIAN_POINT('Ctrl Pts',(200.623087588231,9.83448916145321,29.3263368932514));
#72787=CARTESIAN_POINT('Ctrl Pts',(200.62067512635,9.82944015372225,29.3644871657389));
#72788=CARTESIAN_POINT('Ctrl Pts',(200.616515395183,9.82407423725943,29.4292923526529));
#72789=CARTESIAN_POINT('Ctrl Pts',(200.614794530274,9.82277856374822,29.4558355737844));
#72790=CARTESIAN_POINT('Ctrl Pts',(200.612260669024,9.82220297591759,29.494344844251));
#72791=CARTESIAN_POINT('Ctrl Pts',(200.611469356697,9.82220621789741,29.5062928901909));
#72792=CARTESIAN_POINT('Ctrl Pts',(200.610058330521,9.82253381610417,29.5274450210217));
#72793=CARTESIAN_POINT('Ctrl Pts',(200.609440926464,9.82278436125572,29.536649354243));
#72794=CARTESIAN_POINT('Ctrl Pts',(200.608130602817,9.823540986179,29.5560702375485));
#72795=CARTESIAN_POINT('Ctrl Pts',(200.607436958707,9.82407229265051,29.5662849794616));
#72796=CARTESIAN_POINT('Ctrl Pts',(200.60555504918,9.82586389627428,29.593812397771));
#72797=CARTESIAN_POINT('Ctrl Pts',(200.604359266947,9.82737396042127,29.6111056808609));
#72798=CARTESIAN_POINT('Ctrl Pts',(200.59686614933,9.83911558100066,29.7181988436053));
#72799=CARTESIAN_POINT('Ctrl Pts',(200.590262393601,9.85927264856534,29.8065923087688));
#72800=CARTESIAN_POINT('Ctrl Pts',(200.580765968669,9.90237090652315,29.9287687957684));
#72801=CARTESIAN_POINT('Ctrl Pts',(200.577899560204,9.91725279626853,29.9650710958159));
#72802=CARTESIAN_POINT('Ctrl Pts',(200.573491864858,9.94337801895126,30.0207114460847));
#72803=CARTESIAN_POINT('Ctrl Pts',(200.571914565533,9.95340740458794,30.040587187807));
#72804=CARTESIAN_POINT('Ctrl Pts',(200.569823138748,9.96770573821754,30.0670312988375));
#72805=CARTESIAN_POINT('Ctrl Pts',(200.569283916213,9.97148489707319,30.0738576722635));
#72806=CARTESIAN_POINT('Ctrl Pts',(200.568384887539,9.97794689830022,30.0852611868707));
#72807=CARTESIAN_POINT('Ctrl Pts',(200.568022926901,9.98059329100803,30.0898585980502));
#72808=CARTESIAN_POINT('Ctrl Pts',(200.567272995235,9.98617141474628,30.0993994411089));
#72809=CARTESIAN_POINT('Ctrl Pts',(200.566885353227,9.98910840193206,30.1043395326335));
#72810=CARTESIAN_POINT('Ctrl Pts',(200.565834336185,9.99721437416923,30.1177495470124));
#72811=CARTESIAN_POINT('Ctrl Pts',(200.565175264433,10.0024545491371,30.1261761760927));
#72812=CARTESIAN_POINT('Ctrl Pts',(200.561011821934,10.0365147245592,30.1794347518356));
#72813=CARTESIAN_POINT('Ctrl Pts',(200.557666169063,10.0682437893456,30.2223337114375));
#72814=CARTESIAN_POINT('Ctrl Pts',(200.554352848915,10.1027690892854,30.2629362721474));
#72815=CARTESIAN_POINT('',(200.512132885305,9.82225021170068,29.5007061592685));
#72816=CARTESIAN_POINT('Ctrl Pts',(200.456078305605,10.1027690874833,30.2629362700282));
#72817=CARTESIAN_POINT('Ctrl Pts',(200.459247165187,10.0723083011789,30.227113672302));
#72818=CARTESIAN_POINT('Ctrl Pts',(200.462416024768,10.0439833305474,30.1894488856546));
#72819=CARTESIAN_POINT('Ctrl Pts',(200.465584884349,10.0180138899712,30.1502294535089));
#72820=CARTESIAN_POINT('Ctrl Pts',(200.468756203967,9.99202428890455,30.1109795746932));
#72821=CARTESIAN_POINT('Ctrl Pts',(200.471927523584,9.96839418568235,30.0701731002698));
#72822=CARTESIAN_POINT('Ctrl Pts',(200.475098843202,9.94730004587657,30.0281267547554));
#72823=CARTESIAN_POINT('Ctrl Pts',(200.478271213189,9.92619891949807,29.9860664831055));
#72824=CARTESIAN_POINT('Ctrl Pts',(200.481443583177,9.90763565733653,29.9427660318742));
#72825=CARTESIAN_POINT('Ctrl Pts',(200.484615953165,9.89173914812929,29.8985636043479));
#72826=CARTESIAN_POINT('Ctrl Pts',(200.487794649595,9.87581093758726,29.8542730269055));
#72827=CARTESIAN_POINT('Ctrl Pts',(200.490973346026,9.86256026986468,29.8090774137332));
#72828=CARTESIAN_POINT('Ctrl Pts',(200.494152042457,9.85206611231544,29.7633303096975));
#72829=CARTESIAN_POINT('Ctrl Pts',(200.497157265917,9.84214465893017,29.7200797907234));
#72830=CARTESIAN_POINT('Ctrl Pts',(200.500162489378,9.83468667522977,29.676336831864));
#72831=CARTESIAN_POINT('Ctrl Pts',(200.503167712838,9.82971621933516,29.6324044380404));
#72832=CARTESIAN_POINT('Ctrl Pts',(200.506156103647,9.82477360361806,29.5887181153357));
#72833=CARTESIAN_POINT('Ctrl Pts',(200.509144494455,9.82227661969029,29.5447500160668));
#72834=CARTESIAN_POINT('Ctrl Pts',(200.512132885264,9.82225021170104,29.5007061598695));
#72835=CARTESIAN_POINT('Ctrl Pts',(200.512132885305,9.82225021170068,29.5007061592685));
#72836=CARTESIAN_POINT('Ctrl Pts',(200.515267830035,9.82222250865862,29.4545023446655));
#72837=CARTESIAN_POINT('Ctrl Pts',(200.518402774765,9.82491796434091,29.408194106874));
#72838=CARTESIAN_POINT('Ctrl Pts',(200.521537719495,9.83034710037947,29.3621335540848));
#72839=CARTESIAN_POINT('Ctrl Pts',(200.524668736786,9.83576943483166,29.316130705657));
#72840=CARTESIAN_POINT('Ctrl Pts',(200.527799754078,9.84391861397454,29.2703754939379));
#72841=CARTESIAN_POINT('Ctrl Pts',(200.530930771369,9.85475316768141,29.2252187132204));
#72842=CARTESIAN_POINT('Ctrl Pts',(200.534059329963,9.86557921332608,29.180097392819));
#72843=CARTESIAN_POINT('Ctrl Pts',(200.537187888557,9.87908632916235,29.1355741295138));
#72844=CARTESIAN_POINT('Ctrl Pts',(200.540316447151,9.89518182682023,29.0919903595358));
#72845=CARTESIAN_POINT('Ctrl Pts',(200.543444011243,9.91127220806062,29.0484204439143));
#72846=CARTESIAN_POINT('Ctrl Pts',(200.546571575334,9.92994914174014,29.0057899667846));
#72847=CARTESIAN_POINT('Ctrl Pts',(200.549699139426,9.95107076630701,28.9644231845904));
#72848=CARTESIAN_POINT('Ctrl Pts',(200.552829311202,9.97221000155768,28.923021911805));
#72849=CARTESIAN_POINT('Ctrl Pts',(200.555959482979,9.99579773645662,28.8828869490627));
#72850=CARTESIAN_POINT('Ctrl Pts',(200.559089654755,10.0216457995202,28.8443185827678));
#72851=CARTESIAN_POINT('Ctrl Pts',(200.562221316338,10.0475061649802,28.8057318598431));
#72852=CARTESIAN_POINT('Ctrl Pts',(200.565352977921,10.0756286526337,28.7687136740076));
#72853=CARTESIAN_POINT('Ctrl Pts',(200.568484639504,10.1057835683042,28.7335327562216));
#72854=CARTESIAN_POINT('Ctrl Pts',(200.571621921098,10.1359925993205,28.6982887035375));
#72855=CARTESIAN_POINT('Ctrl Pts',(200.574759202692,10.1682409342474,28.6648889062404));
#72856=CARTESIAN_POINT('Ctrl Pts',(200.577896484286,10.20226213217,28.6335651457091));
#72857=CARTESIAN_POINT('Ctrl Pts',(200.579204193381,10.2164431448211,28.6205085024544));
#72858=CARTESIAN_POINT('Ctrl Pts',(200.580511902477,10.2309317985967,28.607812070833));
#72859=CARTESIAN_POINT('Ctrl Pts',(200.581819611573,10.2457072655321,28.5954904460268));
#72860=CARTESIAN_POINT('Ctrl Pts',(200.58509677402,10.28273507664,28.5646120448321));
#72861=CARTESIAN_POINT('Ctrl Pts',(200.588373936467,10.3217456398475,28.5359414302213));
#72862=CARTESIAN_POINT('Ctrl Pts',(200.591651098915,10.3624431471825,28.5097392656853));
#72863=CARTESIAN_POINT('Ctrl Pts',(200.594825051242,10.4018589375795,28.4843623054505));
#72864=CARTESIAN_POINT('Ctrl Pts',(200.597999003569,10.4428564756788,28.4613009368035));
#72865=CARTESIAN_POINT('Ctrl Pts',(200.601172955896,10.4851331052859,28.4407516140076));
#72866=CARTESIAN_POINT('Ctrl Pts',(200.60434378326,10.5273681107945,28.4202225233599));
#72867=CARTESIAN_POINT('Ctrl Pts',(200.607514610625,10.5708792164448,28.402200825393));
#72868=CARTESIAN_POINT('Ctrl Pts',(200.610685437989,10.6153380446159,28.3868377285498));
#72869=CARTESIAN_POINT('Ctrl Pts',(200.61385453493,10.6597726101605,28.3714830158476));
#72870=CARTESIAN_POINT('Ctrl Pts',(200.61702363187,10.7051533481686,28.3587842115252));
#72871=CARTESIAN_POINT('Ctrl Pts',(200.620192728811,10.7511332497709,28.3488438841189));
#72872=CARTESIAN_POINT('Ctrl Pts',(200.623361486869,10.7971082345838,28.3389046196661));
#72873=CARTESIAN_POINT('Ctrl Pts',(200.626530244927,10.8436817113453,28.3317233618479));
#72874=CARTESIAN_POINT('Ctrl Pts',(200.629699002986,10.8904955705373,28.32735178232));
#72875=CARTESIAN_POINT('Ctrl Pts',(200.632870947417,10.9373565038202,28.3229758069116));
#72876=CARTESIAN_POINT('Ctrl Pts',(200.636042891848,10.9844577463792,28.3214151967753));
#72877=CARTESIAN_POINT('Ctrl Pts',(200.639214836279,11.0314371450912,28.3226696434694));
#72878=CARTESIAN_POINT('Ctrl Pts',(200.642388725544,11.0784453485838,28.3239248593104));
#72879=CARTESIAN_POINT('Ctrl Pts',(200.64556261481,11.1253310047503,28.3279985183767));
#72880=CARTESIAN_POINT('Ctrl Pts',(200.648736504076,11.1717366866115,28.3348383919079));
#72881=CARTESIAN_POINT('Ctrl Pts',(200.65191600855,11.2182244688689,28.3416903664644));
#72882=CARTESIAN_POINT('Ctrl Pts',(200.655095513024,11.2642300394651,28.3513181999576));
#72883=CARTESIAN_POINT('Ctrl Pts',(200.658275017497,11.3094077005038,28.3636189295096));
#72884=CARTESIAN_POINT('Ctrl Pts',(200.659007181767,11.3198110414896,28.3664514950068));
#72885=CARTESIAN_POINT('Ctrl Pts',(200.659739346037,11.33017055685,28.3694255918482));
#72886=CARTESIAN_POINT('Ctrl Pts',(200.660471510307,11.3404821730351,28.3725396005423));
#72887=CARTESIAN_POINT('Ctrl Pts',(200.663748672754,11.3866368991321,28.3864778829378));
#72888=CARTESIAN_POINT('Ctrl Pts',(200.667025835201,11.4320384548995,28.4032864200174));
#72889=CARTESIAN_POINT('Ctrl Pts',(200.670302997649,11.4763064424699,28.4228615523705));
#72890=CARTESIAN_POINT('Ctrl Pts',(200.673476949983,11.519180265401,28.4418201905292));
#72891=CARTESIAN_POINT('Ctrl Pts',(200.676650902317,11.5609903132395,28.463373491059));
#72892=CARTESIAN_POINT('Ctrl Pts',(200.679824854651,11.6014060442784,28.4873767569301));
#72893=CARTESIAN_POINT('Ctrl Pts',(200.682995682023,11.6417819833963,28.5113563900218));
#72894=CARTESIAN_POINT('Ctrl Pts',(200.686166509394,11.6807658463069,28.5377809307864));
#72895=CARTESIAN_POINT('Ctrl Pts',(200.689337336765,11.718050729299,28.5664593138737));
#72896=CARTESIAN_POINT('Ctrl Pts',(200.692506433713,11.7553152647206,28.5951220462368));
#72897=CARTESIAN_POINT('Ctrl Pts',(200.695675530661,11.7908822164014,28.626035845272));
#72898=CARTESIAN_POINT('Ctrl Pts',(200.698844627609,11.824475053101,28.6589673316011));
#72899=CARTESIAN_POINT('Ctrl Pts',(200.702013385675,11.8580642976036,28.6918952964537));
#72900=CARTESIAN_POINT('Ctrl Pts',(200.70518214374,11.8896794504308,28.7268401290094));
#72901=CARTESIAN_POINT('Ctrl Pts',(200.708350901806,11.9190803799067,28.7635311834364));
#72902=CARTESIAN_POINT('Ctrl Pts',(200.711522846244,11.9485108737482,28.8002591328789));
#72903=CARTESIAN_POINT('Ctrl Pts',(200.714694790682,11.9757223546312,28.8387363712393));
#72904=CARTESIAN_POINT('Ctrl Pts',(200.717866735121,12.0005158768177,28.8786602839543));
#72905=CARTESIAN_POINT('Ctrl Pts',(200.721040624394,12.0253246008159,28.9186086754748));
#72906=CARTESIAN_POINT('Ctrl Pts',(200.724214513667,12.0477121510873,28.9600050165492));
#72907=CARTESIAN_POINT('Ctrl Pts',(200.72738840294,12.0675255417332,29.0025220806435));
#72908=CARTESIAN_POINT('Ctrl Pts',(200.730567907421,12.0873739860007,29.0451143654361));
#72909=CARTESIAN_POINT('Ctrl Pts',(200.733747411902,12.1046389855921,29.0888308097341));
#72910=CARTESIAN_POINT('Ctrl Pts',(200.736926916384,12.1192163758018,29.1333260758697));
#72911=CARTESIAN_POINT('Ctrl Pts',(200.737659080603,12.1225732018677,29.1435722768031));
#72912=CARTESIAN_POINT('Ctrl Pts',(200.738391244822,12.1257877244891,29.1538597273475));
#72913=CARTESIAN_POINT('Ctrl Pts',(200.739123409041,12.1288590554845,29.1641841347546));
#72914=CARTESIAN_POINT('Ctrl Pts',(200.742400571488,12.1426063137344,29.2103961174795));
#72915=CARTESIAN_POINT('Ctrl Pts',(200.745677733935,12.1535422530453,29.2575578966654));
#72916=CARTESIAN_POINT('Ctrl Pts',(200.748954896383,12.1615442035913,29.305294772532));
#72917=CARTESIAN_POINT('Ctrl Pts',(200.752128848714,12.1692941427532,29.3515282354373));
#72918=CARTESIAN_POINT('Ctrl Pts',(200.755302801045,12.1742920693538,29.3983005091628));
#72919=CARTESIAN_POINT('Ctrl Pts',(200.758476753376,12.1764770088296,29.4452559574436));
#72920=CARTESIAN_POINT('Ctrl Pts',(200.761647580744,12.17865979709,29.4921651750252));
#72921=CARTESIAN_POINT('Ctrl Pts',(200.764818408113,12.1780350544799,29.5392566563634));
#72922=CARTESIAN_POINT('Ctrl Pts',(200.767989235481,12.1745935321515,29.5861690009678));
#72923=CARTESIAN_POINT('Ctrl Pts',(200.771158332426,12.1711538879736,29.6330557439832));
#72924=CARTESIAN_POINT('Ctrl Pts',(200.774327429371,12.1649005500777,29.6797629895004));
#72925=CARTESIAN_POINT('Ctrl Pts',(200.777496526315,12.1558763137879,29.7259314270396));
#72926=CARTESIAN_POINT('Ctrl Pts',(200.780665284378,12.1468530424906,29.7720949276293));
#72927=CARTESIAN_POINT('Ctrl Pts',(200.78383404244,12.1350595700837,29.8177191888861));
#72928=CARTESIAN_POINT('Ctrl Pts',(200.787002800503,12.1205898359021,29.8624548001793));
#72929=CARTESIAN_POINT('Ctrl Pts',(200.790174744938,12.1061055515507,29.9072353957635));
#72930=CARTESIAN_POINT('Ctrl Pts',(200.793346689373,12.0889398095057,29.9511250284773));
#72931=CARTESIAN_POINT('Ctrl Pts',(200.796518633808,12.0692359015845,29.9937910988088));
#72932=CARTESIAN_POINT('Ctrl Pts',(200.799692523078,12.0495199124794,30.0364833292627));
#72933=CARTESIAN_POINT('Ctrl Pts',(200.802866412348,12.0272629241048,30.0779500137933));
#72934=CARTESIAN_POINT('Ctrl Pts',(200.806040301618,12.0026540628077,30.1178833974425));
#72935=CARTESIAN_POINT('Ctrl Pts',(200.809219806096,11.9780016637975,30.1578874307729));
#72936=CARTESIAN_POINT('Ctrl Pts',(200.812399310575,11.9509894146852,30.1963522992468));
#72937=CARTESIAN_POINT('Ctrl Pts',(200.815578815053,11.9218484211995,30.2330010578655));
#72938=CARTESIAN_POINT('Ctrl Pts',(200.816310979293,11.9151379436652,30.2414403950999));
#72939=CARTESIAN_POINT('Ctrl Pts',(200.817043143534,11.9083147429375,30.2497835799293));
#72940=CARTESIAN_POINT('Ctrl Pts',(200.817775307775,11.9013819154724,30.2580275093685));
#72941=CARTESIAN_POINT('Ctrl Pts',(200.821052470222,11.8703506241902,30.2949272846798));
#72942=CARTESIAN_POINT('Ctrl Pts',(200.82432963267,11.8369797557264,30.3300016816453));
#72943=CARTESIAN_POINT('Ctrl Pts',(200.827606795117,11.8015147581959,30.3629421503752));
#72944=CARTESIAN_POINT('Ctrl Pts',(200.830780747448,11.7671666862285,30.3948452004064));
#72945=CARTESIAN_POINT('Ctrl Pts',(200.833954699779,11.7308548851155,30.4247463368333));
#72946=CARTESIAN_POINT('Ctrl Pts',(200.83712865211,11.6928428181089,30.4523990192639));
#72947=CARTESIAN_POINT('Ctrl Pts',(200.840299479478,11.65486817646,30.4800244758263));
#72948=CARTESIAN_POINT('Ctrl Pts',(200.843470306847,11.6151970307804,30.5054055340862));
#72949=CARTESIAN_POINT('Ctrl Pts',(200.846641134215,11.574126110073,30.5283356807154));
#72950=CARTESIAN_POINT('Ctrl Pts',(200.84981023116,11.5330776031001,30.5512533136193));
#72951=CARTESIAN_POINT('Ctrl Pts',(200.852979328104,11.4906313198475,30.5717224136642));
#72952=CARTESIAN_POINT('Ctrl Pts',(200.856148425049,11.4471108709277,30.5895810807821));
#72953=CARTESIAN_POINT('Ctrl Pts',(200.859317183112,11.4035950757988,30.6074378382115));
#72954=CARTESIAN_POINT('Ctrl Pts',(200.862485941174,11.3590058587834,30.6226845077689));
#72955=CARTESIAN_POINT('Ctrl Pts',(200.865654699236,11.3136866947387,30.6352073467186));
#72956=CARTESIAN_POINT('Ctrl Pts',(200.868826643672,11.2683219596065,30.6477427781202));
#72957=CARTESIAN_POINT('Ctrl Pts',(200.871998588107,11.222226350993,30.6575487674259));
#72958=CARTESIAN_POINT('Ctrl Pts',(200.875170532542,11.1757564507571,30.6645620346367));
#72959=CARTESIAN_POINT('Ctrl Pts',(200.878344421812,11.1292580581322,30.6715796019372));
#72960=CARTESIAN_POINT('Ctrl Pts',(200.881518311082,11.0823854718833,30.6758009898391));
#72961=CARTESIAN_POINT('Ctrl Pts',(200.884692200352,11.0354997368489,30.6772148619448));
#72962=CARTESIAN_POINT('Ctrl Pts',(200.88787170483,10.9885310521139,30.6786312354566));
#72963=CARTESIAN_POINT('Ctrl Pts',(200.891051209308,10.9415497279046,30.6772302056954));
#72964=CARTESIAN_POINT('Ctrl Pts',(200.894230713786,10.8949141696163,30.6730524416038));
#72965=CARTESIAN_POINT('Ctrl Pts',(200.894962878027,10.8841751099998,30.6720904019222));
#72966=CARTESIAN_POINT('Ctrl Pts',(200.895695042268,10.8734543464279,30.6709813348348));
#72967=CARTESIAN_POINT('Ctrl Pts',(200.896427206509,10.8627561735106,30.6697261194786));
#72968=CARTESIAN_POINT('Ctrl Pts',(200.899606238141,10.8163050793372,30.6642760181234));
#72969=CARTESIAN_POINT('Ctrl Pts',(200.902785269774,10.7700774970728,30.6560427733853));
#72970=CARTESIAN_POINT('Ctrl Pts',(200.905964301406,10.7244319227464,30.6450577702888));
#72971=CARTESIAN_POINT('Ctrl Pts',(200.909138523191,10.6788554097755,30.6340893874061));
#72972=CARTESIAN_POINT('Ctrl Pts',(200.912312744977,10.6338596985013,30.6203776167579));
#72973=CARTESIAN_POINT('Ctrl Pts',(200.915486966762,10.5897959969861,30.6040053162967));
#72974=CARTESIAN_POINT('Ctrl Pts',(200.918657779357,10.5457796209378,30.5876506000769));
#72975=CARTESIAN_POINT('Ctrl Pts',(200.921828591952,10.502693791468,30.5686412074309));
#72976=CARTESIAN_POINT('Ctrl Pts',(200.924999404548,10.4608747409026,30.5471098402284));
#72977=CARTESIAN_POINT('Ctrl Pts',(200.92816893808,10.4190725595717,30.5255871584857));
#72978=CARTESIAN_POINT('Ctrl Pts',(200.931338471613,10.3785366434163,30.5015447637476));
#72979=CARTESIAN_POINT('Ctrl Pts',(200.934508005146,10.3395811204066,30.4751625331075));
#72980=CARTESIAN_POINT('Ctrl Pts',(200.937676853713,10.3006340160467,30.4487860039121));
#72981=CARTESIAN_POINT('Ctrl Pts',(200.94084570228,10.2632670839165,30.4200709604753));
#72982=CARTESIAN_POINT('Ctrl Pts',(200.944014550847,10.2277652659539,30.3892404500655));
#72983=CARTESIAN_POINT('Ctrl Pts',(200.947185350756,10.1922415863641,30.3583909545682));
#72984=CARTESIAN_POINT('Ctrl Pts',(200.950356150665,10.1585857254588,30.3254237667288));
#72985=CARTESIAN_POINT('Ctrl Pts',(200.953526950575,10.1270475916668,30.2906005029629));
#72986=CARTESIAN_POINT('Ctrl Pts',(200.954355234997,10.1188091200833,30.2815038813661));
#72987=CARTESIAN_POINT('Ctrl Pts',(200.95518351942,10.1107149503495,30.2722807907571));
#72988=CARTESIAN_POINT('Ctrl Pts',(200.956011803843,10.1027690874833,30.2629362700282));
#72989=CARTESIAN_POINT('Origin',(197.762132885264,11.,29.5));
#72990=CARTESIAN_POINT('',(201.555825452273,10.1027690875306,30.2629362700837));
#72991=CARTESIAN_POINT('',(201.456090246984,10.1027690874833,30.2629362700282));
#72992=CARTESIAN_POINT('',(197.762132885264,10.1027690874833,30.2629362700282));
#72993=CARTESIAN_POINT('',(201.110124610169,9.82225025635667,29.4992229233845));
#72994=CARTESIAN_POINT('Ctrl Pts',(201.555825452273,10.1027690875306,30.2629362700837));
#72995=CARTESIAN_POINT('Ctrl Pts',(201.555549618905,10.1054509716362,30.2660902285697));
#72996=CARTESIAN_POINT('Ctrl Pts',(201.555273125248,10.1081494677841,30.2692300245477));
#72997=CARTESIAN_POINT('Ctrl Pts',(201.554388159376,10.1168182882239,30.2792095689722));
#72998=CARTESIAN_POINT('Ctrl Pts',(201.553777178604,10.1228510196037,30.2859943681334));
#72999=CARTESIAN_POINT('Ctrl Pts',(201.552385338527,10.1366973122065,30.301208855377));
#73000=CARTESIAN_POINT('Ctrl Pts',(201.551602596718,10.1445569451021,30.3095951608155));
#73001=CARTESIAN_POINT('Ctrl Pts',(201.549175793606,10.1691388209297,30.3350666187593));
#73002=CARTESIAN_POINT('Ctrl Pts',(201.547515014436,10.1862586031458,30.3517578027237));
#73003=CARTESIAN_POINT('Ctrl Pts',(201.543511585319,10.2282022413078,30.3902321071941));
#73004=CARTESIAN_POINT('Ctrl Pts',(201.541151785278,10.2534568057504,30.4115140878609));
#73005=CARTESIAN_POINT('Ctrl Pts',(201.535397084206,10.3164119606738,30.4601933751533));
#73006=CARTESIAN_POINT('Ctrl Pts',(201.531979012937,10.3549096272088,30.4864694451067));
#73007=CARTESIAN_POINT('Ctrl Pts',(201.524701344481,10.4400888838457,30.5374844889861));
#73008=CARTESIAN_POINT('Ctrl Pts',(201.520850663775,10.4870900714472,30.5615078491844));
#73009=CARTESIAN_POINT('Ctrl Pts',(201.516251513878,10.5470315736418,30.5872308226599));
#73010=CARTESIAN_POINT('Ctrl Pts',(201.515378181647,10.5585947989421,30.5919765272682));
#73011=CARTESIAN_POINT('Ctrl Pts',(201.514080942196,10.5760746681723,30.5988274464456));
#73012=CARTESIAN_POINT('Ctrl Pts',(201.51364979859,10.5819357851087,30.6010707337444));
#73013=CARTESIAN_POINT('Ctrl Pts',(201.51287173044,10.5926121856065,30.6050594823032));
#73014=CARTESIAN_POINT('Ctrl Pts',(201.512523964578,10.5974211688158,30.6068204810458));
#73015=CARTESIAN_POINT('Ctrl Pts',(201.511719997017,10.6086234810071,30.6108399759856));
#73016=CARTESIAN_POINT('Ctrl Pts',(201.511265144791,10.6150250266977,30.6130747087543));
#73017=CARTESIAN_POINT('Ctrl Pts',(201.509796398557,10.6358891553626,30.6201566872447));
#73018=CARTESIAN_POINT('Ctrl Pts',(201.508794278056,10.6504273009084,30.6247785077277));
#73019=CARTESIAN_POINT('Ctrl Pts',(201.502202986934,10.7477244750533,30.6536413318068));
#73020=CARTESIAN_POINT('Ctrl Pts',(201.496972088734,10.8328495788635,30.6690147384302));
#73021=CARTESIAN_POINT('Ctrl Pts',(201.488076790026,10.9754427654419,30.6788572922696));
#73022=CARTESIAN_POINT('Ctrl Pts',(201.484505489542,11.0321889077722,30.678673128179));
#73023=CARTESIAN_POINT('Ctrl Pts',(201.479808585131,11.1040058410088,30.6732491369712));
#73024=CARTESIAN_POINT('Ctrl Pts',(201.478799070319,11.1192897628913,30.671793782937));
#73025=CARTESIAN_POINT('Ctrl Pts',(201.477129171945,11.1442910596495,30.668918939284));
#73026=CARTESIAN_POINT('Ctrl Pts',(201.476474247601,11.1540271455874,30.6676759076095));
#73027=CARTESIAN_POINT('Ctrl Pts',(201.475187604885,11.1730116136353,30.6650105501108));
#73028=CARTESIAN_POINT('Ctrl Pts',(201.474556278589,11.1822608431334,30.6635994056202));
#73029=CARTESIAN_POINT('Ctrl Pts',(201.473042171879,11.2042798620371,30.6599710207039));
#73030=CARTESIAN_POINT('Ctrl Pts',(201.472156323961,11.2170315548777,30.6576529324552));
#73031=CARTESIAN_POINT('Ctrl Pts',(201.468961859277,11.2625324210609,30.6486032979458));
#73032=CARTESIAN_POINT('Ctrl Pts',(201.466617322494,11.2950272742429,30.6406889769245));
#73033=CARTESIAN_POINT('Ctrl Pts',(201.46028820531,11.3803838628948,30.6160086090594));
#73034=CARTESIAN_POINT('Ctrl Pts',(201.456244397918,11.432470907913,30.5968750927033));
#73035=CARTESIAN_POINT('Ctrl Pts',(201.447493404416,11.5413341584674,30.5479224979836));
#73036=CARTESIAN_POINT('Ctrl Pts',(201.442793146366,11.5974276542748,30.516988579471));
#73037=CARTESIAN_POINT('Ctrl Pts',(201.437436851325,11.6607878214599,30.4749871619562));
#73038=CARTESIAN_POINT('Ctrl Pts',(201.436594469793,11.6707374998226,30.4681692749309));
#73039=CARTESIAN_POINT('Ctrl Pts',(201.435328286891,11.685694011656,30.4575792562201));
#73040=CARTESIAN_POINT('Ctrl Pts',(201.434897902763,11.6907780517263,30.4539182340482));
#73041=CARTESIAN_POINT('Ctrl Pts',(201.434117162802,11.7000053584495,30.4471611834037));
#73042=CARTESIAN_POINT('Ctrl Pts',(201.433766012383,11.7041576548165,30.4440782849928));
#73043=CARTESIAN_POINT('Ctrl Pts',(201.432955784872,11.7137419336976,30.4368639620695));
#73044=CARTESIAN_POINT('Ctrl Pts',(201.432498061956,11.7191584954838,30.4327125469762));
#73045=CARTESIAN_POINT('Ctrl Pts',(201.431009475686,11.736767603365,30.4189717954543));
#73046=CARTESIAN_POINT('Ctrl Pts',(201.429990830916,11.7488073735372,30.4091882281754));
#73047=CARTESIAN_POINT('Ctrl Pts',(201.427504514035,11.7780513681171,30.3844493067417));
#73048=CARTESIAN_POINT('Ctrl Pts',(201.426050920933,11.7950218120127,30.3692266369248));
#73049=CARTESIAN_POINT('Ctrl Pts',(201.418825676392,11.87800179582,30.2903279381873));
#73050=CARTESIAN_POINT('Ctrl Pts',(201.413286511841,11.9368549665042,30.2195896578896));
#73051=CARTESIAN_POINT('Ctrl Pts',(201.405393041502,12.0047709597261,30.1153064062986));
#73052=CARTESIAN_POINT('Ctrl Pts',(201.403288041948,12.021482877036,30.087144871367));
#73053=CARTESIAN_POINT('Ctrl Pts',(201.400276817889,12.0432584451949,30.0467002885503));
#73054=CARTESIAN_POINT('Ctrl Pts',(201.39940495484,12.049321458575,30.0349708802921));
#73055=CARTESIAN_POINT('Ctrl Pts',(201.397907086474,12.0593188706077,30.0148059549901));
#73056=CARTESIAN_POINT('Ctrl Pts',(201.397284545475,12.0633528893501,30.0064210355883));
#73057=CARTESIAN_POINT('Ctrl Pts',(201.396004583675,12.0713976682063,29.9891795274967));
#73058=CARTESIAN_POINT('Ctrl Pts',(201.395346901066,12.0753989496729,29.9803193342964));
#73059=CARTESIAN_POINT('Ctrl Pts',(201.393672237542,12.0852510767664,29.9577629967835));
#73060=CARTESIAN_POINT('Ctrl Pts',(201.392650390361,12.0909525130591,29.9440038740498));
#73061=CARTESIAN_POINT('Ctrl Pts',(201.387908649118,12.1159822610865,29.8802052438645));
#73062=CARTESIAN_POINT('Ctrl Pts',(201.38408836531,12.1321361753797,29.8289964975176));
#73063=CARTESIAN_POINT('Ctrl Pts',(201.379013107253,12.1485851880693,29.7609869860538));
#73064=CARTESIAN_POINT('Ctrl Pts',(201.377822164519,12.1520959573422,29.745024538644));
#73065=CARTESIAN_POINT('Ctrl Pts',(201.371270938611,12.1695242082937,29.6570993215936));
#73066=CARTESIAN_POINT('Ctrl Pts',(201.365846509798,12.1770332629156,29.5840282430586));
#73067=CARTESIAN_POINT('Ctrl Pts',(201.359641872036,12.1778298736185,29.4965991976671));
#73068=CARTESIAN_POINT('Ctrl Pts',(201.358648162214,12.1777042800285,29.4824658365934));
#73069=CARTESIAN_POINT('Ctrl Pts',(201.357148412728,12.1771239453652,29.4608869623649));
#73070=CARTESIAN_POINT('Ctrl Pts',(201.356633905049,12.1768528487025,29.4534382971488));
#73071=CARTESIAN_POINT('Ctrl Pts',(201.355763601846,12.1762704959815,29.4407522067386));
#73072=CARTESIAN_POINT('Ctrl Pts',(201.35540595734,12.1759949284964,29.4355134641921));
#73073=CARTESIAN_POINT('Ctrl Pts',(201.35465083073,12.1753355889074,29.4243956227917));
#73074=CARTESIAN_POINT('Ctrl Pts',(201.354253833354,12.1749426989966,29.4185173258228));
#73075=CARTESIAN_POINT('Ctrl Pts',(201.353148673834,12.1737192878163,29.4020688662455));
#73076=CARTESIAN_POINT('Ctrl Pts',(201.352445587332,12.1727900976472,29.391506316014));
#73077=CARTESIAN_POINT('Ctrl Pts',(201.350854026918,12.1703423423246,29.3674134472792));
#73078=CARTESIAN_POINT('Ctrl Pts',(201.349969715226,12.1687315426173,29.353893852848));
#73079=CARTESIAN_POINT('Ctrl Pts',(201.34699754887,12.1624734799147,29.3081378239526));
#73080=CARTESIAN_POINT('Ctrl Pts',(201.344949057344,12.1567235719836,29.276065773533));
#73081=CARTESIAN_POINT('Ctrl Pts',(201.336773311026,12.1282519611206,29.1480690286486));
#73082=CARTESIAN_POINT('Ctrl Pts',(201.330786981782,12.0948649423851,29.0549408565797));
#73083=CARTESIAN_POINT('Ctrl Pts',(201.323226871369,12.0420926889981,28.9509421419043));
#73084=CARTESIAN_POINT('Ctrl Pts',(201.322044160784,12.0335448886444,28.9350162733253));
#73085=CARTESIAN_POINT('Ctrl Pts',(201.320156042155,12.0194692232059,28.9101802775707));
#73086=CARTESIAN_POINT('Ctrl Pts',(201.319459065865,12.0141828299515,28.9011360941359));
#73087=CARTESIAN_POINT('Ctrl Pts',(201.318150026819,12.0040912363104,28.8843878896256));
#73088=CARTESIAN_POINT('Ctrl Pts',(201.317539078791,11.9993162007732,28.8766665384385));
#73089=CARTESIAN_POINT('Ctrl Pts',(201.316147596791,11.9882972248495,28.8593006567634));
#73090=CARTESIAN_POINT('Ctrl Pts',(201.315365184199,11.982000542372,28.8496908644555));
#73091=CARTESIAN_POINT('Ctrl Pts',(201.312940548797,11.9621861421804,28.8203948766583));
#73092=CARTESIAN_POINT('Ctrl Pts',(201.311281651661,11.9482102224543,28.8010275190197));
#73093=CARTESIAN_POINT('Ctrl Pts',(201.307283867745,11.9135638720506,28.755968661839));
#73094=CARTESIAN_POINT('Ctrl Pts',(201.304927897913,11.8923849995774,28.730694935336));
#73095=CARTESIAN_POINT('Ctrl Pts',(201.299172823292,11.8387511730918,28.6718900263226));
#73096=CARTESIAN_POINT('Ctrl Pts',(201.295750278093,11.805309367304,28.6393339154061));
#73097=CARTESIAN_POINT('Ctrl Pts',(201.288466081575,11.7301155866324,28.574360426116));
#73098=CARTESIAN_POINT('Ctrl Pts',(201.284613343666,11.6879281734789,28.542590367015));
#73099=CARTESIAN_POINT('Ctrl Pts',(201.280012116475,11.633282144719,28.5069214373652));
#73100=CARTESIAN_POINT('Ctrl Pts',(201.279138643055,11.6227062379737,28.5002558936441));
#73101=CARTESIAN_POINT('Ctrl Pts',(201.277841237762,11.6066637765065,28.4904983847786));
#73102=CARTESIAN_POINT('Ctrl Pts',(201.277410066887,11.6012757070054,28.487279911585));
#73103=CARTESIAN_POINT('Ctrl Pts',(201.276631973568,11.5914445068039,28.4815135318708));
#73104=CARTESIAN_POINT('Ctrl Pts',(201.276284209448,11.5870102591065,28.4789513978604));
#73105=CARTESIAN_POINT('Ctrl Pts',(201.275480276416,11.5766670445097,28.4730646831912));
#73106=CARTESIAN_POINT('Ctrl Pts',(201.275025456543,11.57074589883,28.469762090791));
#73107=CARTESIAN_POINT('Ctrl Pts',(201.273556932732,11.5514143989914,28.459197529091));
#73108=CARTESIAN_POINT('Ctrl Pts',(201.272554997358,11.5378908723992,28.4521445307378));
#73109=CARTESIAN_POINT('Ctrl Pts',(201.265967158782,11.4470592720983,28.4069947432926));
#73110=CARTESIAN_POINT('Ctrl Pts',(201.260739134868,11.365899126778,28.3772160635964));
#73111=CARTESIAN_POINT('Ctrl Pts',(201.251844010635,11.2271299694692,28.3429669841012));
#73112=CARTESIAN_POINT('Ctrl Pts',(201.248269598779,11.1711480511288,28.3333720983529));
#73113=CARTESIAN_POINT('Ctrl Pts',(201.24356923747,11.0994158996172,28.3263529986118));
#73114=CARTESIAN_POINT('Ctrl Pts',(201.242559613089,11.0841077992264,28.3251567560074));
#73115=CARTESIAN_POINT('Ctrl Pts',(201.240889581241,11.0589826527097,28.3236869251502));
#73116=CARTESIAN_POINT('Ctrl Pts',(201.240234634754,11.0491775394609,28.3232362330219));
#73117=CARTESIAN_POINT('Ctrl Pts',(201.238947983311,11.030017432227,28.3225954176414));
#73118=CARTESIAN_POINT('Ctrl Pts',(201.238316670836,11.0206635277601,28.3223941207709));
#73119=CARTESIAN_POINT('Ctrl Pts',(201.236802655575,10.9983498961897,28.3221798613185));
#73120=CARTESIAN_POINT('Ctrl Pts',(201.235916886265,10.9853906440994,28.3222693238348));
#73121=CARTESIAN_POINT('Ctrl Pts',(201.232723091143,10.9390208556698,28.3233548597041));
#73122=CARTESIAN_POINT('Ctrl Pts',(201.230379165481,10.9056573083935,28.3255591434639));
#73123=CARTESIAN_POINT('Ctrl Pts',(201.224052454285,10.8173596809428,28.3351794543637));
#73124=CARTESIAN_POINT('Ctrl Pts',(201.220010502055,10.762780938074,28.3450582422521));
#73125=CARTESIAN_POINT('Ctrl Pts',(201.211258505371,10.6471023444632,28.37454347029));
#73126=CARTESIAN_POINT('Ctrl Pts',(201.206555322366,10.5864856007286,28.3953750237505));
#73127=CARTESIAN_POINT('Ctrl Pts',(201.201196459391,10.5168103299881,28.4258639694471));
#73128=CARTESIAN_POINT('Ctrl Pts',(201.200354201222,10.5058375778034,28.4308676426956));
#73129=CARTESIAN_POINT('Ctrl Pts',(201.19908816495,10.4892839566599,28.4387255641742));
#73130=CARTESIAN_POINT('Ctrl Pts',(201.198657806269,10.4836461688041,28.4414571191947));
#73131=CARTESIAN_POINT('Ctrl Pts',(201.1978770897,10.4733941885005,28.4465256866687));
#73132=CARTESIAN_POINT('Ctrl Pts',(201.197525937561,10.4687733628306,28.448848216792));
#73133=CARTESIAN_POINT('Ctrl Pts',(201.196715677012,10.4580903152521,28.4543061961582));
#73134=CARTESIAN_POINT('Ctrl Pts',(201.196257923197,10.452039848233,28.4574639980012));
#73135=CARTESIAN_POINT('Ctrl Pts',(201.19476912224,10.432326330276,28.4679717282163));
#73136=CARTESIAN_POINT('Ctrl Pts',(201.193750298548,10.4187804081867,28.4755393663561));
#73137=CARTESIAN_POINT('Ctrl Pts',(201.191263439141,10.3857088674029,28.4948825062888));
#73138=CARTESIAN_POINT('Ctrl Pts',(201.18980949043,10.3663676710592,28.5069617510702));
#73139=CARTESIAN_POINT('Ctrl Pts',(201.182579463854,10.2709879025143,28.5704518274736));
#73140=CARTESIAN_POINT('Ctrl Pts',(201.177036154116,10.2007937373166,28.6300638566814));
#73141=CARTESIAN_POINT('Ctrl Pts',(201.169141401909,10.1159590098412,28.7211326861858));
#73142=CARTESIAN_POINT('Ctrl Pts',(201.167040102228,10.0946929720052,28.7459564573821));
#73143=CARTESIAN_POINT('Ctrl Pts',(201.164033289955,10.0663277279381,28.7819991352735));
#73144=CARTESIAN_POINT('Ctrl Pts',(201.163161999316,10.0583428892701,28.7925036986413));
#73145=CARTESIAN_POINT('Ctrl Pts',(201.161664806267,10.0450318712351,28.810639800074));
#73146=CARTESIAN_POINT('Ctrl Pts',(201.161042360163,10.0396164721958,28.8182045149888));
#73147=CARTESIAN_POINT('Ctrl Pts',(201.159762321224,10.0287250994101,28.8338058175555));
#73148=CARTESIAN_POINT('Ctrl Pts',(201.159104463604,10.0232579228957,28.8418476419992));
#73149=CARTESIAN_POINT('Ctrl Pts',(201.157428781072,10.0096644400586,28.8623851463101));
#73150=CARTESIAN_POINT('Ctrl Pts',(201.156406077854,10.0016748186599,28.8749687846016));
#73151=CARTESIAN_POINT('Ctrl Pts',(201.1516502623,9.965940543406,28.933683988276));
#73152=CARTESIAN_POINT('Ctrl Pts',(201.147815996433,9.94114400401658,28.9815259589734));
#73153=CARTESIAN_POINT('Ctrl Pts',(201.141216324113,9.90490749591627,29.0649733195644));
#73154=CARTESIAN_POINT('Ctrl Pts',(201.138492222391,9.8917287098359,29.0997371158308));
#73155=CARTESIAN_POINT('Ctrl Pts',(201.131710446974,9.86306996553872,29.1876748563525));
#73156=CARTESIAN_POINT('Ctrl Pts',(201.127658525455,9.84965186003018,29.2414326784359));
#73157=CARTESIAN_POINT('Ctrl Pts',(201.122789792463,9.83771537926866,29.3092826729482));
#73158=CARTESIAN_POINT('Ctrl Pts',(201.121841224332,9.83559814392707,29.322666996057));
#73159=CARTESIAN_POINT('Ctrl Pts',(201.120456024267,9.83281099339859,29.3424981917767));
#73160=CARTESIAN_POINT('Ctrl Pts',(201.12001070515,9.83196261412641,29.3489183439737));
#73161=CARTESIAN_POINT('Ctrl Pts',(201.119215656273,9.8305333574789,29.3604669671642));
#73162=CARTESIAN_POINT('Ctrl Pts',(201.118864938291,9.82993318506185,29.365592610796));
#73163=CARTESIAN_POINT('Ctrl Pts',(201.118176884112,9.82881593833743,29.3757094893251));
#73164=CARTESIAN_POINT('Ctrl Pts',(201.117839437719,9.82829705199674,29.3807002043782));
#73165=CARTESIAN_POINT('Ctrl Pts',(201.117064830852,9.82717379658595,29.3922190304139));
#73166=CARTESIAN_POINT('Ctrl Pts',(201.116628827027,9.82659200228432,29.3987492403682));
#73167=CARTESIAN_POINT('Ctrl Pts',(201.115395904236,9.82509240713505,29.4173356485609));
#73168=CARTESIAN_POINT('Ctrl Pts',(201.114605096929,9.82430565885677,29.4294019282801));
#73169=CARTESIAN_POINT('Ctrl Pts',(201.112573089147,9.82274800621775,29.4607111913763));
#73170=CARTESIAN_POINT('Ctrl Pts',(201.111342978938,9.8222629626427,29.4799650731109));
#73171=CARTESIAN_POINT('Ctrl Pts',(201.110124610169,9.82225025635667,29.4992229233845));
#73172=CARTESIAN_POINT('Ctrl Pts',(201.110124713057,9.82225025743081,29.4992212971066));
#73173=CARTESIAN_POINT('Ctrl Pts',(201.104151888081,9.82218783691321,29.5936292531427));
#73174=CARTESIAN_POINT('Ctrl Pts',(201.098460114152,9.83347653828057,29.6877030432394));
#73175=CARTESIAN_POINT('Ctrl Pts',(201.090358931108,9.86377767613873,29.8117737585436));
#73176=CARTESIAN_POINT('Ctrl Pts',(201.088216876693,9.87304639088254,29.8437721711053));
#73177=CARTESIAN_POINT('Ctrl Pts',(201.08518348506,9.88778237809044,29.8876010103538));
#73178=CARTESIAN_POINT('Ctrl Pts',(201.084328321107,9.89210892235285,29.8997998502548));
#73179=CARTESIAN_POINT('Ctrl Pts',(201.082843920557,9.89990683947174,29.9206870379719));
#73180=CARTESIAN_POINT('Ctrl Pts',(201.082217850589,9.90328237405759,29.929410044389));
#73181=CARTESIAN_POINT('Ctrl Pts',(201.080927360193,9.91041430718043,29.9472074703001));
#73182=CARTESIAN_POINT('Ctrl Pts',(201.080262638926,9.91418102266728,29.9562769355842));
#73183=CARTESIAN_POINT('Ctrl Pts',(201.078547179923,9.92413640189605,29.9794257922263));
#73184=CARTESIAN_POINT('Ctrl Pts',(201.077491086649,9.93048805947844,29.9934326120486));
#73185=CARTESIAN_POINT('Ctrl Pts',(201.072441890579,9.96188800024985,30.0592199816247));
#73186=CARTESIAN_POINT('Ctrl Pts',(201.068332657324,9.99042988014662,30.1092372043916));
#73187=CARTESIAN_POINT('Ctrl Pts',(201.060922689542,10.0472623805589,30.1937980300933));
#73188=CARTESIAN_POINT('Ctrl Pts',(201.05766110407,10.0740622414228,30.2291763656033));
#73189=CARTESIAN_POINT('Ctrl Pts',(201.054417864302,10.1027692940023,30.2629365128992));
#73190=CARTESIAN_POINT('',(201.01213288523,9.8222500132958,29.5001769696233));
#73191=CARTESIAN_POINT('Ctrl Pts',(200.956011803843,10.1027690874833,30.2629362700282));
#73192=CARTESIAN_POINT('Ctrl Pts',(200.959190471249,10.0722756306458,30.2270752509904));
#73193=CARTESIAN_POINT('Ctrl Pts',(200.962369138654,10.043969850099,30.1894237375346));
#73194=CARTESIAN_POINT('Ctrl Pts',(200.965547806059,10.0180504941751,30.1502847303376));
#73195=CARTESIAN_POINT('Ctrl Pts',(200.968724905787,9.99214392133812,30.1111650259864));
#73196=CARTESIAN_POINT('Ctrl Pts',(200.971902005515,9.96862164118809,30.0705598070775));
#73197=CARTESIAN_POINT('Ctrl Pts',(200.975079105243,9.94763539218599,30.028794662152));
#73198=CARTESIAN_POINT('Ctrl Pts',(200.97846066285,9.92529860202408,29.9843417788288));
#73199=CARTESIAN_POINT('Ctrl Pts',(200.981842220457,9.9057468437586,29.9384012012819));
#73200=CARTESIAN_POINT('Ctrl Pts',(200.985223778064,9.88916484957826,29.8913314849172));
#73201=CARTESIAN_POINT('Ctrl Pts',(200.988597235419,9.87262257624429,29.8443745203092));
#73202=CARTESIAN_POINT('Ctrl Pts',(200.991970692773,9.8590360828417,29.796294207783));
#73203=CARTESIAN_POINT('Ctrl Pts',(200.995344150128,9.84854292882478,29.7474705553002));
#73204=CARTESIAN_POINT('Ctrl Pts',(200.998706501391,9.83808432035578,29.6988076399821));
#73205=CARTESIAN_POINT('Ctrl Pts',(201.002068852654,9.83069888325395,29.6494066876973));
#73206=CARTESIAN_POINT('Ctrl Pts',(201.005431203917,9.82647429469484,29.5996618356646));
#73207=CARTESIAN_POINT('Ctrl Pts',(201.007665097688,9.82366754390407,29.566612131338));
#73208=CARTESIAN_POINT('Ctrl Pts',(201.009898991459,9.82225500706502,29.533410987548));
#73209=CARTESIAN_POINT('Ctrl Pts',(201.01213288523,9.8222500132958,29.5001769696233));
#73210=CARTESIAN_POINT('Ctrl Pts',(201.012132885264,9.82225001329572,29.5001769691125));
#73211=CARTESIAN_POINT('Ctrl Pts',(201.015413022268,9.82224268071789,29.4513778124986));
#73212=CARTESIAN_POINT('Ctrl Pts',(201.018693159271,9.82527259804305,29.4026201959092));
#73213=CARTESIAN_POINT('Ctrl Pts',(201.021973296275,9.83129844917431,29.3542888213018));
#73214=CARTESIAN_POINT('Ctrl Pts',(201.025261094398,9.83733837434069,29.3058445634769));
#73215=CARTESIAN_POINT('Ctrl Pts',(201.028548892521,9.84638813450003,29.2578290295261));
#73216=CARTESIAN_POINT('Ctrl Pts',(201.031836690643,9.85835498925079,29.2106183628296));
#73217=CARTESIAN_POINT('Ctrl Pts',(201.035128826312,9.87033763170422,29.1633454117663));
#73218=CARTESIAN_POINT('Ctrl Pts',(201.03842096198,9.88524487952968,29.1168799161247));
#73219=CARTESIAN_POINT('Ctrl Pts',(201.041713097649,9.90293469427636,29.0715810724565));
#73220=CARTESIAN_POINT('Ctrl Pts',(201.045013366669,9.92066821241159,29.0261703161995));
#73221=CARTESIAN_POINT('Ctrl Pts',(201.048313635689,9.94119781207875,28.9819324175217));
#73222=CARTESIAN_POINT('Ctrl Pts',(201.05161390471,9.96433457710791,28.9392039637036));
#73223=CARTESIAN_POINT('Ctrl Pts',(201.052319604466,9.9692819342293,28.9300672965846));
#73224=CARTESIAN_POINT('Ctrl Pts',(201.053025304222,9.97434834264665,28.9209995417588));
#73225=CARTESIAN_POINT('Ctrl Pts',(201.053731003978,9.97953170284227,28.9120038120906));
#73226=CARTESIAN_POINT('Ctrl Pts',(201.057008166425,10.0036024400579,28.8702290102759));
#73227=CARTESIAN_POINT('Ctrl Pts',(201.060285328873,10.0302968970173,28.8298404704134));
#73228=CARTESIAN_POINT('Ctrl Pts',(201.06356249132,10.0594276106822,28.7911850432214));
#73229=CARTESIAN_POINT('Ctrl Pts',(201.066736443651,10.0876408891035,28.7537470201642));
#73230=CARTESIAN_POINT('Ctrl Pts',(201.069910395983,10.1181388718815,28.7179350402314));
#73231=CARTESIAN_POINT('Ctrl Pts',(201.073084348314,10.1507054735937,28.6840380707923));
#73232=CARTESIAN_POINT('Ctrl Pts',(201.076255175683,10.1832400113639,28.650174475129));
#73233=CARTESIAN_POINT('Ctrl Pts',(201.079426003052,10.2178387525764,28.6182225577383));
#73234=CARTESIAN_POINT('Ctrl Pts',(201.08259683042,10.2542458351852,28.5884377211834));
#73235=CARTESIAN_POINT('Ctrl Pts',(201.085765927365,10.2906330492674,28.5586691391804));
#73236=CARTESIAN_POINT('Ctrl Pts',(201.088935024311,10.328826219401,28.5310656471142));
#73237=CARTESIAN_POINT('Ctrl Pts',(201.092104121256,10.3685351866865,28.5058434469125));
#73238=CARTESIAN_POINT('Ctrl Pts',(201.095272879319,10.4082399077559,28.4806239438071));
#73239=CARTESIAN_POINT('Ctrl Pts',(201.098441637381,10.4494596331683,28.4577855234577));
#73240=CARTESIAN_POINT('Ctrl Pts',(201.101610395444,10.4918761932964,28.437500466089));
#73241=CARTESIAN_POINT('Ctrl Pts',(201.10478233988,10.5343354057729,28.4171950109009));
#73242=CARTESIAN_POINT('Ctrl Pts',(201.107954284315,10.5779933502418,28.3994482803588));
#73243=CARTESIAN_POINT('Ctrl Pts',(201.111126228751,10.622510093867,28.3843851770133));
#73244=CARTESIAN_POINT('Ctrl Pts',(201.114300118021,10.6670541323296,28.3693128379303));
#73245=CARTESIAN_POINT('Ctrl Pts',(201.117474007291,10.7124574804751,28.3569275468502));
#73246=CARTESIAN_POINT('Ctrl Pts',(201.120647896562,10.7583666920129,28.3473038531464));
#73247=CARTESIAN_POINT('Ctrl Pts',(201.12382740104,10.8043571255972,28.3376631333148));
#73248=CARTESIAN_POINT('Ctrl Pts',(201.127006905519,10.8508546571298,28.330793834172));
#73249=CARTESIAN_POINT('Ctrl Pts',(201.130186409997,10.8974993081254,28.3267188441532));
#73250=CARTESIAN_POINT('Ctrl Pts',(201.130918574235,10.9082404615346,28.3257804708993));
#73251=CARTESIAN_POINT('Ctrl Pts',(201.131650738474,10.9189894168709,28.3249900534933));
#73252=CARTESIAN_POINT('Ctrl Pts',(201.132382902712,10.9297417918825,28.3243474804637));
#73253=CARTESIAN_POINT('Ctrl Pts',(201.135660065159,10.9778693536535,28.3214713276933));
#73254=CARTESIAN_POINT('Ctrl Pts',(201.138937227607,11.026282390912,28.3215488389594));
#73255=CARTESIAN_POINT('Ctrl Pts',(201.142214390054,11.0745881236887,28.3246142444692));
#73256=CARTESIAN_POINT('Ctrl Pts',(201.145388342385,11.1213725280764,28.3275831088823));
#73257=CARTESIAN_POINT('Ctrl Pts',(201.148562294717,11.1680556831734,28.333354407741));
#73258=CARTESIAN_POINT('Ctrl Pts',(201.151736247049,11.2142774053045,28.3419066289474));
#73259=CARTESIAN_POINT('Ctrl Pts',(201.154907074417,11.2604536191376,28.3504504299347));
#73260=CARTESIAN_POINT('Ctrl Pts',(201.158077901786,11.3061687540886,28.3617696328631));
#73261=CARTESIAN_POINT('Ctrl Pts',(201.161248729155,11.3510687782139,28.3757910445725));
#73262=CARTESIAN_POINT('Ctrl Pts',(201.1644178261,11.3959442989388,28.3898048043425));
#73263=CARTESIAN_POINT('Ctrl Pts',(201.167586923045,11.4400050594317,28.4065176857212));
#73264=CARTESIAN_POINT('Ctrl Pts',(201.17075601999,11.4829109002926,28.4258062908029));
#73265=CARTESIAN_POINT('Ctrl Pts',(201.173924778053,11.5258121530849,28.445092833288));
#73266=CARTESIAN_POINT('Ctrl Pts',(201.177093536116,11.5675582247912,28.4669543223567));
#73267=CARTESIAN_POINT('Ctrl Pts',(201.180262294179,11.6078302289611,28.491219808253));
#73268=CARTESIAN_POINT('Ctrl Pts',(201.183434238615,11.648142729002,28.5155096945239));
#73269=CARTESIAN_POINT('Ctrl Pts',(201.18660618305,11.6869777274219,28.5422081112936));
#73270=CARTESIAN_POINT('Ctrl Pts',(201.189778127486,11.724043933369,28.5710998734786));
#73271=CARTESIAN_POINT('Ctrl Pts',(201.192952016756,11.7611328659576,28.6000093502557));
#73272=CARTESIAN_POINT('Ctrl Pts',(201.196125906026,11.7964504300725,28.631114480428));
#73273=CARTESIAN_POINT('Ctrl Pts',(201.199299795297,11.8297399531936,28.6641610965178));
#73274=CARTESIAN_POINT('Ctrl Pts',(201.202479299775,11.8630883717543,28.6972661782989));
#73275=CARTESIAN_POINT('Ctrl Pts',(201.205658804254,11.89440122465,28.7323191803524));
#73276=CARTESIAN_POINT('Ctrl Pts',(201.208838308733,11.9234613899029,28.7690320637275));
#73277=CARTESIAN_POINT('Ctrl Pts',(201.20957047297,11.9301532545904,28.7774861673327));
#73278=CARTESIAN_POINT('Ctrl Pts',(201.210302637208,11.9367258483966,28.7860281700837));
#73279=CARTESIAN_POINT('Ctrl Pts',(201.211034801446,11.9431768539451,28.7946543509157));
#73280=CARTESIAN_POINT('Ctrl Pts',(201.214311963893,11.9720515135337,28.8332650811653));
#73281=CARTESIAN_POINT('Ctrl Pts',(201.217589126341,11.9986165065409,28.8737388916002));
#73282=CARTESIAN_POINT('Ctrl Pts',(201.220866288788,12.0226271965887,28.9157665883424));
#73283=CARTESIAN_POINT('Ctrl Pts',(201.224040241119,12.045881700107,28.9564706755556));
#73284=CARTESIAN_POINT('Ctrl Pts',(201.227214193451,12.0667401143642,28.9986316932728));
#73285=CARTESIAN_POINT('Ctrl Pts',(201.230388145782,12.0850222847301,29.0419370085468));
#73286=CARTESIAN_POINT('Ctrl Pts',(201.233558973151,12.1032864551077,29.0851996869154));
#73287=CARTESIAN_POINT('Ctrl Pts',(201.23672980052,12.1189791866155,29.129603922032));
#73288=CARTESIAN_POINT('Ctrl Pts',(201.239900627888,12.131966868801,29.1748137911335));
#73289=CARTESIAN_POINT('Ctrl Pts',(201.243069724834,12.1449474631867,29.2199989877421));
#73290=CARTESIAN_POINT('Ctrl Pts',(201.246238821779,12.155225779285,29.2659884130192));
#73291=CARTESIAN_POINT('Ctrl Pts',(201.249407918724,12.1627177647587,29.3124301143186));
#73292=CARTESIAN_POINT('Ctrl Pts',(201.252576676787,12.1702089490887,29.3588668494477));
#73293=CARTESIAN_POINT('Ctrl Pts',(201.25574543485,12.1749143079762,29.4057552147945));
#73294=CARTESIAN_POINT('Ctrl Pts',(201.258914192912,12.1768012023009,29.4527348673623));
#73295=CARTESIAN_POINT('Ctrl Pts',(201.262086137348,12.1786899940089,29.4997617607366));
#73296=CARTESIAN_POINT('Ctrl Pts',(201.265258081784,12.1777546460219,29.5468795671834));
#73297=CARTESIAN_POINT('Ctrl Pts',(201.268430026219,12.1740146404998,29.593726657852));
#73298=CARTESIAN_POINT('Ctrl Pts',(201.271603915489,12.1702723418441,29.6406024721788));
#73299=CARTESIAN_POINT('Ctrl Pts',(201.27477780476,12.1637220412537,29.6872066889426));
#73300=CARTESIAN_POINT('Ctrl Pts',(201.27795169403,12.1544348181607,29.7331851477225));
#73301=CARTESIAN_POINT('Ctrl Pts',(201.281131198509,12.1451311642198,29.7792449510604));
#73302=CARTESIAN_POINT('Ctrl Pts',(201.284310702987,12.133081075288,29.8246762515713));
#73303=CARTESIAN_POINT('Ctrl Pts',(201.287490207466,12.1184056727622,29.8691392875775));
#73304=CARTESIAN_POINT('Ctrl Pts',(201.288222371704,12.1150262767015,29.8793780669544));
#73305=CARTESIAN_POINT('Ctrl Pts',(201.288954535942,12.1115078681575,29.8895655888197));
#73306=CARTESIAN_POINT('Ctrl Pts',(201.28968670018,12.1078522800235,29.8996978710812));
#73307=CARTESIAN_POINT('Ctrl Pts',(201.292963862627,12.0914898909157,29.9450499016802));
#73308=CARTESIAN_POINT('Ctrl Pts',(201.296241025075,12.0723011493438,29.9894978530556));
#73309=CARTESIAN_POINT('Ctrl Pts',(201.299518187522,12.0504097094453,30.0326673491055));
#73310=CARTESIAN_POINT('Ctrl Pts',(201.302692139854,12.0292077129543,30.0744772760912));
#73311=CARTESIAN_POINT('Ctrl Pts',(201.305866092185,12.0054710147095,30.1150875459341));
#73312=CARTESIAN_POINT('Ctrl Pts',(201.309040044517,11.9793616092817,30.1541757414986));
#73313=CARTESIAN_POINT('Ctrl Pts',(201.312210871885,11.9532779102652,30.1932254521868));
#73314=CARTESIAN_POINT('Ctrl Pts',(201.315381699254,11.9248264360125,30.2307555938241));
#73315=CARTESIAN_POINT('Ctrl Pts',(201.318552526623,11.8942142328695,30.2664698090816));
#73316=CARTESIAN_POINT('Ctrl Pts',(201.321721623568,11.8636187357993,30.3021645339328));
#73317=CARTESIAN_POINT('Ctrl Pts',(201.324890720513,11.8308652076759,30.3360448735801));
#73318=CARTESIAN_POINT('Ctrl Pts',(201.328059817458,11.7962013414586,30.3678470408774));
#73319=CARTESIAN_POINT('Ctrl Pts',(201.331228575521,11.7615411819674,30.3996458074597));
#73320=CARTESIAN_POINT('Ctrl Pts',(201.334397333584,11.7249715015898,30.429366468358));
#73321=CARTESIAN_POINT('Ctrl Pts',(201.337566091647,11.6867752802996,30.4567835580054));
#73322=CARTESIAN_POINT('Ctrl Pts',(201.340738036083,11.6485406504601,30.4842282171506));
#73323=CARTESIAN_POINT('Ctrl Pts',(201.343909980518,11.6086766705483,30.5093643597709));
#73324=CARTESIAN_POINT('Ctrl Pts',(201.347081924954,11.5674960638477,30.5320093410514));
#73325=CARTESIAN_POINT('Ctrl Pts',(201.350255814224,11.5262902078167,30.5546682067951));
#73326=CARTESIAN_POINT('Ctrl Pts',(201.353429703494,11.4837666218053,30.5748326331628));
#73327=CARTESIAN_POINT('Ctrl Pts',(201.356603592765,11.44026017321,30.5923671737951));
#73328=CARTESIAN_POINT('Ctrl Pts',(201.359783097243,11.3966767535084,30.6099327363342));
#73329=CARTESIAN_POINT('Ctrl Pts',(201.362962601722,11.352107531153,30.6248589591658));
#73330=CARTESIAN_POINT('Ctrl Pts',(201.366142106201,11.3069028744401,30.6370601075407));
#73331=CARTESIAN_POINT('Ctrl Pts',(201.366874270439,11.296493317459,30.639869741735));
#73332=CARTESIAN_POINT('Ctrl Pts',(201.367606434677,11.2860501029579,30.6425350881116));
#73333=CARTESIAN_POINT('Ctrl Pts',(201.368338598915,11.2755775646891,30.6450554870136));
#73334=CARTESIAN_POINT('Ctrl Pts',(201.371615761362,11.2287025503744,30.6563367763801));
#73335=CARTESIAN_POINT('Ctrl Pts',(201.374892923809,11.1810279166683,30.6647604030086));
#73336=CARTESIAN_POINT('Ctrl Pts',(201.378170086257,11.1329343325491,30.6702237075575));
#73337=CARTESIAN_POINT('Ctrl Pts',(201.381344038588,11.0863553954637,30.6755149521908));
#73338=CARTESIAN_POINT('Ctrl Pts',(201.38451799092,11.0393841082258,30.6780295168643));
#73339=CARTESIAN_POINT('Ctrl Pts',(201.387691943251,10.9923788365881,30.6777253416515));
#73340=CARTESIAN_POINT('Ctrl Pts',(201.39086277062,10.9454198447041,30.6774214659191));
#73341=CARTESIAN_POINT('Ctrl Pts',(201.394033597989,10.8984274890609,30.674304347124));
#73342=CARTESIAN_POINT('Ctrl Pts',(201.397204425357,10.8517631529411,30.6683838836932));
#73343=CARTESIAN_POINT('Ctrl Pts',(201.400373522303,10.805124283064,30.6624666512515));
#73344=CARTESIAN_POINT('Ctrl Pts',(201.403542619248,10.758813629581,30.6537491749466));
#73345=CARTESIAN_POINT('Ctrl Pts',(201.406711716193,10.7131877332229,30.6422932137268));
#73346=CARTESIAN_POINT('Ctrl Pts',(201.409880474256,10.6675667157985,30.6308384775321));
#73347=CARTESIAN_POINT('Ctrl Pts',(201.413049232319,10.6226308493316,30.6166459755668));
#73348=CARTESIAN_POINT('Ctrl Pts',(201.416217990381,10.5787240807764,30.5998280149106));
#73349=CARTESIAN_POINT('Ctrl Pts',(201.419389934817,10.5347731613804,30.582993142805));
#73350=CARTESIAN_POINT('Ctrl Pts',(201.422561879253,10.4918539246562,30.5635277458337));
#73351=CARTESIAN_POINT('Ctrl Pts',(201.425733823688,10.4502909170569,30.5415925242771));
#73352=CARTESIAN_POINT('Ctrl Pts',(201.428907712959,10.4087024256632,30.5196438534368));
#73353=CARTESIAN_POINT('Ctrl Pts',(201.432081602229,10.368472294167,30.4952226336101));
#73354=CARTESIAN_POINT('Ctrl Pts',(201.435255491499,10.3298978326106,30.4685340199291));
#73355=CARTESIAN_POINT('Ctrl Pts',(201.438434995978,10.2912551255625,30.4417981890611));
#73356=CARTESIAN_POINT('Ctrl Pts',(201.441614500456,10.2542743665554,30.4127873088151));
#73357=CARTESIAN_POINT('Ctrl Pts',(201.444794004935,10.2192198762922,30.3817468235967));
#73358=CARTESIAN_POINT('Ctrl Pts',(201.445526169173,10.2111476611634,30.3745989383328));
#73359=CARTESIAN_POINT('Ctrl Pts',(201.446258333411,10.203177431694,30.3673435787545));
#73360=CARTESIAN_POINT('Ctrl Pts',(201.446990497649,10.1953121225757,30.3599840012619));
#73361=CARTESIAN_POINT('Ctrl Pts',(201.450023747427,10.1627272926992,30.3294943438368));
#73362=CARTESIAN_POINT('Ctrl Pts',(201.453056997205,10.1317989100048,30.2970760208492));
#73363=CARTESIAN_POINT('Ctrl Pts',(201.456090246984,10.1027690874833,30.2629362700282));
#73364=CARTESIAN_POINT('Origin',(197.762132885264,11.,29.5));
#73365=CARTESIAN_POINT('',(202.054067314992,10.1027691090856,30.2629362954329));
#73366=CARTESIAN_POINT('',(201.956062524555,10.1027690874833,30.2629362700282));
#73367=CARTESIAN_POINT('',(197.762132885264,10.1027690874833,30.2629362700282));
#73368=CARTESIAN_POINT('Ctrl Pts',(202.054067314992,10.1027691090856,30.2629362954329));
#73369=CARTESIAN_POINT('Ctrl Pts',(202.047604320826,10.1692854702585,30.3411610887122));
#73370=CARTESIAN_POINT('Ctrl Pts',(202.041419150576,10.2457670530881,30.4103772800603));
#73371=CARTESIAN_POINT('Ctrl Pts',(202.033298780019,10.3497453620161,30.482254088737));
#73372=CARTESIAN_POINT('Ctrl Pts',(202.031762106183,10.3695956478954,30.4951102566408));
#73373=CARTESIAN_POINT('Ctrl Pts',(202.029449713983,10.3996093949205,30.5132902939744));
#73374=CARTESIAN_POINT('Ctrl Pts',(202.028690518296,10.4094860381672,30.5190776929628));
#73375=CARTESIAN_POINT('Ctrl Pts',(202.027320246648,10.4273411241685,30.5291934860977));
#73376=CARTESIAN_POINT('Ctrl Pts',(202.02671111811,10.435288304298,30.5335754025877));
#73377=CARTESIAN_POINT('Ctrl Pts',(202.025389899221,10.4525419389523,30.5428303203903));
#73378=CARTESIAN_POINT('Ctrl Pts',(202.024676766715,10.461864480563,30.54767149249));
#73379=CARTESIAN_POINT('Ctrl Pts',(202.022715639286,10.487519976455,30.5605615547266));
#73380=CARTESIAN_POINT('Ctrl Pts',(202.021459201629,10.5039762207167,30.5683571186333));
#73381=CARTESIAN_POINT('Ctrl Pts',(202.014715603041,10.5923578376161,30.6077426043634));
#73382=CARTESIAN_POINT('Ctrl Pts',(202.009007262484,10.6671176615132,30.6324536954834));
#73383=CARTESIAN_POINT('Ctrl Pts',(201.999861081094,10.7888761492997,30.6595937892407));
#73384=CARTESIAN_POINT('Ctrl Pts',(201.996467881437,10.8345403619749,30.6669852233019));
#73385=CARTESIAN_POINT('Ctrl Pts',(201.991379582015,10.9049315607282,30.6741631287229));
#73386=CARTESIAN_POINT('Ctrl Pts',(201.989636245669,10.9294144669434,30.675888997398));
#73387=CARTESIAN_POINT('Ctrl Pts',(201.987365444222,10.9619979569207,30.6771643956317));
#73388=CARTESIAN_POINT('Ctrl Pts',(201.986807326943,10.9700639933086,30.6773971352645));
#73389=CARTESIAN_POINT('Ctrl Pts',(201.985886008559,10.9834855486692,30.6776463837408));
#73390=CARTESIAN_POINT('Ctrl Pts',(201.985520417177,10.9888398392272,30.6777092966193));
#73391=CARTESIAN_POINT('Ctrl Pts',(201.984820686737,10.9991460013706,30.6777600987789));
#73392=CARTESIAN_POINT('Ctrl Pts',(201.984486243844,11.0040976324191,30.6777532811409));
#73393=CARTESIAN_POINT('Ctrl Pts',(201.983565302125,11.0177988477746,30.6776480053991));
#73394=CARTESIAN_POINT('Ctrl Pts',(201.982982270267,11.0265478079249,30.6774832689451));
#73395=CARTESIAN_POINT('Ctrl Pts',(201.98048608091,11.0642849665453,30.6763518657092));
#73396=CARTESIAN_POINT('Ctrl Pts',(201.97861839672,11.0932360963969,30.6744120200369));
#73397=CARTESIAN_POINT('Ctrl Pts',(201.969774122392,11.2319389661801,30.6599558608248));
#73398=CARTESIAN_POINT('Ctrl Pts',(201.963166627069,11.3396324421168,30.6331131497155));
#73399=CARTESIAN_POINT('Ctrl Pts',(201.954551758699,11.4639302367716,30.5827847649107));
#73400=CARTESIAN_POINT('Ctrl Pts',(201.953015188154,11.4855726402678,30.5732535598469));
#73401=CARTESIAN_POINT('Ctrl Pts',(201.950702920697,11.517244745616,30.5581512013742));
#73402=CARTESIAN_POINT('Ctrl Pts',(201.949943743762,11.5275043417661,30.5530741883359));
#73403=CARTESIAN_POINT('Ctrl Pts',(201.948573492258,11.5457621469612,30.5437054653588));
#73404=CARTESIAN_POINT('Ctrl Pts',(201.947964364868,11.5537879206016,30.5394692639389));
#73405=CARTESIAN_POINT('Ctrl Pts',(201.946643132863,11.5709964290611,30.5301303257523));
#73406=CARTESIAN_POINT('Ctrl Pts',(201.94592998591,11.5801613913265,30.5249966623229));
#73407=CARTESIAN_POINT('Ctrl Pts',(201.943968777309,11.6050220390879,30.510630967775));
#73408=CARTESIAN_POINT('Ctrl Pts',(201.942712271764,11.6205736714864,30.5011567687971));
#73409=CARTESIAN_POINT('Ctrl Pts',(201.935970328372,11.7019977138409,30.4489262937548));
#73410=CARTESIAN_POINT('Ctrl Pts',(201.930263870392,11.7636800311644,30.4000282929514));
#73411=CARTESIAN_POINT('Ctrl Pts',(201.921118295787,11.8532150927828,30.3131768532952));
#73412=CARTESIAN_POINT('Ctrl Pts',(201.917723832434,11.8844776970614,30.279058508426));
#73413=CARTESIAN_POINT('Ctrl Pts',(201.912633927381,11.9291404349111,30.2241514782553));
#73414=CARTESIAN_POINT('Ctrl Pts',(201.910890218898,11.9440287093345,30.2046327397892));
#73415=CARTESIAN_POINT('Ctrl Pts',(201.908619018214,11.9629882728012,30.1780956902999));
#73416=CARTESIAN_POINT('Ctrl Pts',(201.908060860826,11.9676118556828,30.1714815593181));
#73417=CARTESIAN_POINT('Ctrl Pts',(201.907139494889,11.9751897873637,30.1604003422456));
#73418=CARTESIAN_POINT('Ctrl Pts',(201.906773895561,11.978182253726,30.1559597672137));
#73419=CARTESIAN_POINT('Ctrl Pts',(201.906074165711,11.9838833958618,30.1473739581172));
#73420=CARTESIAN_POINT('Ctrl Pts',(201.905739731192,11.9865963660816,30.1432318329929));
#73421=CARTESIAN_POINT('Ctrl Pts',(201.904818842101,11.9940307266243,30.1317234572071));
#73422=CARTESIAN_POINT('Ctrl Pts',(201.904235853831,11.9986963911128,30.1243213446484));
#73423=CARTESIAN_POINT('Ctrl Pts',(201.901740218467,12.0184663492074,30.0921673007899));
#73424=CARTESIAN_POINT('Ctrl Pts',(201.899873019277,12.0327374057809,30.0669123042258));
#73425=CARTESIAN_POINT('Ctrl Pts',(201.891028793919,12.0968130081001,29.9430527695842));
#73426=CARTESIAN_POINT('Ctrl Pts',(201.884421002874,12.1335118575356,29.8383012340464));
#73427=CARTESIAN_POINT('Ctrl Pts',(201.87580565366,12.1596976317177,29.7067743291888));
#73428=CARTESIAN_POINT('Ctrl Pts',(201.87426893821,12.1636150592538,29.6834505248178));
#73429=CARTESIAN_POINT('Ctrl Pts',(201.871956495753,12.1683830486066,29.6486847435213));
#73430=CARTESIAN_POINT('Ctrl Pts',(201.871197292512,12.1697729550378,29.637321956628));
#73431=CARTESIAN_POINT('Ctrl Pts',(201.869827012748,12.1719674099389,29.6169179631392));
#73432=CARTESIAN_POINT('Ctrl Pts',(201.869217883747,12.172833497239,29.607884197267));
#73433=CARTESIAN_POINT('Ctrl Pts',(201.867896670141,12.1744766487479,29.5883742357462));
#73434=CARTESIAN_POINT('Ctrl Pts',(201.867183543455,12.1752181151935,29.5778959141664));
#73435=CARTESIAN_POINT('Ctrl Pts',(201.865222448723,12.1768614194645,29.5492318109622));
#73436=CARTESIAN_POINT('Ctrl Pts',(201.863966038411,12.1774818183726,29.5310334640761));
#73437=CARTESIAN_POINT('Ctrl Pts',(201.857221775629,12.1785359029456,29.4342694537427));
#73438=CARTESIAN_POINT('Ctrl Pts',(201.851512679495,12.1715287851462,29.355833786498));
#73439=CARTESIAN_POINT('Ctrl Pts',(201.842366254427,12.1480874499109,29.2333061289548));
#73440=CARTESIAN_POINT('Ctrl Pts',(201.838973561777,12.1367402973589,29.1884678560925));
#73441=CARTESIAN_POINT('Ctrl Pts',(201.833885906584,12.1153800501616,29.1210220266441));
#73442=CARTESIAN_POINT('Ctrl Pts',(201.832142719576,12.107243184764,29.0978685774277));
#73443=CARTESIAN_POINT('Ctrl Pts',(201.829872078345,12.0954765738816,29.0674595486759));
#73444=CARTESIAN_POINT('Ctrl Pts',(201.829313977165,12.0924874723601,29.0599644358746));
#73445=CARTESIAN_POINT('Ctrl Pts',(201.828392677866,12.0873870222569,29.0475475764285));
#73446=CARTESIAN_POINT('Ctrl Pts',(201.828027089674,12.0853187467281,29.0426085330259));
#73447=CARTESIAN_POINT('Ctrl Pts',(201.827327358996,12.0812730920725,29.0331294821189));
#73448=CARTESIAN_POINT('Ctrl Pts',(201.826992912741,12.0793006652321,29.0285875941636));
#73449=CARTESIAN_POINT('Ctrl Pts',(201.826071949894,12.0737635588939,29.0160542923954));
#73450=CARTESIAN_POINT('Ctrl Pts',(201.825488900538,12.0701382928782,29.0080897708088));
#73451=CARTESIAN_POINT('Ctrl Pts',(201.822992488739,12.0541141059541,28.9739012429677));
#73452=CARTESIAN_POINT('Ctrl Pts',(201.82112460981,12.0408365295538,28.9480977777271));
#73453=CARTESIAN_POINT('Ctrl Pts',(201.812280315777,11.9724924757837,28.8265379249276));
#73454=CARTESIAN_POINT('Ctrl Pts',(201.805672939163,11.9050954908719,28.7383588402031));
#73455=CARTESIAN_POINT('Ctrl Pts',(201.797058263843,11.8095516587997,28.6442662914965));
#73456=CARTESIAN_POINT('Ctrl Pts',(201.795521751499,11.7922111113383,28.6281883780274));
#73457=CARTESIAN_POINT('Ctrl Pts',(201.79320955433,11.765775079931,28.6051175412255));
#73458=CARTESIAN_POINT('Ctrl Pts',(201.792450387961,11.7570417936721,28.5977174524661));
#73459=CARTESIAN_POINT('Ctrl Pts',(201.791080147807,11.7411937833177,28.5846808235318));
#73460=CARTESIAN_POINT('Ctrl Pts',(201.790471021064,11.7341190562846,28.5789969475394));
#73461=CARTESIAN_POINT('Ctrl Pts',(201.789149781667,11.7187148100524,28.5669113470457));
#73462=CARTESIAN_POINT('Ctrl Pts',(201.788436626572,11.7103639616308,28.5605382167431));
#73463=CARTESIAN_POINT('Ctrl Pts',(201.786475372225,11.687307325046,28.5434252347977));
#73464=CARTESIAN_POINT('Ctrl Pts',(201.785218828421,11.6724364646892,28.5329137690585));
#73465=CARTESIAN_POINT('Ctrl Pts',(201.778477821833,11.5921799795312,28.4789306773197));
#73466=CARTESIAN_POINT('Ctrl Pts',(201.772772429132,11.5228228254777,28.4417409571442));
#73467=CARTESIAN_POINT('Ctrl Pts',(201.763627197657,11.407565687096,28.394050779051));
#73468=CARTESIAN_POINT('Ctrl Pts',(201.760232018943,11.3638301330806,28.3789016681159));
#73469=CARTESIAN_POINT('Ctrl Pts',(201.755141205018,11.2956911053484,28.3597087112878));
#73470=CARTESIAN_POINT('Ctrl Pts',(201.753397285927,11.271862574244,28.3537939171058));
#73471=CARTESIAN_POINT('Ctrl Pts',(201.751125859302,11.2399757802255,28.3469293998935));
#73472=CARTESIAN_POINT('Ctrl Pts',(201.750567679218,11.2320692096259,28.345312130974));
#73473=CARTESIAN_POINT('Ctrl Pts',(201.749646286374,11.2188896544508,28.3427571329853));
#73474=CARTESIAN_POINT('Ctrl Pts',(201.749280682549,11.2136258672373,28.3417738876973));
#73475=CARTESIAN_POINT('Ctrl Pts',(201.748580953032,11.2034821713149,28.3399506115992));
#73476=CARTESIAN_POINT('Ctrl Pts',(201.748246523249,11.1986034110434,28.3391054031765));
#73477=CARTESIAN_POINT('Ctrl Pts',(201.747325663929,11.1850896448277,28.3368519317845));
#73478=CARTESIAN_POINT('Ctrl Pts',(201.746742700316,11.1764438534976,28.3355090455809));
#73479=CARTESIAN_POINT('Ctrl Pts',(201.744247378285,11.1390879395483,28.3301324408666));
#73480=CARTESIAN_POINT('Ctrl Pts',(201.742380453405,11.1102470027975,28.3270628949147));
#73481=CARTESIAN_POINT('Ctrl Pts',(201.73353625568,10.9711290027812,28.31743427112));
#73482=CARTESIAN_POINT('Ctrl Pts',(201.72692829733,10.8604139469235,28.3253454561834));
#73483=CARTESIAN_POINT('Ctrl Pts',(201.718312676124,10.7292979740445,28.3535381843589));
#73484=CARTESIAN_POINT('Ctrl Pts',(201.716775878743,10.7063348884977,28.3592042405397));
#73485=CARTESIAN_POINT('Ctrl Pts',(201.714463337342,10.6725325493593,28.3686330501083));
#73486=CARTESIAN_POINT('Ctrl Pts',(201.713704119228,10.6615518002158,28.3718692861725));
#73487=CARTESIAN_POINT('Ctrl Pts',(201.712333823487,10.6419536574919,28.3779571144504));
#73488=CARTESIAN_POINT('Ctrl Pts',(201.711724693574,10.6333186558883,28.3807492664827));
#73489=CARTESIAN_POINT('Ctrl Pts',(201.710403490368,10.6147603270199,28.3869879628022));
#73490=CARTESIAN_POINT('Ctrl Pts',(201.709690375138,10.6048491818316,28.3904680179411));
#73491=CARTESIAN_POINT('Ctrl Pts',(201.70772934477,10.5778899510145,28.4003411207563));
#73492=CARTESIAN_POINT('Ctrl Pts',(201.706472988289,10.5609420727921,28.4069974302987));
#73493=CARTESIAN_POINT('Ctrl Pts',(201.699727422266,10.471697163321,28.4444591092895));
#73494=CARTESIAN_POINT('Ctrl Pts',(201.694016843361,10.4024756117815,28.4820455440432));
#73495=CARTESIAN_POINT('Ctrl Pts',(201.68486993985,10.2993270241127,28.5522201876927));
#73496=CARTESIAN_POINT('Ctrl Pts',(201.681478241867,10.26269194068,28.5804314140691));
#73497=CARTESIAN_POINT('Ctrl Pts',(201.676391850609,10.2092860804806,28.6268057140235));
#73498=CARTESIAN_POINT('Ctrl Pts',(201.674648956634,10.1912701038536,28.6434645896286));
#73499=CARTESIAN_POINT('Ctrl Pts',(201.67237862979,10.1680364659596,28.6663352971444));
#73500=CARTESIAN_POINT('Ctrl Pts',(201.671820560203,10.1623447491578,28.6720544411017));
#73501=CARTESIAN_POINT('Ctrl Pts',(201.67089929836,10.1529743245136,28.6816655720861));
#73502=CARTESIAN_POINT('Ctrl Pts',(201.670533716425,10.1492626445055,28.6855249008713));
#73503=CARTESIAN_POINT('Ctrl Pts',(201.669833985278,10.1421692905466,28.6930018246362));
#73504=CARTESIAN_POINT('Ctrl Pts',(201.669499532425,10.1387839261544,28.6966156228104));
#73505=CARTESIAN_POINT('Ctrl Pts',(201.668578528106,10.1294792159885,28.7066745925052));
#73506=CARTESIAN_POINT('Ctrl Pts',(201.667995444401,10.1236086164729,28.7131646985526));
#73507=CARTESIAN_POINT('Ctrl Pts',(201.665498595918,10.0985891738631,28.7414518277028));
#73508=CARTESIAN_POINT('Ctrl Pts',(201.663630334685,10.0801755231633,28.7638885730886));
#73509=CARTESIAN_POINT('Ctrl Pts',(201.654786001899,9.99574773947515,28.8748846540172));
#73510=CARTESIAN_POINT('Ctrl Pts',(201.648178858281,9.9415828047883,28.9717508545302));
#73511=CARTESIAN_POINT('Ctrl Pts',(201.639564561913,9.89316655028268,29.0967957128793));
#73512=CARTESIAN_POINT('Ctrl Pts',(201.638028163855,9.88529655822736,29.1190930553388));
#73513=CARTESIAN_POINT('Ctrl Pts',(201.635716104707,9.87462011352128,29.1525144725769));
#73514=CARTESIAN_POINT('Ctrl Pts',(201.634956959086,9.8712962453129,29.1634678325912));
#73515=CARTESIAN_POINT('Ctrl Pts',(201.633581134087,9.86560107529085,29.1832697842408));
#73516=CARTESIAN_POINT('Ctrl Pts',(201.632966342806,9.8631723337018,29.1921009920791));
#73517=CARTESIAN_POINT('Ctrl Pts',(201.631637182221,9.85817164950415,29.2111503965525));
#73518=CARTESIAN_POINT('Ctrl Pts',(201.630921805251,9.85563335531425,29.221376516513));
#73519=CARTESIAN_POINT('Ctrl Pts',(201.628948054172,9.84904982180014,29.2495090307131));
#73520=CARTESIAN_POINT('Ctrl Pts',(201.627681055577,9.84528564528884,29.2674774580354));
#73521=CARTESIAN_POINT('Ctrl Pts',(201.621361377559,9.82877745453049,29.3566136511067));
#73522=CARTESIAN_POINT('Ctrl Pts',(201.616125382876,9.82218736478418,29.4287520479956));
#73523=CARTESIAN_POINT('Ctrl Pts',(201.605715287031,9.82231138499072,29.570843521344));
#73524=CARTESIAN_POINT('Ctrl Pts',(201.600568081262,9.82858002547111,29.6405204828484));
#73525=CARTESIAN_POINT('Ctrl Pts',(201.594829067043,9.84306271396452,29.7207440406304));
#73526=CARTESIAN_POINT('Ctrl Pts',(201.594012838175,9.84531164554728,29.7322211117353));
#73527=CARTESIAN_POINT('Ctrl Pts',(201.592777789827,9.84901148175518,29.7497174095076));
#73528=CARTESIAN_POINT('Ctrl Pts',(201.592352843163,9.85033943740846,29.7557615077516));
#73529=CARTESIAN_POINT('Ctrl Pts',(201.591577011976,9.85286650159896,29.7668457133549));
#73530=CARTESIAN_POINT('Ctrl Pts',(201.59122540484,9.85405127028369,29.7718885954875));
#73531=CARTESIAN_POINT('Ctrl Pts',(201.59040772308,9.85689882168436,29.7836596291627));
#73532=CARTESIAN_POINT('Ctrl Pts',(201.589943095713,9.85858776797011,29.7903811486136));
#73533=CARTESIAN_POINT('Ctrl Pts',(201.588405920724,9.86440889735034,29.8127117079266));
#73534=CARTESIAN_POINT('Ctrl Pts',(201.58734671775,9.86880290442364,29.8282513621288));
#73535=CARTESIAN_POINT('Ctrl Pts',(201.584736262872,9.88055530235827,29.8667704947647));
#73536=CARTESIAN_POINT('Ctrl Pts',(201.583200983467,9.88830296911926,29.8896240191425));
#73537=CARTESIAN_POINT('Ctrl Pts',(201.574624847396,9.93597219059407,30.0172029435896));
#73538=CARTESIAN_POINT('Ctrl Pts',(201.567898488929,9.98997597966212,30.1160409303099));
#73539=CARTESIAN_POINT('Ctrl Pts',(201.559462506899,10.0679552947174,30.2202179066136));
#73540=CARTESIAN_POINT('Ctrl Pts',(201.558280744897,10.0791072321931,30.234423324952));
#73541=CARTESIAN_POINT('Ctrl Pts',(201.556667637363,10.0946044914041,30.2532556885621));
#73542=CARTESIAN_POINT('Ctrl Pts',(201.55624731731,10.0986673606599,30.2581125432704));
#73543=CARTESIAN_POINT('Ctrl Pts',(201.555825452273,10.1027690875306,30.2629362700837));
#73544=CARTESIAN_POINT('',(201.512132885209,9.82225036610555,29.4990713657972));
#73545=CARTESIAN_POINT('Ctrl Pts',(201.456090246984,10.1027690874833,30.2629362700282));
#73546=CARTESIAN_POINT('Ctrl Pts',(201.459217919371,10.0728355900905,30.2277337764049));
#73547=CARTESIAN_POINT('Ctrl Pts',(201.462345591759,10.0449212876478,30.1907011699184));
#73548=CARTESIAN_POINT('Ctrl Pts',(201.465473264147,10.0192575340884,30.1521037325899));
#73549=CARTESIAN_POINT('Ctrl Pts',(201.468597790043,9.99361959870365,30.1135451249428));
#73550=CARTESIAN_POINT('Ctrl Pts',(201.471722315939,9.97022805109866,30.0734252765857));
#73551=CARTESIAN_POINT('Ctrl Pts',(201.474846841836,9.94927302065566,30.032041236539));
#73552=CARTESIAN_POINT('Ctrl Pts',(201.47797127168,9.92831863439262,29.9906584686817));
#73553=CARTESIAN_POINT('Ctrl Pts',(201.481095701525,9.90980090327951,29.9480120850801));
#73554=CARTESIAN_POINT('Ctrl Pts',(201.48422013137,9.89386448097275,29.9044246234421));
#73555=CARTESIAN_POINT('Ctrl Pts',(201.487344187057,9.87792996708856,29.8608423815012));
#73556=CARTESIAN_POINT('Ctrl Pts',(201.490468242744,9.86457633736907,29.8163198290956));
#73557=CARTESIAN_POINT('Ctrl Pts',(201.493592298432,9.85389912864669,29.7711970781243));
#73558=CARTESIAN_POINT('Ctrl Pts',(201.496720654507,9.84320722231794,29.7260122138752));
#73559=CARTESIAN_POINT('Ctrl Pts',(201.499849010582,9.83519921713805,29.6802260650162));
#73560=CARTESIAN_POINT('Ctrl Pts',(201.502977366658,9.82991956341843,29.6341895466461));
#73561=CARTESIAN_POINT('Ctrl Pts',(201.506029206175,9.82476904491298,29.5892790369074));
#73562=CARTESIAN_POINT('Ctrl Pts',(201.509081045692,9.82221483756981,29.5441307872882));
#73563=CARTESIAN_POINT('Ctrl Pts',(201.512132885209,9.82225036610555,29.4990713657972));
#73564=CARTESIAN_POINT('Ctrl Pts',(201.512132885264,9.82225036610619,29.4990713649792));
#73565=CARTESIAN_POINT('Ctrl Pts',(201.516636055637,9.82230279061592,29.4325835137179));
#73566=CARTESIAN_POINT('Ctrl Pts',(201.52113922601,9.82798776705774,29.3663156636972));
#73567=CARTESIAN_POINT('Ctrl Pts',(201.525642396383,9.83918085218961,29.3010176676768));
#73568=CARTESIAN_POINT('Ctrl Pts',(201.52891955883,9.84732657070003,29.2534973380618));
#73569=CARTESIAN_POINT('Ctrl Pts',(201.532196721278,9.8584134694595,29.2063708183464));
#73570=CARTESIAN_POINT('Ctrl Pts',(201.535473883725,9.87238554473478,29.1600283794536));
#73571=CARTESIAN_POINT('Ctrl Pts',(201.538647836056,9.88591758704595,29.1151454374751));
#73572=CARTESIAN_POINT('Ctrl Pts',(201.541821788388,9.90215558414496,29.0709984974849));
#73573=CARTESIAN_POINT('Ctrl Pts',(201.544995740719,9.92099666492068,29.0279334100069));
#73574=CARTESIAN_POINT('Ctrl Pts',(201.548166568088,9.93981919542436,28.9849107229144));
#73575=CARTESIAN_POINT('Ctrl Pts',(201.551337395457,9.96123951442141,28.9429682879285));
#73576=CARTESIAN_POINT('Ctrl Pts',(201.554508222825,9.98510582347525,28.9024342103532));
#73577=CARTESIAN_POINT('Ctrl Pts',(201.557677319771,10.0089591079097,28.8619222535396));
#73578=CARTESIAN_POINT('Ctrl Pts',(201.560846416716,10.0352554558839,28.8228176105625));
#73579=CARTESIAN_POINT('Ctrl Pts',(201.564015513661,10.0637973353376,28.7854234588381));
#73580=CARTESIAN_POINT('Ctrl Pts',(201.567184271724,10.0923361627101,28.7480333057985));
#73581=CARTESIAN_POINT('Ctrl Pts',(201.570353029787,10.1231197053437,28.7123537218591));
#73582=CARTESIAN_POINT('Ctrl Pts',(201.573521787849,10.1559089641209,28.6786563534984));
#73583=CARTESIAN_POINT('Ctrl Pts',(201.576693732285,10.1887311944281,28.6449251004499));
#73584=CARTESIAN_POINT('Ctrl Pts',(201.579865676721,10.2235627746507,28.6131804382304));
#73585=CARTESIAN_POINT('Ctrl Pts',(201.583037621156,10.2601279062822,28.5836570797798));
#73586=CARTESIAN_POINT('Ctrl Pts',(201.586211510427,10.2967154573282,28.5541156194825));
#73587=CARTESIAN_POINT('Ctrl Pts',(201.589385399697,10.335038221367,28.5267984963833));
#73588=CARTESIAN_POINT('Ctrl Pts',(201.592559288967,10.3747903130615,28.5018978459805));
#73589=CARTESIAN_POINT('Ctrl Pts',(201.595738793446,10.4146127336974,28.4769531416348));
#73590=CARTESIAN_POINT('Ctrl Pts',(201.598918297924,10.4558690362348,28.4544337009151));
#73591=CARTESIAN_POINT('Ctrl Pts',(201.602097802403,10.49822934729,28.4344854414045));
#73592=CARTESIAN_POINT('Ctrl Pts',(201.602829966641,10.5079839191355,28.4298918318265));
#73593=CARTESIAN_POINT('Ctrl Pts',(201.603562130879,10.5177969584718,28.4254343595157));
#73594=CARTESIAN_POINT('Ctrl Pts',(201.604294295117,10.5276643146806,28.4211144347643));
#73595=CARTESIAN_POINT('Ctrl Pts',(201.607571457564,10.5718305379666,28.4017784792043));
#73596=CARTESIAN_POINT('Ctrl Pts',(201.610848620012,10.617285683156,28.3851154074467));
#73597=CARTESIAN_POINT('Ctrl Pts',(201.614125782459,10.6636730183221,28.3712931186993));
#73598=CARTESIAN_POINT('Ctrl Pts',(201.61729973479,10.7085994426223,28.3579061455775));
#73599=CARTESIAN_POINT('Ctrl Pts',(201.620473687122,10.7543996275644,28.3471838361457));
#73600=CARTESIAN_POINT('Ctrl Pts',(201.623647639453,10.8007281584948,28.3392305156996));
#73601=CARTESIAN_POINT('Ctrl Pts',(201.626818466822,10.8470110759668,28.3312850258158));
#73602=CARTESIAN_POINT('Ctrl Pts',(201.629989294191,10.8938207633434,28.3261032224443));
#73603=CARTESIAN_POINT('Ctrl Pts',(201.633160121559,10.940799712924,28.3237388094007));
#73604=CARTESIAN_POINT('Ctrl Pts',(201.636329218505,10.9877530245671,28.3213756866941));
#73605=CARTESIAN_POINT('Ctrl Pts',(201.63949831545,11.0348748601952,28.3218269362728));
#73606=CARTESIAN_POINT('Ctrl Pts',(201.642667412395,11.0818033742262,28.3250943567821));
#73607=CARTESIAN_POINT('Ctrl Pts',(201.645836170458,11.1287268700302,28.328361427895));
#73608=CARTESIAN_POINT('Ctrl Pts',(201.649004928521,11.175456530261,28.3344440311103));
#73609=CARTESIAN_POINT('Ctrl Pts',(201.652173686583,11.2216340326959,28.3432919910146));
#73610=CARTESIAN_POINT('Ctrl Pts',(201.655345631019,11.2678579693282,28.3521488480635));
#73611=CARTESIAN_POINT('Ctrl Pts',(201.658517575455,11.3135280930283,28.3637765030913));
#73612=CARTESIAN_POINT('Ctrl Pts',(201.66168951989,11.3582966842705,28.3780737330195));
#73613=CARTESIAN_POINT('Ctrl Pts',(201.664863409161,11.4030927247672,28.3923797291003));
#73614=CARTESIAN_POINT('Ctrl Pts',(201.668037298431,11.4469856134574,28.409358356266));
#73615=CARTESIAN_POINT('Ctrl Pts',(201.671211187701,11.4896466391654,28.4288598451864));
#73616=CARTESIAN_POINT('Ctrl Pts',(201.67439069218,11.5323831402671,28.4483958359157));
#73617=CARTESIAN_POINT('Ctrl Pts',(201.677570196658,11.5738829418941,28.4704633272616));
#73618=CARTESIAN_POINT('Ctrl Pts',(201.680749701137,11.6138427361426,28.4948670944671));
#73619=CARTESIAN_POINT('Ctrl Pts',(201.681481865375,11.6230445260779,28.5004867014665));
#73620=CARTESIAN_POINT('Ctrl Pts',(201.682214029613,11.6321647839154,28.5062300190961));
#73621=CARTESIAN_POINT('Ctrl Pts',(201.682946193851,11.6412000488187,28.5120943567856));
#73622=CARTESIAN_POINT('Ctrl Pts',(201.686223356298,11.6816418367429,28.5383430947793));
#73623=CARTESIAN_POINT('Ctrl Pts',(201.689500518745,11.7205603945304,28.5671384771231));
#73624=CARTESIAN_POINT('Ctrl Pts',(201.692777681193,11.7576192831497,28.5982749397406));
#73625=CARTESIAN_POINT('Ctrl Pts',(201.695951633524,11.7935110486119,28.6284307985705));
#73626=CARTESIAN_POINT('Ctrl Pts',(201.699125585856,11.8276580881997,28.6607820666704));
#73627=CARTESIAN_POINT('Ctrl Pts',(201.702299538187,11.8597832804536,28.6950976623513));
#73628=CARTESIAN_POINT('Ctrl Pts',(201.705470365556,11.891876843362,28.7293794720915));
#73629=CARTESIAN_POINT('Ctrl Pts',(201.708641192925,11.9219521202615,28.7656213765379));
#73630=CARTESIAN_POINT('Ctrl Pts',(201.711812020293,11.9497676133906,28.8035543502509));
#73631=CARTESIAN_POINT('Ctrl Pts',(201.714981117239,11.9775679267023,28.8414666227091));
#73632=CARTESIAN_POINT('Ctrl Pts',(201.718150214184,12.003110570642,28.8810676878428));
#73633=CARTESIAN_POINT('Ctrl Pts',(201.721319311129,12.0261950089443,28.9220563469353));
#73634=CARTESIAN_POINT('Ctrl Pts',(201.724488069192,12.0492769787485,28.9630406229699));
#73635=CARTESIAN_POINT('Ctrl Pts',(201.727656827255,12.0699009937059,29.0054117123376));
#73636=CARTESIAN_POINT('Ctrl Pts',(201.730825585317,12.0879118606755,29.0488427703099));
#73637=CARTESIAN_POINT('Ctrl Pts',(201.733997529753,12.1059408386322,29.092317500768));
#73638=CARTESIAN_POINT('Ctrl Pts',(201.737169474189,12.121351214005,29.1368538105736));
#73639=CARTESIAN_POINT('Ctrl Pts',(201.740341418624,12.1340362571272,29.1821056307184));
#73640=CARTESIAN_POINT('Ctrl Pts',(201.743515307895,12.1467290779115,29.227385196403));
#73641=CARTESIAN_POINT('Ctrl Pts',(201.746689197165,12.1566931234071,29.273380601123));
#73642=CARTESIAN_POINT('Ctrl Pts',(201.749863086435,12.1638726619692,29.319734947312));
#73643=CARTESIAN_POINT('Ctrl Pts',(201.753042590914,12.1710649024881,29.3661713030746));
#73644=CARTESIAN_POINT('Ctrl Pts',(201.756222095392,12.1754627611754,29.4129673130365));
#73645=CARTESIAN_POINT('Ctrl Pts',(201.759401599871,12.177062440713,29.4597622917797));
#73646=CARTESIAN_POINT('Ctrl Pts',(201.760133764109,12.1774308088526,29.4705380620888));
#73647=CARTESIAN_POINT('Ctrl Pts',(201.760865928347,12.1776510155898,29.4813137898791));
#73648=CARTESIAN_POINT('Ctrl Pts',(201.761598092585,12.1777234042577,29.4920851049469));
#73649=CARTESIAN_POINT('Ctrl Pts',(201.764875255032,12.1780474154721,29.5402974423047));
#73650=CARTESIAN_POINT('Ctrl Pts',(201.76815241748,12.1754067908878,29.58863847339));
#73651=CARTESIAN_POINT('Ctrl Pts',(201.771429579927,12.1697881439925,29.6367141568183));
#73652=CARTESIAN_POINT('Ctrl Pts',(201.774603532259,12.1643464493251,29.6832757569724));
#73653=CARTESIAN_POINT('Ctrl Pts',(201.77777748459,12.1561116114345,29.729587875313));
#73654=CARTESIAN_POINT('Ctrl Pts',(201.780951436922,12.1451241821247,29.7752919723006));
#73655=CARTESIAN_POINT('Ctrl Pts',(201.78412226429,12.1341475706553,29.8209510706257));
#73656=CARTESIAN_POINT('Ctrl Pts',(201.787293091659,12.1204238616838,29.8660027934623));
#73657=CARTESIAN_POINT('Ctrl Pts',(201.790463919028,12.1040448898881,29.9100974806213));
#73658=CARTESIAN_POINT('Ctrl Pts',(201.793633015973,12.0876748566289,29.9541681038784));
#73659=CARTESIAN_POINT('Ctrl Pts',(201.796802112918,12.0686526248256,29.9972822050097));
#73660=CARTESIAN_POINT('Ctrl Pts',(201.799971209864,12.0471194290063,30.0391066349968));
#73661=CARTESIAN_POINT('Ctrl Pts',(201.803139967926,12.0255885358054,30.0809265925542));
#73662=CARTESIAN_POINT('Ctrl Pts',(201.806308725989,12.0015474684606,30.1214566590244));
#73663=CARTESIAN_POINT('Ctrl Pts',(201.809477484052,11.9751838203621,30.1603874461284));
#73664=CARTESIAN_POINT('Ctrl Pts',(201.812649428488,11.9487936620634,30.1993573804307));
#73665=CARTESIAN_POINT('Ctrl Pts',(201.815821372923,11.9200765775157,30.236724366064));
#73666=CARTESIAN_POINT('Ctrl Pts',(201.818993317359,11.8892628723486,30.2722089136771));
#73667=CARTESIAN_POINT('Ctrl Pts',(201.822167206629,11.8584302741761,30.3077152181592));
#73668=CARTESIAN_POINT('Ctrl Pts',(201.8253410959,11.8254988870274,30.3413363900374));
#73669=CARTESIAN_POINT('Ctrl Pts',(201.82851498517,11.7907361113877,30.3728295736554));
#73670=CARTESIAN_POINT('Ctrl Pts',(201.831694489648,11.7559118338471,30.4043784746499));
#73671=CARTESIAN_POINT('Ctrl Pts',(201.834873994127,11.719250140878,30.4337915326009));
#73672=CARTESIAN_POINT('Ctrl Pts',(201.838053498606,11.6810501629335,30.4608671802431));
#73673=CARTESIAN_POINT('Ctrl Pts',(201.838785662844,11.6722536168253,30.4671020577406));
#73674=CARTESIAN_POINT('Ctrl Pts',(201.839517827082,11.6633756096369,30.4732131778327));
#73675=CARTESIAN_POINT('Ctrl Pts',(201.84024999132,11.6544199799073,30.4791984234046));
#73676=CARTESIAN_POINT('Ctrl Pts',(201.843527153767,11.6143346385116,30.505988344307));
#73677=CARTESIAN_POINT('Ctrl Pts',(201.846804316214,11.5725111150186,30.5303731975406));
#73678=CARTESIAN_POINT('Ctrl Pts',(201.850081478662,11.5292711218841,30.5521250600758));
#73679=CARTESIAN_POINT('Ctrl Pts',(201.853255430993,11.4873929180307,30.5731918750174));
#73680=CARTESIAN_POINT('Ctrl Pts',(201.856429383325,11.4441866877486,30.5917888243663));
#73681=CARTESIAN_POINT('Ctrl Pts',(201.859603335656,11.3999741637609,30.6077525584822));
#73682=CARTESIAN_POINT('Ctrl Pts',(201.862774163025,11.3558051698847,30.6237005752613));
#73683=CARTESIAN_POINT('Ctrl Pts',(201.865944990394,11.3106323648664,30.6370203202011));
#73684=CARTESIAN_POINT('Ctrl Pts',(201.869115817762,11.2647982743046,30.6475961556337));
#73685=CARTESIAN_POINT('Ctrl Pts',(201.872284914708,11.2189891968934,30.6581662194897));
#73686=CARTESIAN_POINT('Ctrl Pts',(201.875454011653,11.1725200905719,30.6659952153911));
#73687=CARTESIAN_POINT('Ctrl Pts',(201.878623108598,11.1257468644904,30.6710178429771));
#73688=CARTESIAN_POINT('Ctrl Pts',(201.881791866661,11.0789786400304,30.6760399334764));
#73689=CARTESIAN_POINT('Ctrl Pts',(201.884960624724,11.0319069139624,30.6782561943257));
#73690=CARTESIAN_POINT('Ctrl Pts',(201.888129382786,10.9848932519535,30.6776531104971));
#73691=CARTESIAN_POINT('Ctrl Pts',(201.891301327222,10.9378323149396,30.6770494202321));
#73692=CARTESIAN_POINT('Ctrl Pts',(201.894473271658,10.8908301160774,30.6736207379259));
#73693=CARTESIAN_POINT('Ctrl Pts',(201.897645216093,10.8442467455301,30.6674056648064));
#73694=CARTESIAN_POINT('Ctrl Pts',(201.900819105364,10.797634813021,30.6611867809991));
#73695=CARTESIAN_POINT('Ctrl Pts',(201.903992994634,10.7514427664435,30.6521782133556));
#73696=CARTESIAN_POINT('Ctrl Pts',(201.907166883904,10.7060205061947,30.6404696925925));
#73697=CARTESIAN_POINT('Ctrl Pts',(201.910346388383,10.6605178854079,30.6287404572497));
#73698=CARTESIAN_POINT('Ctrl Pts',(201.913525892861,10.6157882955807,30.6143019149662));
#73699=CARTESIAN_POINT('Ctrl Pts',(201.91670539734,10.5721646090964,30.597293005897));
#73700=CARTESIAN_POINT('Ctrl Pts',(201.917437561578,10.5621191119466,30.5933762587959));
#73701=CARTESIAN_POINT('Ctrl Pts',(201.918169725816,10.5521321604145,30.5893234080077));
#73702=CARTESIAN_POINT('Ctrl Pts',(201.918901890054,10.542207633965,30.5851364946863));
#73703=CARTESIAN_POINT('Ctrl Pts',(201.922080584737,10.4991202529918,30.5669589896641));
#73704=CARTESIAN_POINT('Ctrl Pts',(201.925259279421,10.4570229406646,30.5461714465251));
#73705=CARTESIAN_POINT('Ctrl Pts',(201.928437974104,10.4162511379083,30.5229038706089));
#73706=CARTESIAN_POINT('Ctrl Pts',(201.931612116937,10.3755377198582,30.4996696135672));
#73707=CARTESIAN_POINT('Ctrl Pts',(201.93478625977,10.3361465356879,30.4739626231147));
#73708=CARTESIAN_POINT('Ctrl Pts',(201.937960402603,10.2983917674929,30.4459603324549));
#73709=CARTESIAN_POINT('Ctrl Pts',(201.941131583528,10.2606722296368,30.4179841717448));
#73710=CARTESIAN_POINT('Ctrl Pts',(201.944302764454,10.2245865330093,30.387717277307));
#73711=CARTESIAN_POINT('Ctrl Pts',(201.947473945379,10.1904207089845,30.3553808707581));
#73712=CARTESIAN_POINT('Ctrl Pts',(201.950336805105,10.1595766909726,30.3261884032997));
#73713=CARTESIAN_POINT('Ctrl Pts',(201.95319966483,10.1302972464099,30.2953100293104));
#73714=CARTESIAN_POINT('Ctrl Pts',(201.956062524555,10.1027690874833,30.2629362700282));
#73715=CARTESIAN_POINT('Origin',(197.762132885264,11.,29.5));
#73716=CARTESIAN_POINT('',(202.554740968482,10.1027692175106,30.2629364229433));
#73717=CARTESIAN_POINT('',(202.455993057958,10.1022055060817,30.2634229920695));
#73718=CARTESIAN_POINT('',(197.762132885264,10.1027690874833,30.2629362700282));
#73719=CARTESIAN_POINT('',(202.111797459566,9.8222500756293,29.4995779279502));
#73720=CARTESIAN_POINT('Ctrl Pts',(202.554740968482,10.1027692175106,30.2629364229433));
#73721=CARTESIAN_POINT('Ctrl Pts',(202.551960232187,10.1273404241732,30.2918327271669));
#73722=CARTESIAN_POINT('Ctrl Pts',(202.549173805468,10.153306367189,30.3195406316827));
#73723=CARTESIAN_POINT('Ctrl Pts',(202.544099121304,10.2035899648221,30.3682466365461));
#73724=CARTESIAN_POINT('Ctrl Pts',(202.541804407233,10.2275005328419,30.38958760777));
#73725=CARTESIAN_POINT('Ctrl Pts',(202.53893503173,10.2592317714701,30.4156631874325));
#73726=CARTESIAN_POINT('Ctrl Pts',(202.53830860141,10.2662759625235,30.42131736682));
#73727=CARTESIAN_POINT('Ctrl Pts',(202.537305432702,10.2777569378722,30.4303176259428));
#73728=CARTESIAN_POINT('Ctrl Pts',(202.536925418902,10.2821534200698,30.433714205095));
#73729=CARTESIAN_POINT('Ctrl Pts',(202.536178482652,10.2908921212018,30.4403672336965));
#73730=CARTESIAN_POINT('Ctrl Pts',(202.535811484359,10.2952331101845,30.4436250056164));
#73731=CARTESIAN_POINT('Ctrl Pts',(202.53487939963,10.3063745309721,30.4518665087001));
#73732=CARTESIAN_POINT('Ctrl Pts',(202.534317098837,10.3132063951316,30.4568075543328));
#73733=CARTESIAN_POINT('Ctrl Pts',(202.531901256486,10.3430070821966,30.4778767893962));
#73734=CARTESIAN_POINT('Ctrl Pts',(202.530090716421,10.3664970192476,30.4932557345955));
#73735=CARTESIAN_POINT('Ctrl Pts',(202.524534891989,10.4413265274764,30.538510954867));
#73736=CARTESIAN_POINT('Ctrl Pts',(202.520889207193,10.4943911262989,30.5653551229465));
#73737=CARTESIAN_POINT('Ctrl Pts',(202.5131142898,10.6102180391572,30.6133369245908));
#73738=CARTESIAN_POINT('Ctrl Pts',(202.50898715164,10.6731865122077,30.6334198461389));
#73739=CARTESIAN_POINT('Ctrl Pts',(202.50365987023,10.7528961863222,30.65164411892));
#73740=CARTESIAN_POINT('Ctrl Pts',(202.502622187586,10.7683602303358,30.6548538653976));
#73741=CARTESIAN_POINT('Ctrl Pts',(202.500917937525,10.7936207382878,30.6595692213524));
#73742=CARTESIAN_POINT('Ctrl Pts',(202.500257289207,10.8033801954236,30.6612638895795));
#73743=CARTESIAN_POINT('Ctrl Pts',(202.498968081178,10.8223535997132,30.6643124711324));
#73744=CARTESIAN_POINT('Ctrl Pts',(202.498340015447,10.8315645386323,30.6656805998332));
#73745=CARTESIAN_POINT('Ctrl Pts',(202.49684793314,10.8533640313455,30.6686547785236));
#73746=CARTESIAN_POINT('Ctrl Pts',(202.49598108415,10.8659640130026,30.6701668390432));
#73747=CARTESIAN_POINT('Ctrl Pts',(202.492943980129,10.9098685401097,30.674717208421));
#73748=CARTESIAN_POINT('Ctrl Pts',(202.490742375719,10.9412661100783,30.6767048129087));
#73749=CARTESIAN_POINT('Ctrl Pts',(202.48495580168,11.0226725331412,30.6785920801637));
#73750=CARTESIAN_POINT('Ctrl Pts',(202.481324238941,11.0726604337243,30.6765682955158));
#73751=CARTESIAN_POINT('Ctrl Pts',(202.472322134592,11.1949393537006,30.6637947971776));
#73752=CARTESIAN_POINT('Ctrl Pts',(202.466933679217,11.2666576728945,30.6494846240999));
#73753=CARTESIAN_POINT('Ctrl Pts',(202.460988769861,11.3476182720866,30.6253394768748));
#73754=CARTESIAN_POINT('Ctrl Pts',(202.460186126835,11.3585940687382,30.6218902439131));
#73755=CARTESIAN_POINT('Ctrl Pts',(202.458967291192,11.3753552867929,30.6163517657282));
#73756=CARTESIAN_POINT('Ctrl Pts',(202.458545202683,11.3811774940067,30.614377215505));
#73757=CARTESIAN_POINT('Ctrl Pts',(202.457775241298,11.391835545058,30.6106693265542));
#73758=CARTESIAN_POINT('Ctrl Pts',(202.457426647153,11.3966757122099,30.6089498762958));
#73759=CARTESIAN_POINT('Ctrl Pts',(202.456610106818,11.4080459226621,30.6048266836054));
#73760=CARTESIAN_POINT('Ctrl Pts',(202.456143665445,11.4145661335786,30.6023966629925));
#73761=CARTESIAN_POINT('Ctrl Pts',(202.454593513435,11.4363025805553,30.5940755660237));
#73762=CARTESIAN_POINT('Ctrl Pts',(202.453523456901,11.451418580527,30.5879258311098));
#73763=CARTESIAN_POINT('Ctrl Pts',(202.450879379118,11.4888880727225,30.5717663645126));
#73764=CARTESIAN_POINT('Ctrl Pts',(202.449321865635,11.5110668531565,30.5613696350463));
#73765=CARTESIAN_POINT('Ctrl Pts',(202.442124088541,11.6130560481044,30.5096212632605));
#73766=CARTESIAN_POINT('Ctrl Pts',(202.436687165938,11.6882865249071,30.4599141788348));
#73767=CARTESIAN_POINT('Ctrl Pts',(202.42895147597,11.781624207456,30.3815786737201));
#73768=CARTESIAN_POINT('Ctrl Pts',(202.426893926822,11.8052661872954,30.3600368931716));
#73769=CARTESIAN_POINT('Ctrl Pts',(202.423938905603,11.8373133630245,30.328355515304));
#73770=CARTESIAN_POINT('Ctrl Pts',(202.423074020923,11.8464710510474,30.318995277839));
#73771=CARTESIAN_POINT('Ctrl Pts',(202.421584374208,11.8618529485024,30.302739552475));
#73772=CARTESIAN_POINT('Ctrl Pts',(202.420962979096,11.8681552567601,30.2959194279658));
#73773=CARTESIAN_POINT('Ctrl Pts',(202.419682016383,11.8809095878748,30.2817854357582));
#73774=CARTESIAN_POINT('Ctrl Pts',(202.419022150206,11.8873527111679,30.2744645413184));
#73775=CARTESIAN_POINT('Ctrl Pts',(202.417334792171,11.9035022669995,30.2556487574543));
#73776=CARTESIAN_POINT('Ctrl Pts',(202.416302283388,11.9130804741851,30.2440466401949));
#73777=CARTESIAN_POINT('Ctrl Pts',(202.411377175681,11.9573232165224,30.1883140802555));
#73778=CARTESIAN_POINT('Ctrl Pts',(202.407373961684,11.9890223013109,30.1419324680314));
#73779=CARTESIAN_POINT('Ctrl Pts',(202.398253272719,12.0522852548754,30.0334916020876));
#73780=CARTESIAN_POINT('Ctrl Pts',(202.393111617308,12.0819038483196,29.9705330789618));
#73781=CARTESIAN_POINT('Ctrl Pts',(202.386012449755,12.1157085920347,29.8783091286168));
#73782=CARTESIAN_POINT('Ctrl Pts',(202.383957111363,12.1246210724822,29.8509290349413));
#73783=CARTESIAN_POINT('Ctrl Pts',(202.381338506928,12.1349182299877,29.8148521876278));
#73784=CARTESIAN_POINT('Ctrl Pts',(202.38073346103,12.1372211548994,29.80642999999));
#73785=CARTESIAN_POINT('Ctrl Pts',(202.379793334744,12.1406821241273,29.7931958978888));
#73786=CARTESIAN_POINT('Ctrl Pts',(202.379454893384,12.1419038102303,29.7884011672507));
#73787=CARTESIAN_POINT('Ctrl Pts',(202.37875356737,12.1443853892996,29.7783987215763));
#73788=CARTESIAN_POINT('Ctrl Pts',(202.378391016823,12.1456400219038,29.7731898774099));
#73789=CARTESIAN_POINT('Ctrl Pts',(202.377486181234,12.1486986892493,29.7600995061544));
#73790=CARTESIAN_POINT('Ctrl Pts',(202.376946358788,12.150457234793,29.7522074377083));
#73791=CARTESIAN_POINT('Ctrl Pts',(202.374774466698,12.1572542137225,29.7201521377375));
#73792=CARTESIAN_POINT('Ctrl Pts',(202.37317534365,12.1616141169352,29.6958497265245));
#73793=CARTESIAN_POINT('Ctrl Pts',(202.368618143973,12.1720047861223,29.6252230135169));
#73794=CARTESIAN_POINT('Ctrl Pts',(202.36572306985,12.1760485810298,29.5786531489674));
#73795=CARTESIAN_POINT('Ctrl Pts',(202.358010189211,12.1794285207688,29.4541597543406));
#73796=CARTESIAN_POINT('Ctrl Pts',(202.353204361497,12.1738233144532,29.3763464469293));
#73797=CARTESIAN_POINT('Ctrl Pts',(202.346979318126,12.1574835634851,29.2816897795632));
#73798=CARTESIAN_POINT('Ctrl Pts',(202.345786354447,12.1539650812882,29.2637965155006));
#73799=CARTESIAN_POINT('Ctrl Pts',(202.343885584894,12.1477660694697,29.2357301101122));
#73800=CARTESIAN_POINT('Ctrl Pts',(202.343186407096,12.1453621271405,29.225498432039));
#73801=CARTESIAN_POINT('Ctrl Pts',(202.341875473737,12.1406280520877,29.2064952212172));
#73802=CARTESIAN_POINT('Ctrl Pts',(202.341264863963,12.1383328279824,29.1977157409286));
#73803=CARTESIAN_POINT('Ctrl Pts',(202.339877172715,12.1329154633657,29.1779309598615));
#73804=CARTESIAN_POINT('Ctrl Pts',(202.339098253862,12.1297340102291,29.1669430018586));
#73805=CARTESIAN_POINT('Ctrl Pts',(202.336696535335,12.1194997990496,29.1334317791305));
#73806=CARTESIAN_POINT('Ctrl Pts',(202.335057518132,12.1119300388235,29.1110738972545));
#73807=CARTESIAN_POINT('Ctrl Pts',(202.325639836195,12.0651794541282,28.9855427454284));
#73808=CARTESIAN_POINT('Ctrl Pts',(202.317416187995,12.0123216839667,28.888059953376));
#73809=CARTESIAN_POINT('Ctrl Pts',(202.307332262731,11.9293526571941,28.7759499391536));
#73810=CARTESIAN_POINT('Ctrl Pts',(202.305249809137,11.9111457026238,28.7531675856395));
#73811=CARTESIAN_POINT('Ctrl Pts',(202.302602928235,11.8863896722701,28.7244452344738));
#73812=CARTESIAN_POINT('Ctrl Pts',(202.301995624792,11.8805947336533,28.7178716397885));
#73813=CARTESIAN_POINT('Ctrl Pts',(202.301015472042,11.8710455793582,28.7072800725767));
#73814=CARTESIAN_POINT('Ctrl Pts',(202.300639603373,11.8673357648595,28.7032227671791));
#73815=CARTESIAN_POINT('Ctrl Pts',(202.299893400544,11.8598719906001,28.6951737800827));
#73816=CARTESIAN_POINT('Ctrl Pts',(202.299523063515,11.8561183161034,28.6911820252706));
#73817=CARTESIAN_POINT('Ctrl Pts',(202.298571373718,11.8463483251833,28.6809365869243));
#73818=CARTESIAN_POINT('Ctrl Pts',(202.297993043373,11.8402903825742,28.674722806553));
#73819=CARTESIAN_POINT('Ctrl Pts',(202.295379379666,11.8123910955407,28.6467315616968));
#73820=CARTESIAN_POINT('Ctrl Pts',(202.293396270798,11.7897663499811,28.6257484455269));
#73821=CARTESIAN_POINT('Ctrl Pts',(202.286833881049,11.7110523478269,28.5582987942358));
#73822=CARTESIAN_POINT('Ctrl Pts',(202.282398957624,11.6514865005786,28.5161489115263));
#73823=CARTESIAN_POINT('Ctrl Pts',(202.274682174716,11.5444209384503,28.454400060992));
#73824=CARTESIAN_POINT('Ctrl Pts',(202.271468008235,11.498845016673,28.4319053525508));
#73825=CARTESIAN_POINT('Ctrl Pts',(202.267172728344,11.4380660658995,28.4066475079555));
#73826=CARTESIAN_POINT('Ctrl Pts',(202.266182580057,11.4240599287354,28.4011393656927));
#73827=CARTESIAN_POINT('Ctrl Pts',(202.264536251259,11.4008091643122,28.3925063411857));
#73828=CARTESIAN_POINT('Ctrl Pts',(202.263885221659,11.3916241559436,28.3892251796864));
#73829=CARTESIAN_POINT('Ctrl Pts',(202.26259994936,11.3735168342792,28.3830092030314));
#73830=CARTESIAN_POINT('Ctrl Pts',(202.261966025628,11.364598058348,28.3800662907447));
#73831=CARTESIAN_POINT('Ctrl Pts',(202.260434968091,11.3430929283237,28.3732543876834));
#73832=CARTESIAN_POINT('Ctrl Pts',(202.259534584571,11.3304752646235,28.3694892713367));
#73833=CARTESIAN_POINT('Ctrl Pts',(202.256213440429,11.2840583506269,28.3564819015173));
#73834=CARTESIAN_POINT('Ctrl Pts',(202.25375283203,11.2499172890328,28.348538446409));
#73835=CARTESIAN_POINT('Ctrl Pts',(202.244297781506,11.1196581841898,28.3242976779898));
#73836=CARTESIAN_POINT('Ctrl Pts',(202.237035502614,11.0220119630204,28.3184306998474));
#73837=CARTESIAN_POINT('Ctrl Pts',(202.228099293334,10.8983345845817,28.3263472824764));
#73838=CARTESIAN_POINT('Ctrl Pts',(202.22621225451,10.8719652531414,28.3289304495842));
#73839=CARTESIAN_POINT('Ctrl Pts',(202.223770475137,10.8372581888328,28.3335169381678));
#73840=CARTESIAN_POINT('Ctrl Pts',(202.223180472195,10.8288249651324,28.3347246039811));
#73841=CARTESIAN_POINT('Ctrl Pts',(202.22225810465,10.815555613766,28.3367719870329));
#73842=CARTESIAN_POINT('Ctrl Pts',(202.221922579919,10.8107105513479,28.3375505823512));
#73843=CARTESIAN_POINT('Ctrl Pts',(202.221221699291,10.8005485419445,28.3392488245125));
#73844=CARTESIAN_POINT('Ctrl Pts',(202.220856727616,10.7952327938774,28.34017476805));
#73845=CARTESIAN_POINT('Ctrl Pts',(202.219936861365,10.781779926252,28.3426134789471));
#73846=CARTESIAN_POINT('Ctrl Pts',(202.2193846068,10.7736518502921,28.34417558238));
#73847=CARTESIAN_POINT('Ctrl Pts',(202.217082032174,10.7395825240928,28.3510964225721));
#73848=CARTESIAN_POINT('Ctrl Pts',(202.215369865782,10.7138074880022,28.3572442206944));
#73849=CARTESIAN_POINT('Ctrl Pts',(202.210303398002,10.6370712384756,28.3783068840432));
#73850=CARTESIAN_POINT('Ctrl Pts',(202.207029744722,10.5868880170377,28.3958025914628));
#73851=CARTESIAN_POINT('Ctrl Pts',(202.199473587729,10.4746513116737,28.4436598272312));
#73852=CARTESIAN_POINT('Ctrl Pts',(202.195190834194,10.4137510780786,28.4762047962713));
#73853=CARTESIAN_POINT('Ctrl Pts',(202.189533890876,10.3406406648647,28.5239472412827));
#73854=CARTESIAN_POINT('Ctrl Pts',(202.188330212342,10.3254710142461,28.5343684401743));
#73855=CARTESIAN_POINT('Ctrl Pts',(202.186416224703,10.302002181585,28.551313894553));
#73856=CARTESIAN_POINT('Ctrl Pts',(202.185714750933,10.2935355456379,28.5576018654728));
#73857=CARTESIAN_POINT('Ctrl Pts',(202.184395967035,10.2778765181609,28.5695610664678));
#73858=CARTESIAN_POINT('Ctrl Pts',(202.183779773645,10.2706635842321,28.5752041757013));
#73859=CARTESIAN_POINT('Ctrl Pts',(202.182386878713,10.2545957512016,28.5880798968049));
#73860=CARTESIAN_POINT('Ctrl Pts',(202.181608405642,10.2457789925937,28.5953583997615));
#73861=CARTESIAN_POINT('Ctrl Pts',(202.179209599797,10.2191172016969,28.61802922611));
#73862=CARTESIAN_POINT('Ctrl Pts',(202.177573107094,10.2016279420082,28.6338289358867));
#73863=CARTESIAN_POINT('Ctrl Pts',(202.168164433066,10.1050545951264,28.7264837400066));
#73864=CARTESIAN_POINT('Ctrl Pts',(202.15994785122,10.036606398993,28.813618377259));
#73865=CARTESIAN_POINT('Ctrl Pts',(202.149860365087,9.9665980474703,28.9342861070032));
#73866=CARTESIAN_POINT('Ctrl Pts',(202.147769170218,9.9528569689626,28.9601448580042));
#73867=CARTESIAN_POINT('Ctrl Pts',(202.145113181235,9.93626771097557,28.9943858770252));
#73868=CARTESIAN_POINT('Ctrl Pts',(202.144505155025,9.93253089424146,29.002323655675));
#73869=CARTESIAN_POINT('Ctrl Pts',(202.143524132538,9.92659628328447,29.0153044567301));
#73870=CARTESIAN_POINT('Ctrl Pts',(202.14314810735,9.92434458167624,29.0203222614596));
#73871=CARTESIAN_POINT('Ctrl Pts',(202.142401887484,9.91992072897877,29.0303684108311));
#73872=CARTESIAN_POINT('Ctrl Pts',(202.142031687107,9.91774834296817,29.0353964970172));
#73873=CARTESIAN_POINT('Ctrl Pts',(202.141080789307,9.91222894697797,29.0484201886932));
#73874=CARTESIAN_POINT('Ctrl Pts',(202.140503104659,9.90893491206901,29.0564380826462));
#73875=CARTESIAN_POINT('Ctrl Pts',(202.137897873104,9.89436865289219,29.0930376925021));
#73876=CARTESIAN_POINT('Ctrl Pts',(202.135922137746,9.88412800905759,29.1220197890091));
#73877=CARTESIAN_POINT('Ctrl Pts',(202.130618443937,9.85933247914011,29.2020310365511));
#73878=CARTESIAN_POINT('Ctrl Pts',(202.127354402169,9.84707220739804,29.2536953932601));
#73879=CARTESIAN_POINT('Ctrl Pts',(202.120047762593,9.8276522411702,29.3699887905078));
#73880=CARTESIAN_POINT('Ctrl Pts',(202.116002863071,9.8222733154405,29.4347295545688));
#73881=CARTESIAN_POINT('Ctrl Pts',(202.111797459566,9.8222500756293,29.4995779279502));
#73882=CARTESIAN_POINT('Ctrl Pts',(202.111797390249,9.82225007524673,29.4995789968314));
#73883=CARTESIAN_POINT('Ctrl Pts',(202.110815059892,9.82224466046326,29.5147267707691));
#73884=CARTESIAN_POINT('Ctrl Pts',(202.109824898362,9.82253148291806,29.5298728065725));
#73885=CARTESIAN_POINT('Ctrl Pts',(202.108225926865,9.82345809938344,29.5541020106972));
#73886=CARTESIAN_POINT('Ctrl Pts',(202.107622749208,9.82391123110373,29.5631907553504));
#73887=CARTESIAN_POINT('Ctrl Pts',(202.106433228909,9.82500660924456,29.5810072000648));
#73888=CARTESIAN_POINT('Ctrl Pts',(202.105847166201,9.82564090147191,29.5897348066708));
#73889=CARTESIAN_POINT('Ctrl Pts',(202.104673854135,9.82709785043405,29.6071024061211));
#73890=CARTESIAN_POINT('Ctrl Pts',(202.104086690831,9.82791887480166,29.6157419841826));
#73891=CARTESIAN_POINT('Ctrl Pts',(202.102511124886,9.83036559446865,29.6387819218762));
#73892=CARTESIAN_POINT('Ctrl Pts',(202.101517551966,9.83216167784353,29.6531622850066));
#73893=CARTESIAN_POINT('Ctrl Pts',(202.097419651724,9.84059314690329,29.7118423120483));
#73894=CARTESIAN_POINT('Ctrl Pts',(202.094247697465,9.84948708032826,29.7557744767564));
#73895=CARTESIAN_POINT('Ctrl Pts',(202.08804442112,9.87134243596284,29.8390149254104));
#73896=CARTESIAN_POINT('Ctrl Pts',(202.085026047646,9.88391647458372,29.8783599405461));
#73897=CARTESIAN_POINT('Ctrl Pts',(202.078610468218,9.91489553506312,29.9601960921077));
#73898=CARTESIAN_POINT('Ctrl Pts',(202.075216367976,9.93379397194834,30.0024313043787));
#73899=CARTESIAN_POINT('Ctrl Pts',(202.070126924273,9.96645013082245,30.065218459771));
#73900=CARTESIAN_POINT('Ctrl Pts',(202.068383322709,9.97845184713072,30.0866317426348));
#73901=CARTESIAN_POINT('Ctrl Pts',(202.066112236727,9.99527814067069,30.1145682724623));
#73902=CARTESIAN_POINT('Ctrl Pts',(202.065554090862,9.99951254329009,30.1214378763027));
#73903=CARTESIAN_POINT('Ctrl Pts',(202.064632738586,10.0066736826792,30.1327926677804));
#73904=CARTESIAN_POINT('Ctrl Pts',(202.06426714154,10.0095609550455,30.1373023109949));
#73905=CARTESIAN_POINT('Ctrl Pts',(202.063567411522,10.0151771608702,30.145943924965));
#73906=CARTESIAN_POINT('Ctrl Pts',(202.063232974597,10.0179015365306,30.1500786021413));
#73907=CARTESIAN_POINT('Ctrl Pts',(202.062312070389,10.0255119565867,30.1614715930988));
#73908=CARTESIAN_POINT('Ctrl Pts',(202.061729069598,10.030453044844,30.1686929999087));
#73909=CARTESIAN_POINT('Ctrl Pts',(202.059233275113,10.0521150070246,30.1996070229639));
#73910=CARTESIAN_POINT('Ctrl Pts',(202.057365936619,10.0696285723152,30.222734561568));
#73911=CARTESIAN_POINT('Ctrl Pts',(202.055038058666,10.0928528699894,30.251158084902));
#73912=CARTESIAN_POINT('Ctrl Pts',(202.054551786683,10.0977829845227,30.2570724965672));
#73913=CARTESIAN_POINT('Ctrl Pts',(202.054067314992,10.1027691090856,30.2629362954329));
#73914=CARTESIAN_POINT('',(202.012132885264,9.82225039357706,29.5009628450546));
#73915=CARTESIAN_POINT('Ctrl Pts',(201.956062524555,10.1027690874833,30.2629362700282));
#73916=CARTESIAN_POINT('Ctrl Pts',(201.959231248475,10.0722998560055,30.2271037405805));
#73917=CARTESIAN_POINT('Ctrl Pts',(201.962399972395,10.0439770287748,30.1894390707115));
#73918=CARTESIAN_POINT('Ctrl Pts',(201.965568696315,10.0180161642766,30.1502328881854));
#73919=CARTESIAN_POINT('Ctrl Pts',(201.968740482662,9.99203020978663,30.1109888146717));
#73920=CARTESIAN_POINT('Ctrl Pts',(201.971912269009,9.96841108119265,30.0702007206587));
#73921=CARTESIAN_POINT('Ctrl Pts',(201.975084055356,9.94733054177144,30.0281875369722));
#73922=CARTESIAN_POINT('Ctrl Pts',(201.978257627242,9.92623813518307,29.9861507022082));
#73923=CARTESIAN_POINT('Ctrl Pts',(201.981431199127,9.90768738274832,29.9428879167524));
#73924=CARTESIAN_POINT('Ctrl Pts',(201.984604771013,9.89180212028469,29.8987386636564));
#73925=CARTESIAN_POINT('Ctrl Pts',(201.987784073839,9.87588817169199,29.8545096843881));
#73926=CARTESIAN_POINT('Ctrl Pts',(201.990963376665,9.86264947248109,29.8093915779742));
#73927=CARTESIAN_POINT('Ctrl Pts',(201.994142679492,9.85215965284453,29.7637377484207));
#73928=CARTESIAN_POINT('Ctrl Pts',(201.995279715924,9.84840810486501,29.7474102482393));
#73929=CARTESIAN_POINT('Ctrl Pts',(201.996416752356,9.84500766990641,29.7310142991353));
#73930=CARTESIAN_POINT('Ctrl Pts',(201.997553788788,9.84196010705662,29.7145662341835));
#73931=CARTESIAN_POINT('Ctrl Pts',(202.002413487614,9.82893480972929,29.6442671305995));
#73932=CARTESIAN_POINT('Ctrl Pts',(202.007273186439,9.8223090797843,29.57274766355));
#73933=CARTESIAN_POINT('Ctrl Pts',(202.012132885264,9.82225039357706,29.5009628450546));
#73934=CARTESIAN_POINT('Ctrl Pts',(202.012133243127,9.82166172758912,29.5009580375033));
#73935=CARTESIAN_POINT('Ctrl Pts',(202.033490724592,9.82444460082249,29.1853167740295));
#73936=CARTESIAN_POINT('Ctrl Pts',(202.081065505636,10.1166312015937,28.4776655224031));
#73937=CARTESIAN_POINT('Ctrl Pts',(202.154857586256,11.3065618033661,28.1464851504412));
#73938=CARTESIAN_POINT('Ctrl Pts',(202.233509484991,12.2989858935547,29.0115143445247));
#73939=CARTESIAN_POINT('Ctrl Pts',(202.312161383725,12.122459760303,30.3161290791044));
#73940=CARTESIAN_POINT('Ctrl Pts',(202.386322574714,11.003589618022,30.8537585105574));
#73941=CARTESIAN_POINT('Ctrl Pts',(202.434266466125,10.3124415083501,30.5059938962083));
#73942=CARTESIAN_POINT('Ctrl Pts',(202.455993057958,10.1022055060817,30.2634229920695));
#73943=CARTESIAN_POINT('Origin',(197.762132885264,11.,29.5));
#73944=CARTESIAN_POINT('',(203.055732095072,10.1027690874946,30.2629362700414));
#73945=CARTESIAN_POINT('',(202.956095255396,10.1027690874833,30.2629362700282));
#73946=CARTESIAN_POINT('',(197.762132885264,10.1027690874833,30.2629362700282));
#73947=CARTESIAN_POINT('Ctrl Pts',(203.055732095072,10.1027690874946,30.2629362700414));
#73948=CARTESIAN_POINT('Ctrl Pts',(203.055680843042,10.1032781498017,30.2635349392308));
#73949=CARTESIAN_POINT('Ctrl Pts',(203.055629568757,10.1037878130808,30.264133101021));
#73950=CARTESIAN_POINT('Ctrl Pts',(203.054627409232,10.1137565972493,30.2758091832254));
#73951=CARTESIAN_POINT('Ctrl Pts',(203.053669019665,10.1234194835438,30.2867107637418));
#73952=CARTESIAN_POINT('Ctrl Pts',(203.052647775855,10.1338394543902,30.2980361208704));
#73953=CARTESIAN_POINT('Ctrl Pts',(203.05259308966,10.1343978004303,30.2986417050714));
#73954=CARTESIAN_POINT('Ctrl Pts',(203.05248303782,10.1355221718152,30.2998586382674));
#73955=CARTESIAN_POINT('Ctrl Pts',(203.052427671609,10.1360882114565,30.3004699733555));
#73956=CARTESIAN_POINT('Ctrl Pts',(203.052315191132,10.1372389239659,30.3017101255663));
#73957=CARTESIAN_POINT('Ctrl Pts',(203.052258075249,10.1378236366753,30.3023389048731));
#73958=CARTESIAN_POINT('Ctrl Pts',(203.052184527674,10.1385770753782,30.3031473514772));
#73959=CARTESIAN_POINT('Ctrl Pts',(203.052168121955,10.1387451720562,30.3033276072637));
#73960=CARTESIAN_POINT('Ctrl Pts',(203.05212771863,10.1391592337816,30.3037713403921));
#73961=CARTESIAN_POINT('Ctrl Pts',(203.05210371837,10.1394052631049,30.304034757487));
#73962=CARTESIAN_POINT('Ctrl Pts',(203.052042729131,10.1400306470631,30.3047037236707));
#73963=CARTESIAN_POINT('Ctrl Pts',(203.052005733301,10.1404101673567,30.3051091171356));
#73964=CARTESIAN_POINT('Ctrl Pts',(203.051906171747,10.1414319576996,30.3061990202835));
#73965=CARTESIAN_POINT('Ctrl Pts',(203.051843584017,10.1420747585667,30.3068830297314));
#73966=CARTESIAN_POINT('Ctrl Pts',(203.051167479638,10.1490236547461,30.3142597135316));
#73967=CARTESIAN_POINT('Ctrl Pts',(203.050550754934,10.1554069532658,30.3208789183382));
#73968=CARTESIAN_POINT('Ctrl Pts',(203.049237100713,10.16909327834,30.3347424048816));
#73969=CARTESIAN_POINT('Ctrl Pts',(203.048539392156,10.1764149779946,30.341967079295));
#73970=CARTESIAN_POINT('Ctrl Pts',(203.046633966654,10.1965459228127,30.3613174168705));
#73971=CARTESIAN_POINT('Ctrl Pts',(203.04541840481,10.2095340063792,30.3732523128998));
#73972=CARTESIAN_POINT('Ctrl Pts',(203.038084981684,10.2887110509025,30.4427949462142));
#73973=CARTESIAN_POINT('Ctrl Pts',(203.031681283272,10.3608914857695,30.4931411840402));
#73974=CARTESIAN_POINT('Ctrl Pts',(203.022267843458,10.4737248643307,30.5544118795783));
#73975=CARTESIAN_POINT('Ctrl Pts',(203.01929087227,10.510457895681,30.5719602586778));
#73976=CARTESIAN_POINT('Ctrl Pts',(203.014738385877,10.5690456783002,30.5963081303578));
#73977=CARTESIAN_POINT('Ctrl Pts',(203.013124362118,10.5903147573183,30.6044325703768));
#73978=CARTESIAN_POINT('Ctrl Pts',(203.010993040844,10.6192317412858,30.6145278971009));
#73979=CARTESIAN_POINT('Ctrl Pts',(203.010449461822,10.6266820344865,30.6170454803909));
#73980=CARTESIAN_POINT('Ctrl Pts',(203.009545315264,10.6392099006661,30.6211395196765));
#73981=CARTESIAN_POINT('Ctrl Pts',(203.009182539078,10.6442738607892,30.6227565349147));
#73982=CARTESIAN_POINT('Ctrl Pts',(203.008433252243,10.6548140336075,30.6260437312999));
#73983=CARTESIAN_POINT('Ctrl Pts',(203.008047045596,10.6602917430333,30.6277083575887));
#73984=CARTESIAN_POINT('Ctrl Pts',(203.007004280114,10.6751966696347,30.6321193700147));
#73985=CARTESIAN_POINT('Ctrl Pts',(203.006351911604,10.6846466765809,30.6347879837958));
#73986=CARTESIAN_POINT('Ctrl Pts',(203.002164895242,10.7460214579951,30.6512938443267));
#73987=CARTESIAN_POINT('Ctrl Pts',(202.998791908116,10.7988145861149,30.6616834621295));
#73988=CARTESIAN_POINT('Ctrl Pts',(202.992769888853,10.894926854562,30.6738461823303));
#73989=CARTESIAN_POINT('Ctrl Pts',(202.990114214701,10.9379801782754,30.6769064415476));
#73990=CARTESIAN_POINT('Ctrl Pts',(202.98397387263,11.0365449798987,30.6784880093941));
#73991=CARTESIAN_POINT('Ctrl Pts',(202.980474848749,11.0919731100244,30.6754613590028));
#73992=CARTESIAN_POINT('Ctrl Pts',(202.975877275283,11.1618656840739,30.6666703536199));
#73993=CARTESIAN_POINT('Ctrl Pts',(202.974889972326,11.1767157005816,30.6645135215963));
#73994=CARTESIAN_POINT('Ctrl Pts',(202.973247102297,11.2011345833073,30.6604890754538));
#73995=CARTESIAN_POINT('Ctrl Pts',(202.972596641371,11.2107289459064,30.6587852763489));
#73996=CARTESIAN_POINT('Ctrl Pts',(202.971318688234,11.2294276491071,30.6552247986348));
#73997=CARTESIAN_POINT('Ctrl Pts',(202.970691580828,11.2385333564163,30.6533790404657));
#73998=CARTESIAN_POINT('Ctrl Pts',(202.969170521598,11.2604449155126,30.6486669227774));
#73999=CARTESIAN_POINT('Ctrl Pts',(202.968273291072,11.2732263043942,30.6456939452318));
#74000=CARTESIAN_POINT('Ctrl Pts',(202.965153367229,11.3171608775189,30.634697693232));
#74001=CARTESIAN_POINT('Ctrl Pts',(202.962898111862,11.3480309674229,30.6256127175271));
#74002=CARTESIAN_POINT('Ctrl Pts',(202.954032973177,11.4659757254293,30.5855861397693));
#74003=CARTESIAN_POINT('Ctrl Pts',(202.947174156403,11.5496610942254,30.5457054026598));
#74004=CARTESIAN_POINT('Ctrl Pts',(202.938813610157,11.6471416240832,30.4842889339539));
#74005=CARTESIAN_POINT('Ctrl Pts',(202.937169021679,11.666113520727,30.4715502473107));
#74006=CARTESIAN_POINT('Ctrl Pts',(202.934445477494,11.6973457816444,30.4492340790081));
#74007=CARTESIAN_POINT('Ctrl Pts',(202.933354180476,11.7098084929985,30.4399512939669));
#74008=CARTESIAN_POINT('Ctrl Pts',(202.931804333534,11.7274791297496,30.4262374467272));
#74009=CARTESIAN_POINT('Ctrl Pts',(202.931334035724,11.7328373648677,30.4220038471901));
#74010=CARTESIAN_POINT('Ctrl Pts',(202.930513096468,11.7421886970022,30.4144822302504));
#74011=CARTESIAN_POINT('Ctrl Pts',(202.930161151955,11.7461973778875,30.4112141834317));
#74012=CARTESIAN_POINT('Ctrl Pts',(202.929387288056,11.7550115095409,30.4039313513662));
#74013=CARTESIAN_POINT('Ctrl Pts',(202.928966216342,11.7598066278451,30.3999045283765));
#74014=CARTESIAN_POINT('Ctrl Pts',(202.927717016697,11.7740209647889,30.3877730600783));
#74015=CARTESIAN_POINT('Ctrl Pts',(202.926896294633,11.7833446006181,30.379557119491));
#74016=CARTESIAN_POINT('Ctrl Pts',(202.922710967772,11.8306909423731,30.3364855536004));
#74017=CARTESIAN_POINT('Ctrl Pts',(202.919481849449,11.8665279785901,30.2993034108727));
#74018=CARTESIAN_POINT('Ctrl Pts',(202.913535620728,11.9283039056173,30.2261519439091));
#74019=CARTESIAN_POINT('Ctrl Pts',(202.910816554321,11.9548732780497,30.1908413557434));
#74020=CARTESIAN_POINT('Ctrl Pts',(202.904784716255,12.0085664476718,30.1104482551197));
#74021=CARTESIAN_POINT('Ctrl Pts',(202.901462639821,12.0347786643422,30.0648765558394));
#74022=CARTESIAN_POINT('Ctrl Pts',(202.8970664188,12.0643751118692,30.0044009185384));
#74023=CARTESIAN_POINT('Ctrl Pts',(202.896091023205,12.0706371536587,29.9909691628448));
#74024=CARTESIAN_POINT('Ctrl Pts',(202.894462614784,12.080578718015,29.9685498037149));
#74025=CARTESIAN_POINT('Ctrl Pts',(202.893814522233,12.0844035991361,29.9596282292777));
#74026=CARTESIAN_POINT('Ctrl Pts',(202.892537267893,12.091681752065,29.9420551674603));
#74027=CARTESIAN_POINT('Ctrl Pts',(202.8919084453,12.0951435290475,29.9334079615581));
#74028=CARTESIAN_POINT('Ctrl Pts',(202.890376220481,12.1032835029046,29.912354649154));
#74029=CARTESIAN_POINT('Ctrl Pts',(202.889469418248,12.1078553795046,29.8999090870023));
#74030=CARTESIAN_POINT('Ctrl Pts',(202.88627442573,12.1231051703897,29.8561261108039));
#74031=CARTESIAN_POINT('Ctrl Pts',(202.883951519012,12.1326703187605,29.8244204337307));
#74032=CARTESIAN_POINT('Ctrl Pts',(202.875321200213,12.1627358145608,29.7070933788016));
#74033=CARTESIAN_POINT('Ctrl Pts',(202.868797896447,12.1749561833651,29.6196543094049));
#74034=CARTESIAN_POINT('Ctrl Pts',(202.860603847715,12.1779880007342,29.5070022994887));
#74035=CARTESIAN_POINT('Ctrl Pts',(202.858822267767,12.1778759334513,29.4823028715509));
#74036=CARTESIAN_POINT('Ctrl Pts',(202.855901017729,12.1763968956361,29.4412228894436));
#74037=CARTESIAN_POINT('Ctrl Pts',(202.854746807826,12.1754636066253,29.4248349871955));
#74038=CARTESIAN_POINT('Ctrl Pts',(202.853125269173,12.1736460752085,29.4015186213488));
#74039=CARTESIAN_POINT('Ctrl Pts',(202.852644716915,12.1730423771763,29.3945709759028));
#74040=CARTESIAN_POINT('Ctrl Pts',(202.85181264557,12.171882352138,29.3824683395311));
#74041=CARTESIAN_POINT('Ctrl Pts',(202.851459696122,12.1713536465001,29.3773110556263));
#74042=CARTESIAN_POINT('Ctrl Pts',(202.850691619274,12.1701223728775,29.366034995921));
#74043=CARTESIAN_POINT('Ctrl Pts',(202.850277242421,12.1694058481839,29.3599180373785));
#74044=CARTESIAN_POINT('Ctrl Pts',(202.849092397077,12.167207046065,29.3423412191106));
#74045=CARTESIAN_POINT('Ctrl Pts',(202.848328100148,12.1656040163684,29.3308968340791));
#74046=CARTESIAN_POINT('Ctrl Pts',(202.842847317745,12.1527817371813,29.24823135497));
#74047=CARTESIAN_POINT('Ctrl Pts',(202.838409050936,12.1352104187687,29.1781410722922));
#74048=CARTESIAN_POINT('Ctrl Pts',(202.830816480958,12.0946178772813,29.06244240569));
#74049=CARTESIAN_POINT('Ctrl Pts',(202.827685327214,12.0748540342913,29.0159201462508));
#74050=CARTESIAN_POINT('Ctrl Pts',(202.822465190349,12.0379475106917,28.9425401119848));
#74051=CARTESIAN_POINT('Ctrl Pts',(202.820426284475,12.0225954238784,28.9148548074865));
#74052=CARTESIAN_POINT('Ctrl Pts',(202.817514404407,11.9995378481877,28.8769583579396));
#74053=CARTESIAN_POINT('Ctrl Pts',(202.816673700478,11.9927521488411,28.8662019657554));
#74054=CARTESIAN_POINT('Ctrl Pts',(202.815206204755,11.9806961195293,28.8477600313134));
#74055=CARTESIAN_POINT('Ctrl Pts',(202.814582382036,11.9755062121205,28.8400231236357));
#74056=CARTESIAN_POINT('Ctrl Pts',(202.813288878381,11.964615496345,28.8241968261762));
#74057=CARTESIAN_POINT('Ctrl Pts',(202.812618811956,11.9589034392141,28.8161161139785));
#74058=CARTESIAN_POINT('Ctrl Pts',(202.810872551444,11.9438405194629,28.795366726435));
#74059=CARTESIAN_POINT('Ctrl Pts',(202.809790622335,11.9343364768442,28.7828122399104));
#74060=CARTESIAN_POINT('Ctrl Pts',(202.804141480277,11.8838563209864,28.7188367650232));
#74061=CARTESIAN_POINT('Ctrl Pts',(202.799419252803,11.8388844241077,28.6707301712796));
#74062=CARTESIAN_POINT('Ctrl Pts',(202.790264333226,11.7459129723658,28.5866182531947));
#74063=CARTESIAN_POINT('Ctrl Pts',(202.785860359933,11.6987083496574,28.550021470181));
#74064=CARTESIAN_POINT('Ctrl Pts',(202.779523365885,11.6254627175357,28.5016601115336));
#74065=CARTESIAN_POINT('Ctrl Pts',(202.777517313253,11.601441470568,28.4870071209755));
#74066=CARTESIAN_POINT('Ctrl Pts',(202.774967519875,11.5695615095073,28.4690946086997));
#74067=CARTESIAN_POINT('Ctrl Pts',(202.774383337573,11.5621619376391,28.4650409645794));
#74068=CARTESIAN_POINT('Ctrl Pts',(202.773430952061,11.5499305941691,28.4585102632211));
#74069=CARTESIAN_POINT('Ctrl Pts',(202.773060028539,11.545124234702,28.4559865409443));
#74070=CARTESIAN_POINT('Ctrl Pts',(202.772359851088,11.535966984788,28.4512587362909));
#74071=CARTESIAN_POINT('Ctrl Pts',(202.77203019341,11.5316195730708,28.4490482986031));
#74072=CARTESIAN_POINT('Ctrl Pts',(202.771139869936,11.5197845981412,28.4431230469294));
#74073=CARTESIAN_POINT('Ctrl Pts',(202.770582289674,11.5122708547884,28.4394607487037));
#74074=CARTESIAN_POINT('Ctrl Pts',(202.76837294971,11.4821223770687,28.4251611633876));
#74075=CARTESIAN_POINT('Ctrl Pts',(202.766754577643,11.4591887894553,28.4151652821945));
#74076=CARTESIAN_POINT('Ctrl Pts',(202.760508462554,11.3681958896788,28.3789082449727));
#74077=CARTESIAN_POINT('Ctrl Pts',(202.756061716407,11.2980736246609,28.3582607568604));
#74078=CARTESIAN_POINT('Ctrl Pts',(202.749151273178,11.1891143927155,28.3369087664863));
#74079=CARTESIAN_POINT('Ctrl Pts',(202.746761534561,11.1514098555323,28.3314024538564));
#74080=CARTESIAN_POINT('Ctrl Pts',(202.742636273087,11.0872377364288,28.3251888764688));
#74081=CARTESIAN_POINT('Ctrl Pts',(202.740926536077,11.0608922317289,28.3235291871946));
#74082=CARTESIAN_POINT('Ctrl Pts',(202.738405999966,11.0226011179861,28.3224065615593));
#74083=CARTESIAN_POINT('Ctrl Pts',(202.737616553207,11.0106833403763,28.3222381539321));
#74084=CARTESIAN_POINT('Ctrl Pts',(202.736207610044,10.989561162409,28.3222602955815));
#74085=CARTESIAN_POINT('Ctrl Pts',(202.735590398887,10.9803575762404,28.3223778416808));
#74086=CARTESIAN_POINT('Ctrl Pts',(202.734279188534,10.9609157152983,28.3228541218712));
#74087=CARTESIAN_POINT('Ctrl Pts',(202.733584450051,10.9506788985628,28.3232385894829));
#74088=CARTESIAN_POINT('Ctrl Pts',(202.731696215378,10.9230379234061,28.3246380079384));
#74089=CARTESIAN_POINT('Ctrl Pts',(202.7304951147,10.9056497422518,28.3259059037964));
#74090=CARTESIAN_POINT('Ctrl Pts',(202.722146413182,10.7861721740504,28.3372890096141));
#74091=CARTESIAN_POINT('Ctrl Pts',(202.714591947284,10.6857714163812,28.360319457924));
#74092=CARTESIAN_POINT('Ctrl Pts',(202.704835598859,10.5606254772465,28.4068377045368));
#74093=CARTESIAN_POINT('Ctrl Pts',(202.702586784527,10.5320375337698,28.4187668478015));
#74094=CARTESIAN_POINT('Ctrl Pts',(202.699434230431,10.4919845989892,28.4373667124116));
#74095=CARTESIAN_POINT('Ctrl Pts',(202.698499505484,10.4801114007151,28.4431248765721));
#74096=CARTESIAN_POINT('Ctrl Pts',(202.696847966787,10.4590990843684,28.4537550755485));
#74097=CARTESIAN_POINT('Ctrl Pts',(202.696127656477,10.4499228236178,28.4585503561841));
#74098=CARTESIAN_POINT('Ctrl Pts',(202.695011820326,10.4356721149258,28.4662383304664));
#74099=CARTESIAN_POINT('Ctrl Pts',(202.694611657582,10.4305541653932,28.4690486935046));
#74100=CARTESIAN_POINT('Ctrl Pts',(202.693855194093,10.4208613809318,28.4744653881438));
#74101=CARTESIAN_POINT('Ctrl Pts',(202.693498502634,10.4162828478185,28.4770644851774));
#74102=CARTESIAN_POINT('Ctrl Pts',(202.692714019237,10.4061986483785,28.4828787370349));
#74103=CARTESIAN_POINT('Ctrl Pts',(202.692287098517,10.4007012857268,28.4861081101428));
#74104=CARTESIAN_POINT('Ctrl Pts',(202.690820638438,10.3817975197126,28.4974204221378));
#74105=CARTESIAN_POINT('Ctrl Pts',(202.689793854242,10.3685256027968,28.5057262661534));
#74106=CARTESIAN_POINT('Ctrl Pts',(202.683424349168,10.2863011080919,28.5594949332292));
#74107=CARTESIAN_POINT('Ctrl Pts',(202.678402752934,10.2221184000583,28.6118450978308));
#74108=CARTESIAN_POINT('Ctrl Pts',(202.670801216305,10.1360005821777,28.6986428328698));
#74109=CARTESIAN_POINT('Ctrl Pts',(202.668316523167,10.1095060957555,28.7281913549308));
#74110=CARTESIAN_POINT('Ctrl Pts',(202.664047620732,10.0674885565508,28.7801019418046));
#74111=CARTESIAN_POINT('Ctrl Pts',(202.662291833948,10.0511576767984,28.8017673180915));
#74112=CARTESIAN_POINT('Ctrl Pts',(202.659716200441,10.0286803261493,28.8338333036164));
#74113=CARTESIAN_POINT('Ctrl Pts',(202.658919095352,10.0219223088576,28.843795772036));
#74114=CARTESIAN_POINT('Ctrl Pts',(202.657501573814,10.0102608438711,28.8615671936962));
#74115=CARTESIAN_POINT('Ctrl Pts',(202.656883543495,10.0052940965329,28.869333524916));
#74116=CARTESIAN_POINT('Ctrl Pts',(202.655575836246,9.99503453246077,28.8857987765837));
#74117=CARTESIAN_POINT('Ctrl Pts',(202.654885479561,9.98976235763914,28.8945095966244));
#74118=CARTESIAN_POINT('Ctrl Pts',(202.653022544091,9.97592383109144,28.9180579291021));
#74119=CARTESIAN_POINT('Ctrl Pts',(202.651842708975,9.96756747539825,28.9330153416418));
#74120=CARTESIAN_POINT('Ctrl Pts',(202.643424956179,9.91083221083597,29.0399839594525));
#74121=CARTESIAN_POINT('Ctrl Pts',(202.635766425098,9.87450427603867,29.1378502867752));
#74122=CARTESIAN_POINT('Ctrl Pts',(202.62595135567,9.8447502920661,29.2688722253721));
#74123=CARTESIAN_POINT('Ctrl Pts',(202.623741271508,9.83916153736228,29.2988129817721));
#74124=CARTESIAN_POINT('Ctrl Pts',(202.620636630948,9.8328427917312,29.3418558450068));
#74125=CARTESIAN_POINT('Ctrl Pts',(202.619711978533,9.83116131894318,29.3548046486921));
#74126=CARTESIAN_POINT('Ctrl Pts',(202.618076318371,9.82854248947339,29.3779842841225));
#74127=CARTESIAN_POINT('Ctrl Pts',(202.617361904896,9.82752301187368,29.3882043654187));
#74128=CARTESIAN_POINT('Ctrl Pts',(202.616253121267,9.82613533765032,29.4042362220099));
#74129=CARTESIAN_POINT('Ctrl Pts',(202.615854204919,9.82567635150799,29.4100393480641));
#74130=CARTESIAN_POINT('Ctrl Pts',(202.615098540063,9.82488372064845,29.4211039742857));
#74131=CARTESIAN_POINT('Ctrl Pts',(202.61474141895,9.82454235063374,29.4263646250114));
#74132=CARTESIAN_POINT('Ctrl Pts',(202.613954494939,9.82386441492197,29.4380227049632));
#74133=CARTESIAN_POINT('Ctrl Pts',(202.613525584593,9.82354469624644,29.4444210255535));
#74134=CARTESIAN_POINT('Ctrl Pts',(202.612019626454,9.82259988548525,29.4670282102739));
#74135=CARTESIAN_POINT('Ctrl Pts',(202.610956421556,9.82225741589799,29.4832478281828));
#74136=CARTESIAN_POINT('Ctrl Pts',(202.608292383451,9.82223891553685,29.5243782920293));
#74137=CARTESIAN_POINT('Ctrl Pts',(202.606709136802,9.82301788011519,29.5492819480859));
#74138=CARTESIAN_POINT('Ctrl Pts',(202.599236485343,9.83049718147126,29.6678529509664));
#74139=CARTESIAN_POINT('Ctrl Pts',(202.593563375472,9.84759260540199,29.7605174382398));
#74140=CARTESIAN_POINT('Ctrl Pts',(202.585762568486,9.88397375315317,29.8773468721764));
#74141=CARTESIAN_POINT('Ctrl Pts',(202.583924565957,9.89341845913494,29.9042058166407));
#74142=CARTESIAN_POINT('Ctrl Pts',(202.581310258946,9.90797830106162,29.9412624933523));
#74143=CARTESIAN_POINT('Ctrl Pts',(202.580560010367,9.91228290717186,29.9517692889339));
#74144=CARTESIAN_POINT('Ctrl Pts',(202.579182362429,9.92041068852575,29.9708179357425));
#74145=CARTESIAN_POINT('Ctrl Pts',(202.578556616415,9.9241850848633,29.9793796720359));
#74146=CARTESIAN_POINT('Ctrl Pts',(202.577278736077,9.93205712452158,29.9966750750828));
#74147=CARTESIAN_POINT('Ctrl Pts',(202.576626434617,9.93616085624116,30.0054051664011));
#74148=CARTESIAN_POINT('Ctrl Pts',(202.574983263801,9.94670784972809,30.0271446196849));
#74149=CARTESIAN_POINT('Ctrl Pts',(202.573987895985,9.95328512521703,30.0400867915711));
#74150=CARTESIAN_POINT('Ctrl Pts',(202.569638853393,9.98281966813092,30.0956353175832));
#74151=CARTESIAN_POINT('Ctrl Pts',(202.566204732469,10.0081489902168,30.1369205345175));
#74152=CARTESIAN_POINT('Ctrl Pts',(202.560074241281,10.0568819520254,30.2063655021954));
#74153=CARTESIAN_POINT('Ctrl Pts',(202.557410233282,10.0791829978597,30.2351984861022));
#74154=CARTESIAN_POINT('Ctrl Pts',(202.554740968482,10.1027692175106,30.2629364229433));
#74155=CARTESIAN_POINT('',(202.512132885264,9.82241330366484,29.4997412329417));
#74156=CARTESIAN_POINT('Ctrl Pts',(202.455993057958,10.1022055060817,30.2634229920695));
#74157=CARTESIAN_POINT('Ctrl Pts',(202.460483765703,10.0587514544313,30.2132855822843));
#74158=CARTESIAN_POINT('Ctrl Pts',(202.479197041472,9.89600478671947,29.9892296846299));
#74159=CARTESIAN_POINT('Ctrl Pts',(202.49791031724,9.82442155048356,29.7110002446274));
#74160=CARTESIAN_POINT('Ctrl Pts',(202.512132885264,9.82399939596064,29.4997415814752));
#74161=CARTESIAN_POINT('Ctrl Pts',(202.512132885264,9.82225002843514,29.499741197063));
#74162=CARTESIAN_POINT('Ctrl Pts',(202.515518432404,9.82226109535632,29.4493782983299));
#74163=CARTESIAN_POINT('Ctrl Pts',(202.518903979543,9.82550685479233,29.3990983077968));
#74164=CARTESIAN_POINT('Ctrl Pts',(202.522289526683,9.83193010758237,29.3493089620201));
#74165=CARTESIAN_POINT('Ctrl Pts',(202.525682877626,9.83836816619204,29.299404850081));
#74166=CARTESIAN_POINT('Ctrl Pts',(202.529076228569,9.84799823769769,29.2499940631929));
#74167=CARTESIAN_POINT('Ctrl Pts',(202.532469579511,9.86071226979931,29.2014727310376));
#74168=CARTESIAN_POINT('Ctrl Pts',(202.535875585276,9.87347371633343,29.1527704483065));
#74169=CARTESIAN_POINT('Ctrl Pts',(202.539281591041,9.88934198360819,29.1049646660309));
#74170=CARTESIAN_POINT('Ctrl Pts',(202.542687596805,9.90815950392749,29.0584352894126));
#74171=CARTESIAN_POINT('Ctrl Pts',(202.544497424512,9.91815845049761,29.0337112693051));
#74172=CARTESIAN_POINT('Ctrl Pts',(202.54630725222,9.92898931246574,29.0093472532393));
#74173=CARTESIAN_POINT('Ctrl Pts',(202.548117079927,9.94062323588956,28.9853973045515));
#74174=CARTESIAN_POINT('Ctrl Pts',(202.551394242374,9.96168947153411,28.9420297109759));
#74175=CARTESIAN_POINT('Ctrl Pts',(202.554671404822,9.98547061576457,28.8998599900416));
#74176=CARTESIAN_POINT('Ctrl Pts',(202.557948567269,10.0118041206999,28.8592473436386));
#74177=CARTESIAN_POINT('Ctrl Pts',(202.561122519601,10.0373082849678,28.8199137415311));
#74178=CARTESIAN_POINT('Ctrl Pts',(202.564296471932,10.0652060874267,28.7820410933764));
#74179=CARTESIAN_POINT('Ctrl Pts',(202.567470424264,10.0953023489157,28.7459328792325));
#74180=CARTESIAN_POINT('Ctrl Pts',(202.570641251632,10.1253689786737,28.7098602159789));
#74181=CARTESIAN_POINT('Ctrl Pts',(202.573812079001,10.1576294280711,28.6755489740434));
#74182=CARTESIAN_POINT('Ctrl Pts',(202.57698290637,10.1918464743423,28.6432719559469));
#74183=CARTESIAN_POINT('Ctrl Pts',(202.580152003315,10.2260448472609,28.6110125524667));
#74184=CARTESIAN_POINT('Ctrl Pts',(202.58332110026,10.262197297307,28.5807855550173));
#74185=CARTESIAN_POINT('Ctrl Pts',(202.586490197205,10.300029626991,28.5528270805129));
#74186=CARTESIAN_POINT('Ctrl Pts',(202.589658955268,10.3378579111343,28.5248715957041));
#74187=CARTESIAN_POINT('Ctrl Pts',(202.592827713331,10.3773652693388,28.4991844811355));
#74188=CARTESIAN_POINT('Ctrl Pts',(202.595996471394,10.4182464671013,28.4759600156928));
#74189=CARTESIAN_POINT('Ctrl Pts',(202.599168415829,10.4591687733149,28.4527121966829));
#74190=CARTESIAN_POINT('Ctrl Pts',(202.602340360265,10.5014671895777,28.431932241392));
#74191=CARTESIAN_POINT('Ctrl Pts',(202.6055123047,10.5448114327462,28.4137687029268));
#74192=CARTESIAN_POINT('Ctrl Pts',(202.608686193971,10.5881822518494,28.3955940277343));
#74193=CARTESIAN_POINT('Ctrl Pts',(202.611860083241,10.6325996482413,28.3800391456787));
#74194=CARTESIAN_POINT('Ctrl Pts',(202.615033972511,10.677716309635,28.3672033344749));
#74195=CARTESIAN_POINT('Ctrl Pts',(202.61821347699,10.7229127909046,28.3543448143023));
#74196=CARTESIAN_POINT('Ctrl Pts',(202.621392981468,10.7688104610883,28.3442150768383));
#74197=CARTESIAN_POINT('Ctrl Pts',(202.624572485947,10.8150518504685,28.3368623278026));
#74198=CARTESIAN_POINT('Ctrl Pts',(202.625304650185,10.8257001423181,28.3351691646282));
#74199=CARTESIAN_POINT('Ctrl Pts',(202.626036814423,10.8363666458221,28.3336230393355));
#74200=CARTESIAN_POINT('Ctrl Pts',(202.626768978661,10.8470469817718,28.3322241496268));
#74201=CARTESIAN_POINT('Ctrl Pts',(202.630046141109,10.8948520971775,28.325962728237));
#74202=CARTESIAN_POINT('Ctrl Pts',(202.633323303556,10.9431501762926,28.3226275013512));
#74203=CARTESIAN_POINT('Ctrl Pts',(202.636600466003,10.9915518289659,28.3222803003659));
#74204=CARTESIAN_POINT('Ctrl Pts',(202.639774418335,11.0384291323728,28.3219440340396));
#74205=CARTESIAN_POINT('Ctrl Pts',(202.642948370666,11.0854029767498,28.324410368306));
#74206=CARTESIAN_POINT('Ctrl Pts',(202.646122322998,11.1321125579884,28.3296832332562));
#74207=CARTESIAN_POINT('Ctrl Pts',(202.649293150366,11.1787761505999,28.3349509067272));
#74208=CARTESIAN_POINT('Ctrl Pts',(202.652463977735,11.2251754441529,28.3430195792481));
#74209=CARTESIAN_POINT('Ctrl Pts',(202.655634805104,11.2709521280664,28.3538411947744));
#74210=CARTESIAN_POINT('Ctrl Pts',(202.658803902049,11.3167038301579,28.3646569045938));
#74211=CARTESIAN_POINT('Ctrl Pts',(202.661972998994,11.3618330547225,28.3782224532127));
#74212=CARTESIAN_POINT('Ctrl Pts',(202.665142095939,11.4059917903771,28.3944387268693));
#74213=CARTESIAN_POINT('Ctrl Pts',(202.668310854002,11.4501458039867,28.4106532664641));
#74214=CARTESIAN_POINT('Ctrl Pts',(202.671479612065,11.4933290131051,28.4295177743398));
#74215=CARTESIAN_POINT('Ctrl Pts',(202.674648370128,11.5352112745426,28.4508842036732));
#74216=CARTESIAN_POINT('Ctrl Pts',(202.677820314563,11.5771356510597,28.4722721182091));
#74217=CARTESIAN_POINT('Ctrl Pts',(202.680992258999,11.6177559739234,28.4961667186593));
#74218=CARTESIAN_POINT('Ctrl Pts',(202.684164203435,11.6567665088359,28.5223738877406));
#74219=CARTESIAN_POINT('Ctrl Pts',(202.687338092705,11.6958009625288,28.5485971253921));
#74220=CARTESIAN_POINT('Ctrl Pts',(202.690511981975,11.7332232213621,28.5771354154916));
#74221=CARTESIAN_POINT('Ctrl Pts',(202.693685871246,11.7687593354638,28.6077533151436));
#74222=CARTESIAN_POINT('Ctrl Pts',(202.696865375724,11.804358319648,28.63842538363));
#74223=CARTESIAN_POINT('Ctrl Pts',(202.700044880203,11.838064106692,28.6711840104192));
#74224=CARTESIAN_POINT('Ctrl Pts',(202.703224384681,11.8696398113512,28.7057571775502));
#74225=CARTESIAN_POINT('Ctrl Pts',(202.70395654892,11.87691094492,28.7137185554139));
#74226=CARTESIAN_POINT('Ctrl Pts',(202.704688713158,11.8840693001278,28.7217760209683));
#74227=CARTESIAN_POINT('Ctrl Pts',(202.705420877396,11.8911123030715,28.7299260257516));
#74228=CARTESIAN_POINT('Ctrl Pts',(202.708698039843,11.922636739202,28.7664053950365));
#74229=CARTESIAN_POINT('Ctrl Pts',(202.71197520229,11.9519885788489,28.8049060144331));
#74230=CARTESIAN_POINT('Ctrl Pts',(202.715252364738,11.9789019996351,28.8451367031124));
#74231=CARTESIAN_POINT('Ctrl Pts',(202.718426317069,12.0049678160328,28.8841003767756));
#74232=CARTESIAN_POINT('Ctrl Pts',(202.721600269401,12.0287461994947,28.9246862528936));
#74233=CARTESIAN_POINT('Ctrl Pts',(202.724774221732,12.0500354065866,28.9665951749238));
#74234=CARTESIAN_POINT('Ctrl Pts',(202.727945049101,12.0713036530665,29.0084628348886));
#74235=CARTESIAN_POINT('Ctrl Pts',(202.73111587647,12.0900873230514,29.0516504680771));
#74236=CARTESIAN_POINT('Ctrl Pts',(202.734286703838,12.1062294598556,29.095832405248));
#74237=CARTESIAN_POINT('Ctrl Pts',(202.737455800784,12.1223627873718,29.1399902309018));
#74238=CARTESIAN_POINT('Ctrl Pts',(202.740624897729,12.1358572467915,29.1851407633922));
#74239=CARTESIAN_POINT('Ctrl Pts',(202.743793994674,12.1466041863574,29.2309388502076));
#74240=CARTESIAN_POINT('Ctrl Pts',(202.746962752737,12.1573499767163,29.2767320396764));
#74241=CARTESIAN_POINT('Ctrl Pts',(202.7501315108,12.1653487056253,29.3231721036627));
#74242=CARTESIAN_POINT('Ctrl Pts',(202.753300268863,12.1705424152397,29.3699018961518));
#74243=CARTESIAN_POINT('Ctrl Pts',(202.756472213298,12.1757413474348,29.4166786781985));
#74244=CARTESIAN_POINT('Ctrl Pts',(202.759644157734,12.1781295729463,29.4637452155598));
#74245=CARTESIAN_POINT('Ctrl Pts',(202.76281610217,12.1777010349264,29.510739405633));
#74246=CARTESIAN_POINT('Ctrl Pts',(202.76598999144,12.1772722341542,29.5577624095565));
#74247=CARTESIAN_POINT('Ctrl Pts',(202.76916388071,12.1740232716144,29.604712422341));
#74248=CARTESIAN_POINT('Ctrl Pts',(202.772337769981,12.1680000858249,29.6512311542408));
#74249=CARTESIAN_POINT('Ctrl Pts',(202.775517274459,12.1619662438848,29.6978321865436));
#74250=CARTESIAN_POINT('Ctrl Pts',(202.778696778938,12.1531484963889,29.7439998704635));
#74251=CARTESIAN_POINT('Ctrl Pts',(202.781876283416,12.1416437142876,29.7893867518176));
#74252=CARTESIAN_POINT('Ctrl Pts',(202.782608447654,12.1389944366799,29.7998382707944));
#74253=CARTESIAN_POINT('Ctrl Pts',(202.783340611892,12.1362028793193,29.8102484584892));
#74254=CARTESIAN_POINT('Ctrl Pts',(202.78407277613,12.1332705898496,29.8206132135175));
#74255=CARTESIAN_POINT('Ctrl Pts',(202.787349938577,12.1201456809315,29.8670057907543));
#74256=CARTESIAN_POINT('Ctrl Pts',(202.790627101024,12.1041377229001,29.9126957619106));
#74257=CARTESIAN_POINT('Ctrl Pts',(202.793904263472,12.0853436732396,29.9573009659499));
#74258=CARTESIAN_POINT('Ctrl Pts',(202.797078215803,12.067141518571,30.0005013851046));
#74259=CARTESIAN_POINT('Ctrl Pts',(202.800252168135,12.0463264053124,30.0426837975565));
#74260=CARTESIAN_POINT('Ctrl Pts',(202.803426120466,12.0230371985048,30.0835151694477));
#74261=CARTESIAN_POINT('Ctrl Pts',(202.806596947835,11.9997709214392,30.1243063401919));
#74262=CARTESIAN_POINT('Ctrl Pts',(202.809767775204,11.9740356470927,30.1637486217276));
#74263=CARTESIAN_POINT('Ctrl Pts',(202.812938602572,11.9460170171285,30.2015317995667));
#74264=CARTESIAN_POINT('Ctrl Pts',(202.816107699517,11.91801367784,30.2392943578993));
#74265=CARTESIAN_POINT('Ctrl Pts',(202.819276796462,11.8877297826949,30.2753991597121));
#74266=CARTESIAN_POINT('Ctrl Pts',(202.822445893408,11.8553938146777,30.3095656145806));
#74267=CARTESIAN_POINT('Ctrl Pts',(202.82561465147,11.8230613044563,30.3437284159128));
#74268=CARTESIAN_POINT('Ctrl Pts',(202.828783409533,11.7886775412368,30.3759528791974));
#74269=CARTESIAN_POINT('Ctrl Pts',(202.831952167596,11.752508908463,30.4059941529524));
#74270=CARTESIAN_POINT('Ctrl Pts',(202.835124112032,11.7163039059995,30.4360656349767));
#74271=CARTESIAN_POINT('Ctrl Pts',(202.838296056467,11.6783108832264,30.4639491925107));
#74272=CARTESIAN_POINT('Ctrl Pts',(202.841468000903,11.6388289112696,30.4894405917619));
#74273=CARTESIAN_POINT('Ctrl Pts',(202.844641890173,11.5993227314772,30.5149476207188));
#74274=CARTESIAN_POINT('Ctrl Pts',(202.847815779443,11.5583262709911,30.5380592992723));
#74275=CARTESIAN_POINT('Ctrl Pts',(202.850989668714,11.5161640169009,30.5586169137874));
#74276=CARTESIAN_POINT('Ctrl Pts',(202.854169173192,11.4739271698379,30.5792108985966));
#74277=CARTESIAN_POINT('Ctrl Pts',(202.857348677671,11.430520930021,30.597241596151));
#74278=CARTESIAN_POINT('Ctrl Pts',(202.860528182149,11.3862887509629,30.612598788144));
#74279=CARTESIAN_POINT('Ctrl Pts',(202.861260346387,11.3761031324462,30.6161351840996));
#74280=CARTESIAN_POINT('Ctrl Pts',(202.861992510626,11.3658737695475,30.6195300235928));
#74281=CARTESIAN_POINT('Ctrl Pts',(202.862724674864,11.3556049387415,30.6227823431292));
#74282=CARTESIAN_POINT('Ctrl Pts',(202.866001837311,11.309641717742,30.6373397045696));
#74283=CARTESIAN_POINT('Ctrl Pts',(202.869278999759,11.2626794349558,30.6491028750644));
#74284=CARTESIAN_POINT('Ctrl Pts',(202.872556162206,11.2150905762247,30.6579426179735));
#74285=CARTESIAN_POINT('Ctrl Pts',(202.875730114537,11.1690004688363,30.6665039642808));
#74286=CARTESIAN_POINT('Ctrl Pts',(202.878904066869,11.1223232641915,30.672323193331));
#74287=CARTESIAN_POINT('Ctrl Pts',(202.8820780192,11.075413471924,30.6753330892783));
#74288=CARTESIAN_POINT('Ctrl Pts',(202.885248846569,11.0285498654045,30.6783400217868));
#74289=CARTESIAN_POINT('Ctrl Pts',(202.888419673937,10.98145467782,30.6785430605955));
#74290=CARTESIAN_POINT('Ctrl Pts',(202.891590501306,10.9344890912761,30.6759266062719));
#74291=CARTESIAN_POINT('Ctrl Pts',(202.894759598251,10.887549135377,30.6733115798323));
#74292=CARTESIAN_POINT('Ctrl Pts',(202.897928695196,10.8407391954672,30.667880139443));
#74293=CARTESIAN_POINT('Ctrl Pts',(202.901097792141,10.7944192786983,30.659668758538));
#74294=CARTESIAN_POINT('Ctrl Pts',(202.904266550204,10.7481043150769,30.6514582557041));
#74295=CARTESIAN_POINT('Ctrl Pts',(202.907435308267,10.7022798181404,30.6404685019495));
#74296=CARTESIAN_POINT('Ctrl Pts',(202.91060406633,10.657296795633,30.6267872808195));
#74297=CARTESIAN_POINT('Ctrl Pts',(202.913776010765,10.6122685400483,30.6130923024162));
#74298=CARTESIAN_POINT('Ctrl Pts',(202.916947955201,10.5680839801183,30.5967006208692));
#74299=CARTESIAN_POINT('Ctrl Pts',(202.920119899636,10.5250781824901,30.5777496600571));
#74300=CARTESIAN_POINT('Ctrl Pts',(202.923293788907,10.4820460164404,30.5587870797203));
#74301=CARTESIAN_POINT('Ctrl Pts',(202.926467678177,10.4401945461271,30.5372623522999));
#74302=CARTESIAN_POINT('Ctrl Pts',(202.929641567447,10.3998348030737,30.5133591657939));
#74303=CARTESIAN_POINT('Ctrl Pts',(202.932821071926,10.3594036560292,30.4894136900465));
#74304=CARTESIAN_POINT('Ctrl Pts',(202.936000576404,10.3204699591061,30.4630816762004));
#74305=CARTESIAN_POINT('Ctrl Pts',(202.939180080882,10.2833146764623,30.4345893266701));
#74306=CARTESIAN_POINT('Ctrl Pts',(202.939912245121,10.2747586988218,30.4280282164279));
#74307=CARTESIAN_POINT('Ctrl Pts',(202.94064440936,10.266296877498,30.4213527104206));
#74308=CARTESIAN_POINT('Ctrl Pts',(202.941376573598,10.2579323694205,30.4145658500874));
#74309=CARTESIAN_POINT('Ctrl Pts',(202.944516392661,10.2220619450998,30.3854610231567));
#74310=CARTESIAN_POINT('Ctrl Pts',(202.947656211723,10.1878184127143,30.3541710319064));
#74311=CARTESIAN_POINT('Ctrl Pts',(202.950796030786,10.1554840821467,30.3209067711941));
#74312=CARTESIAN_POINT('Ctrl Pts',(202.952562438989,10.1372933438807,30.3021928702224));
#74313=CARTESIAN_POINT('Ctrl Pts',(202.954328847192,10.1197063743492,30.2828549158538));
#74314=CARTESIAN_POINT('Ctrl Pts',(202.956095255396,10.1027690874833,30.2629362700282));
#74315=CARTESIAN_POINT('Origin',(197.762132885264,11.,29.5));
#74316=CARTESIAN_POINT('',(203.553841401988,10.1027690875417,30.2629362700969));
#74317=CARTESIAN_POINT('',(203.45604596219,10.1027690874833,30.2629362700282));
#74318=CARTESIAN_POINT('',(197.762132885264,10.1027690874833,30.2629362700282));
#74319=CARTESIAN_POINT('',(203.111140857964,9.82225052377447,29.5010225701789));
#74320=CARTESIAN_POINT('Ctrl Pts',(203.553841401988,10.1027690875417,30.2629362700969));
#74321=CARTESIAN_POINT('Ctrl Pts',(203.553636636426,10.1048324583781,30.2653628424999));
#74322=CARTESIAN_POINT('Ctrl Pts',(203.553432306356,10.1069057386442,30.267781121179));
#74323=CARTESIAN_POINT('Ctrl Pts',(203.55059954678,10.13584324624,30.3012580633699));
#74324=CARTESIAN_POINT('Ctrl Pts',(203.548040546119,10.1643058974711,30.3309014308498));
#74325=CARTESIAN_POINT('Ctrl Pts',(203.540101214774,10.257669174366,30.4184760026797));
#74326=CARTESIAN_POINT('Ctrl Pts',(203.534766044947,10.3274611959891,30.4707435858822));
#74327=CARTESIAN_POINT('Ctrl Pts',(203.527971980805,10.4176818116929,30.5238732857151));
#74328=CARTESIAN_POINT('Ctrl Pts',(203.526807829198,10.4331989868856,30.5325442052846));
#74329=CARTESIAN_POINT('Ctrl Pts',(203.524948872563,10.4580209192621,30.5456864325651));
#74330=CARTESIAN_POINT('Ctrl Pts',(203.524262225733,10.4671987967357,30.550392453231));
#74331=CARTESIAN_POINT('Ctrl Pts',(203.522955832613,10.4846693017841,30.5590626964345));
#74332=CARTESIAN_POINT('Ctrl Pts',(203.522336990897,10.4929488755893,30.5630515851031));
#74333=CARTESIAN_POINT('Ctrl Pts',(203.520916426367,10.5119574595265,30.5719368514128));
#74334=CARTESIAN_POINT('Ctrl Pts',(203.520112631508,10.5227148846532,30.5767697228317));
#74335=CARTESIAN_POINT('Ctrl Pts',(203.517544095768,10.5570836449706,30.5915939907905));
#74336=CARTESIAN_POINT('Ctrl Pts',(203.515759663993,10.5809481313927,30.6009757928831));
#74337=CARTESIAN_POINT('Ctrl Pts',(203.511378082039,10.6394852467639,30.6218094422828));
#74338=CARTESIAN_POINT('Ctrl Pts',(203.508758939796,10.6744197841495,30.6324418009247));
#74339=CARTESIAN_POINT('Ctrl Pts',(203.502977007787,10.7516242361449,30.6520711223058));
#74340=CARTESIAN_POINT('Ctrl Pts',(203.499806159218,10.7940114884619,30.6603994551776));
#74341=CARTESIAN_POINT('Ctrl Pts',(203.492960851652,10.8865368697168,30.6733488831739));
#74342=CARTESIAN_POINT('Ctrl Pts',(203.489295674134,10.9367148356339,30.6771225000189));
#74343=CARTESIAN_POINT('Ctrl Pts',(203.484880907378,10.9993434717685,30.6778146708193));
#74344=CARTESIAN_POINT('Ctrl Pts',(203.484017430906,11.01170462077,30.6777567072013));
#74345=CARTESIAN_POINT('Ctrl Pts',(203.482731775176,11.0303103551321,30.6773764855621));
#74346=CARTESIAN_POINT('Ctrl Pts',(203.482302541188,11.0365566237423,30.6771991012756));
#74347=CARTESIAN_POINT('Ctrl Pts',(203.48152285457,11.0479712475656,30.6767840009988));
#74348=CARTESIAN_POINT('Ctrl Pts',(203.481171622502,11.0531396972671,30.6765619405509));
#74349=CARTESIAN_POINT('Ctrl Pts',(203.480359884649,11.0651442126838,30.6759669037407));
#74350=CARTESIAN_POINT('Ctrl Pts',(203.479900752068,11.0719787137758,30.6755683721173));
#74351=CARTESIAN_POINT('Ctrl Pts',(203.478402346832,11.0944138676409,30.6740637435272));
#74352=CARTESIAN_POINT('Ctrl Pts',(203.477375516184,11.1099966881769,30.6727064580783));
#74353=CARTESIAN_POINT('Ctrl Pts',(203.474864332617,11.1484745056807,30.668581198148));
#74354=CARTESIAN_POINT('Ctrl Pts',(203.473394427601,11.171324538913,30.6654504371996));
#74355=CARTESIAN_POINT('Ctrl Pts',(203.465942303451,11.2878575234329,30.6459820541884));
#74356=CARTESIAN_POINT('Ctrl Pts',(203.460206011005,11.3794025856853,30.6190136665376));
#74357=CARTESIAN_POINT('Ctrl Pts',(203.452249434493,11.4941904108065,30.5694702720876));
#74358=CARTESIAN_POINT('Ctrl Pts',(203.450319445721,11.5212054434442,30.5565677853047));
#74359=CARTESIAN_POINT('Ctrl Pts',(203.447599861438,11.5578902891465,30.5372974642034));
#74360=CARTESIAN_POINT('Ctrl Pts',(203.446839455317,11.568002993592,30.5317946443496));
#74361=CARTESIAN_POINT('Ctrl Pts',(203.445505825468,11.5854764090567,30.5219517696008));
#74362=CARTESIAN_POINT('Ctrl Pts',(203.444934948519,11.5928736848672,30.5176781575262));
#74363=CARTESIAN_POINT('Ctrl Pts',(203.443726955957,11.6083489010225,30.5085117055143));
#74364=CARTESIAN_POINT('Ctrl Pts',(203.443089249355,11.6164157580093,30.5036014397842));
#74365=CARTESIAN_POINT('Ctrl Pts',(203.441534193548,11.6358334500228,30.4914595344302));
#74366=CARTESIAN_POINT('Ctrl Pts',(203.440613334216,11.6471208353088,30.4841294545266));
#74367=CARTESIAN_POINT('Ctrl Pts',(203.437103110023,11.6893366263854,30.455674019676));
#74368=CARTESIAN_POINT('Ctrl Pts',(203.434467613505,11.7193740864881,30.4332728556166));
#74369=CARTESIAN_POINT('Ctrl Pts',(203.42688226914,11.8012436767198,30.3659132596763));
#74370=CARTESIAN_POINT('Ctrl Pts',(203.421835920595,11.8502866209029,30.3178070395446));
#74371=CARTESIAN_POINT('Ctrl Pts',(203.413178882355,11.9271919331121,30.2279306311516));
#74372=CARTESIAN_POINT('Ctrl Pts',(203.409566143736,11.9571003411006,30.1881335961857));
#74373=CARTESIAN_POINT('Ctrl Pts',(203.405397137579,11.9897842094336,30.1383715841497));
#74374=CARTESIAN_POINT('Ctrl Pts',(203.404716303748,11.9950608584083,30.1301150405122));
#74375=CARTESIAN_POINT('Ctrl Pts',(203.403647752854,12.0032541186534,30.1169351329356));
#74376=CARTESIAN_POINT('Ctrl Pts',(203.403255992826,12.0062388214089,30.1120549179457));
#74377=CARTESIAN_POINT('Ctrl Pts',(203.402504458088,12.0119295212609,30.1025960412482));
#74378=CARTESIAN_POINT('Ctrl Pts',(203.402144417686,12.0146402345381,30.0980205185362));
#74379=CARTESIAN_POINT('Ctrl Pts',(203.401255858066,12.021288573188,30.0866231765656));
#74380=CARTESIAN_POINT('Ctrl Pts',(203.400729611035,12.025189023181,30.0797797651401));
#74381=CARTESIAN_POINT('Ctrl Pts',(203.398690151874,12.0401442069583,30.0529177301412));
#74382=CARTESIAN_POINT('Ctrl Pts',(203.397205025935,12.0506843521603,30.0326166886945));
#74383=CARTESIAN_POINT('Ctrl Pts',(203.393116409464,12.0784494872939,29.9751024204265));
#74384=CARTESIAN_POINT('Ctrl Pts',(203.39056161515,12.0943331256441,29.9372768651497));
#74385=CARTESIAN_POINT('Ctrl Pts',(203.382618604363,12.1376858578538,29.8167744589788));
#74386=CARTESIAN_POINT('Ctrl Pts',(203.377276129873,12.1579817250588,29.731844394941));
#74387=CARTESIAN_POINT('Ctrl Pts',(203.37047461223,12.1709266666097,29.6278327676274));
#74388=CARTESIAN_POINT('Ctrl Pts',(203.369311362076,12.1727210608599,29.6101623133969));
#74389=CARTESIAN_POINT('Ctrl Pts',(203.367453509063,12.1749246345349,29.5821795748549));
#74390=CARTESIAN_POINT('Ctrl Pts',(203.366767047409,12.1755990500046,29.5718904847246));
#74391=CARTESIAN_POINT('Ctrl Pts',(203.365460800093,12.1766189296353,29.552415910573));
#74392=CARTESIAN_POINT('Ctrl Pts',(203.364841916287,12.1769921268865,29.5432326075625));
#74393=CARTESIAN_POINT('Ctrl Pts',(203.363420960911,12.1775988502407,29.5222531143959));
#74394=CARTESIAN_POINT('Ctrl Pts',(203.362616813096,12.1777626698849,29.5104560605453));
#74395=CARTESIAN_POINT('Ctrl Pts',(203.360045845327,12.1777200091808,29.4729916996093));
#74396=CARTESIAN_POINT('Ctrl Pts',(203.358259281262,12.1768517339911,29.4473341596087));
#74397=CARTESIAN_POINT('Ctrl Pts',(203.353871047536,12.1727162341265,29.3852460691279));
#74398=CARTESIAN_POINT('Ctrl Pts',(203.35124729432,12.1685891161939,29.3489010139919));
#74399=CARTESIAN_POINT('Ctrl Pts',(203.345465724963,12.1559294554885,29.2702625248178));
#74400=CARTESIAN_POINT('Ctrl Pts',(203.34230011101,12.1467501375995,29.2281248277924));
#74401=CARTESIAN_POINT('Ctrl Pts',(203.335462429083,12.1219155940489,29.1381662317735));
#74402=CARTESIAN_POINT('Ctrl Pts',(203.331799656383,12.1054630618378,29.0906461159768));
#74403=CARTESIAN_POINT('Ctrl Pts',(203.327387251835,12.0812429095858,29.0329223127718));
#74404=CARTESIAN_POINT('Ctrl Pts',(203.32652387479,12.0762819787965,29.0216017065007));
#74405=CARTESIAN_POINT('Ctrl Pts',(203.325238336129,12.0685458854959,29.0046780909974));
#74406=CARTESIAN_POINT('Ctrl Pts',(203.324809121602,12.0659029818614,28.9990160275945));
#74407=CARTESIAN_POINT('Ctrl Pts',(203.324029452841,12.0609896902548,28.9887048767647));
#74408=CARTESIAN_POINT('Ctrl Pts',(203.323678219427,12.0587336289821,28.9840494883115));
#74409=CARTESIAN_POINT('Ctrl Pts',(203.322866456162,12.0534206842414,28.9732678155437));
#74410=CARTESIAN_POINT('Ctrl Pts',(203.322407299839,12.0503409623433,28.9671531171396));
#74411=CARTESIAN_POINT('Ctrl Pts',(203.320908728761,12.0400504899214,28.9471576188553));
#74412=CARTESIAN_POINT('Ctrl Pts',(203.319881759805,12.0326162117128,28.9333929622172));
#74413=CARTESIAN_POINT('Ctrl Pts',(203.317370155283,12.0135481399249,28.8997108435776));
#74414=CARTESIAN_POINT('Ctrl Pts',(203.31589997391,12.0015990869346,28.8799787938515));
#74415=CARTESIAN_POINT('Ctrl Pts',(203.308443865967,11.9374227544632,28.7807040093803));
#74416=CARTESIAN_POINT('Ctrl Pts',(203.302704103762,11.8762761801676,28.7073529890055));
#74417=CARTESIAN_POINT('Ctrl Pts',(203.294746800868,11.7852095666352,28.6216871657776));
#74418=CARTESIAN_POINT('Ctrl Pts',(203.292820309845,11.7626809659901,28.6020551142903));
#74419=CARTESIAN_POINT('Ctrl Pts',(203.290104610918,11.730474164568,28.5760762995567));
#74420=CARTESIAN_POINT('Ctrl Pts',(203.28934446815,11.7214113556898,28.5689827337202));
#74421=CARTESIAN_POINT('Ctrl Pts',(203.288011163924,11.70544331556,28.5568575096024));
#74422=CARTESIAN_POINT('Ctrl Pts',(203.287440346225,11.6985844840604,28.551765988347));
#74423=CARTESIAN_POINT('Ctrl Pts',(203.286232341902,11.6840266682557,28.541202950828));
#74424=CARTESIAN_POINT('Ctrl Pts',(203.285594562917,11.6763160657195,28.5357485624812));
#74425=CARTESIAN_POINT('Ctrl Pts',(203.284039054702,11.6574566101502,28.5227451009566));
#74426=CARTESIAN_POINT('Ctrl Pts',(203.283117810409,11.6462425140864,28.5152934858205));
#74427=CARTESIAN_POINT('Ctrl Pts',(203.279603900548,11.6033185058647,28.4878201052407));
#74428=CARTESIAN_POINT('Ctrl Pts',(203.276964975755,11.570789227894,28.4691263427009));
#74429=CARTESIAN_POINT('Ctrl Pts',(203.269363205353,11.4762523855355,28.4206459399401));
#74430=CARTESIAN_POINT('Ctrl Pts',(203.264303288652,11.4124527858537,28.3946933889983));
#74431=CARTESIAN_POINT('Ctrl Pts',(203.255650874701,11.2994601710618,28.3598822669803));
#74432=CARTESIAN_POINT('Ctrl Pts',(203.252055591277,11.2512821311311,28.3483042309437));
#74433=CARTESIAN_POINT('Ctrl Pts',(203.24790306089,11.192864578211,28.338107463902));
#74434=CARTESIAN_POINT('Ctrl Pts',(203.247222407506,11.1831941114399,28.3365435358324));
#74435=CARTESIAN_POINT('Ctrl Pts',(203.246154073071,11.1678474828549,28.3342577467001));
#74436=CARTESIAN_POINT('Ctrl Pts',(203.245762351698,11.1621838764581,28.3334563135946));
#74437=CARTESIAN_POINT('Ctrl Pts',(203.24501083687,11.1512432709921,28.3319893746366));
#74438=CARTESIAN_POINT('Ctrl Pts',(203.244650778316,11.1459672783901,28.3313183055983));
#74439=CARTESIAN_POINT('Ctrl Pts',(203.243762097893,11.1328652368477,28.3297419283086));
#74440=CARTESIAN_POINT('Ctrl Pts',(203.243235749618,11.1250341290514,28.3288793399453));
#74441=CARTESIAN_POINT('Ctrl Pts',(203.2411953387,11.0944277162182,28.3258185881347));
#74442=CARTESIAN_POINT('Ctrl Pts',(203.239709395691,11.0715974789532,28.3242055706098));
#74443=CARTESIAN_POINT('Ctrl Pts',(203.235617558168,11.0077351314567,28.3215608008853));
#74444=CARTESIAN_POINT('Ctrl Pts',(203.233060451799,10.9666736567975,28.3220065475302));
#74445=CARTESIAN_POINT('Ctrl Pts',(203.225119466313,10.8388956570369,28.3300818467023));
#74446=CARTESIAN_POINT('Ctrl Pts',(203.21978100919,10.752958694087,28.3451701345876));
#74447=CARTESIAN_POINT('Ctrl Pts',(203.212983590418,10.6524160561556,28.3745684588741));
#74448=CARTESIAN_POINT('Ctrl Pts',(203.211819843834,10.6354782552229,28.379939914059));
#74449=CARTESIAN_POINT('Ctrl Pts',(203.209961383137,10.6089120299119,28.3890312281864));
#74450=CARTESIAN_POINT('Ctrl Pts',(203.209274819587,10.5991994816548,28.392498150978));
#74451=CARTESIAN_POINT('Ctrl Pts',(203.207968492222,10.5809196819271,28.3992951281812));
#74452=CARTESIAN_POINT('Ctrl Pts',(203.207349631759,10.5723434035504,28.4025988175659));
#74453=CARTESIAN_POINT('Ctrl Pts',(203.205928892179,10.5528505094967,28.4103709250597));
#74454=CARTESIAN_POINT('Ctrl Pts',(203.205124939132,10.5419607497753,28.4149035915338));
#74455=CARTESIAN_POINT('Ctrl Pts',(203.202555313135,10.5076106808615,28.4298103988605));
#74456=CARTESIAN_POINT('Ctrl Pts',(203.200769925438,10.484421693482,28.4407871505742));
#74457=CARTESIAN_POINT('Ctrl Pts',(203.196385362001,10.4291232886598,28.4692094700497));
#74458=CARTESIAN_POINT('Ctrl Pts',(203.193764153209,10.3974327053614,28.4874084791047));
#74459=CARTESIAN_POINT('Ctrl Pts',(203.18798329268,10.3302856508829,28.5302385699635));
#74460=CARTESIAN_POINT('Ctrl Pts',(203.184815721449,10.2952321636467,28.5554066429871));
#74461=CARTESIAN_POINT('Ctrl Pts',(203.177973873752,10.2224817316164,28.6139488910721));
#74462=CARTESIAN_POINT('Ctrl Pts',(203.17430888967,10.185377989793,28.6479359682478));
#74463=CARTESIAN_POINT('Ctrl Pts',(203.169894313044,10.1419954182802,28.6931072160547));
#74464=CARTESIAN_POINT('Ctrl Pts',(203.169030844627,10.1335744349118,28.7021562829259));
#74465=CARTESIAN_POINT('Ctrl Pts',(203.1677451985,10.121112863154,28.7159773557035));
#74466=CARTESIAN_POINT('Ctrl Pts',(203.167315966204,10.1169655329529,28.7206513998919));
#74467=CARTESIAN_POINT('Ctrl Pts',(203.166536281233,10.1094528436882,28.7292551732299));
#74468=CARTESIAN_POINT('Ctrl Pts',(203.166185049144,10.1060760096403,28.7331742526192));
#74469=CARTESIAN_POINT('Ctrl Pts',(203.165373309486,10.0982905533223,28.7423312060794));
#74470=CARTESIAN_POINT('Ctrl Pts',(203.164914175149,10.0939016286838,28.7475854369919));
#74471=CARTESIAN_POINT('Ctrl Pts',(203.164448903624,10.0894724894911,28.752982775601));
#74472=CARTESIAN_POINT('Ctrl Pts',(203.164439855082,10.0893863593136,28.7530877706596));
#74473=CARTESIAN_POINT('Ctrl Pts',(203.163392505071,10.0794178020576,28.7652440037462));
#74474=CARTESIAN_POINT('Ctrl Pts',(203.162369421707,10.0697749725908,28.7774908921946));
#74475=CARTESIAN_POINT('Ctrl Pts',(203.159304242824,10.0412927769419,28.8151806545838));
#74476=CARTESIAN_POINT('Ctrl Pts',(203.157300038872,10.0232324749491,28.8411961071008));
#74477=CARTESIAN_POINT('Ctrl Pts',(203.149760445824,9.95861039114315,28.9427935158048));
#74478=CARTESIAN_POINT('Ctrl Pts',(203.144377351342,9.91959760795539,29.0228185425296));
#74479=CARTESIAN_POINT('Ctrl Pts',(203.136921817303,9.88053724125063,29.1329978671223));
#74480=CARTESIAN_POINT('Ctrl Pts',(203.135103511391,9.87208632508038,29.1598559353139));
#74481=CARTESIAN_POINT('Ctrl Pts',(203.132512680251,9.86160149975831,29.1978878992864));
#74482=CARTESIAN_POINT('Ctrl Pts',(203.131765577045,9.85875411881394,29.2088287598886));
#74483=CARTESIAN_POINT('Ctrl Pts',(203.130391855611,9.85384163159301,29.2288849342393));
#74484=CARTESIAN_POINT('Ctrl Pts',(203.129766856375,9.85172666596165,29.23798716397));
#74485=CARTESIAN_POINT('Ctrl Pts',(203.128488574466,9.84764550124394,29.2565507440171));
#74486=CARTESIAN_POINT('Ctrl Pts',(203.127835103543,9.84568699177589,29.2660130333497));
#74487=CARTESIAN_POINT('Ctrl Pts',(203.126513125027,9.84198180605738,29.2850942464111));
#74488=CARTESIAN_POINT('Ctrl Pts',(203.125844583352,9.84023802567225,29.2947129487094));
#74489=CARTESIAN_POINT('Ctrl Pts',(203.124213212264,9.8362974465002,29.3181046142437));
#74490=CARTESIAN_POINT('Ctrl Pts',(203.123246670765,9.83422521864639,29.3318967718816));
#74491=CARTESIAN_POINT('Ctrl Pts',(203.118646184257,9.82559445279263,29.3972158368744));
#74492=CARTESIAN_POINT('Ctrl Pts',(203.114921238938,9.82220532788681,29.4490958683268));
#74493=CARTESIAN_POINT('Ctrl Pts',(203.111140945057,9.82225044453215,29.5010232767361));
#74494=CARTESIAN_POINT('Ctrl Pts',(203.111140995759,9.82225044392725,29.5010225802788));
#74495=CARTESIAN_POINT('Ctrl Pts',(203.105006122021,9.82232361193448,29.5852933117094));
#74496=CARTESIAN_POINT('Ctrl Pts',(203.098739959637,9.83144089566503,29.6693162629537));
#74497=CARTESIAN_POINT('Ctrl Pts',(203.092040144829,9.85165111638797,29.7617175719854));
#74498=CARTESIAN_POINT('Ctrl Pts',(203.091315249602,9.85398500002695,29.7717551871937));
#74499=CARTESIAN_POINT('Ctrl Pts',(203.089999077818,9.85849885695753,29.7900750212459));
#74500=CARTESIAN_POINT('Ctrl Pts',(203.089405973835,9.86063798134824,29.7983665172388));
#74501=CARTESIAN_POINT('Ctrl Pts',(203.088442892122,9.86428759874874,29.8119008793343));
#74502=CARTESIAN_POINT('Ctrl Pts',(203.088070079566,9.86574439045436,29.8171577408209));
#74503=CARTESIAN_POINT('Ctrl Pts',(203.087324016489,9.86874974884729,29.8277170143305));
#74504=CARTESIAN_POINT('Ctrl Pts',(203.086950823131,9.87029919496497,29.8330190181278));
#74505=CARTESIAN_POINT('Ctrl Pts',(203.085982673637,9.87443783667621,29.8468195535655));
#74506=CARTESIAN_POINT('Ctrl Pts',(203.08539094096,9.87708604300266,29.8553002153843));
#74507=CARTESIAN_POINT('Ctrl Pts',(203.082791863014,9.88923285766064,29.8927063498549));
#74508=CARTESIAN_POINT('Ctrl Pts',(203.080834768041,9.89975574636381,29.921289493624));
#74509=CARTESIAN_POINT('Ctrl Pts',(203.07444233653,9.93828889423108,30.014624729076));
#74510=CARTESIAN_POINT('Ctrl Pts',(203.070141600923,9.97100438833895,30.077267771998));
#74511=CARTESIAN_POINT('Ctrl Pts',(203.063517996035,10.0284167532611,30.1666289928229));
#74512=CARTESIAN_POINT('Ctrl Pts',(203.061273057511,10.0490566481164,30.1957547666944));
#74513=CARTESIAN_POINT('Ctrl Pts',(203.057910865136,10.0813012417469,30.2371358911483));
#74514=CARTESIAN_POINT('Ctrl Pts',(203.056826574791,10.0918981353055,30.250151775798));
#74515=CARTESIAN_POINT('Ctrl Pts',(203.055732095072,10.1027690874946,30.2629362700414));
#74516=CARTESIAN_POINT('',(203.012132885223,9.82225017240322,29.4993627435653));
#74517=CARTESIAN_POINT('Ctrl Pts',(202.956095255396,10.1027690874833,30.2629362700282));
#74518=CARTESIAN_POINT('Ctrl Pts',(202.959228378578,10.0727269907474,30.2276060610354));
#74519=CARTESIAN_POINT('Ctrl Pts',(202.96236150176,10.0447311384701,30.19044701957));
#74520=CARTESIAN_POINT('Ctrl Pts',(202.965494624942,10.0190091789132,30.1517300602576));
#74521=CARTESIAN_POINT('Ctrl Pts',(202.96862550212,9.9933056583499,30.1130408555089));
#74522=CARTESIAN_POINT('Ctrl Pts',(202.971756379298,9.96987312057105,30.0727964182464));
#74523=CARTESIAN_POINT('Ctrl Pts',(202.974887256475,9.94889727092247,30.0312985181852));
#74524=CARTESIAN_POINT('Ctrl Pts',(202.978019397072,9.92791295678256,29.9897838722652));
#74525=CARTESIAN_POINT('Ctrl Pts',(202.981151537668,9.90938758623201,29.9470152558707));
#74526=CARTESIAN_POINT('Ctrl Pts',(202.984283678265,9.89346090484598,29.9033190962448));
#74527=CARTESIAN_POINT('Ctrl Pts',(202.9874161995,9.87753228794224,29.8596176263669));
#74528=CARTESIAN_POINT('Ctrl Pts',(202.990548720735,9.86420316801225,29.8149889334246));
#74529=CARTESIAN_POINT('Ctrl Pts',(202.993681241971,9.85356378597987,29.7697759620188));
#74530=CARTESIAN_POINT('Ctrl Pts',(202.99681923689,9.84290581297378,29.7244839866672));
#74531=CARTESIAN_POINT('Ctrl Pts',(202.99995723181,9.83494707659015,29.6786062571383));
#74532=CARTESIAN_POINT('Ctrl Pts',(203.00309522673,9.82972653664071,29.632495597878));
#74533=CARTESIAN_POINT('Ctrl Pts',(203.006107779561,9.82471468900977,29.5882282231212));
#74534=CARTESIAN_POINT('Ctrl Pts',(203.009120332392,9.82222615716822,29.5437466639892));
#74535=CARTESIAN_POINT('Ctrl Pts',(203.012132885223,9.82225017240322,29.4993627435653));
#74536=CARTESIAN_POINT('Ctrl Pts',(203.012132885264,9.82225017240355,29.4993627429623));
#74537=CARTESIAN_POINT('Ctrl Pts',(203.01476474762,9.82227115289961,29.4605875327235));
#74538=CARTESIAN_POINT('Ctrl Pts',(203.017396609976,9.82420692233509,29.4218659833471));
#74539=CARTESIAN_POINT('Ctrl Pts',(203.020028472332,9.82804235792228,29.3833366052456));
#74540=CARTESIAN_POINT('Ctrl Pts',(203.02330563478,9.83281819486747,29.3353603002785));
#74541=CARTESIAN_POINT('Ctrl Pts',(203.026582797227,9.8405556551505,29.2875695073051));
#74542=CARTESIAN_POINT('Ctrl Pts',(203.029859959674,9.85122638381556,29.2403574740946));
#74543=CARTESIAN_POINT('Ctrl Pts',(203.033033912005,9.86156105128063,29.1946323245856));
#74544=CARTESIAN_POINT('Ctrl Pts',(203.036207864336,9.87464682220411,29.1494506086035));
#74545=CARTESIAN_POINT('Ctrl Pts',(203.039381816667,9.89040545971779,29.1051645676033));
#74546=CARTESIAN_POINT('Ctrl Pts',(203.042552644036,9.90614858182573,29.0609221290969));
#74547=CARTESIAN_POINT('Ctrl Pts',(203.045723471404,9.92455917570205,29.0175741423954));
#74548=CARTESIAN_POINT('Ctrl Pts',(203.048894298772,9.94550894802642,28.9754585966698));
#74549=CARTESIAN_POINT('Ctrl Pts',(203.052063395717,9.96644728738013,28.9333660347643));
#74550=CARTESIAN_POINT('Ctrl Pts',(203.055232492661,9.98992181238473,28.8925050791412));
#74551=CARTESIAN_POINT('Ctrl Pts',(203.058401589606,10.0157568527323,28.8531920767673));
#74552=CARTESIAN_POINT('Ctrl Pts',(203.061570347669,10.0415891304504,28.8138832782676));
#74553=CARTESIAN_POINT('Ctrl Pts',(203.064739105731,10.0697811148109,28.7761225682047));
#74554=CARTESIAN_POINT('Ctrl Pts',(203.067907863793,10.1001135490356,28.7401977639736));
#74555=CARTESIAN_POINT('Ctrl Pts',(203.071079808229,10.130476484309,28.7042368352366));
#74556=CARTESIAN_POINT('Ctrl Pts',(203.074251752664,10.1629838025832,28.6701159205608));
#74557=CARTESIAN_POINT('Ctrl Pts',(203.077423697099,10.197376935849,28.6380885895912));
#74558=CARTESIAN_POINT('Ctrl Pts',(203.080597586369,10.2317911567981,28.606041621498));
#74559=CARTESIAN_POINT('Ctrl Pts',(203.083771475639,10.2680930640106,28.5760911458728));
#74560=CARTESIAN_POINT('Ctrl Pts',(203.086945364909,10.3059910762788,28.5484503815905));
#74561=CARTESIAN_POINT('Ctrl Pts',(203.090124869387,10.3439561372725,28.5207607155872));
#74562=CARTESIAN_POINT('Ctrl Pts',(203.093304373865,10.3835224658961,28.4953892089696));
#74563=CARTESIAN_POINT('Ctrl Pts',(203.096483878343,10.4243712947476,28.4725046685316));
#74564=CARTESIAN_POINT('Ctrl Pts',(203.097216042584,10.4337778082397,28.4672349032912));
#74565=CARTESIAN_POINT('Ctrl Pts',(203.097948206825,10.4432522398561,28.4620968154283));
#74566=CARTESIAN_POINT('Ctrl Pts',(203.098680371066,10.4527905487114,28.4570921042967));
#74567=CARTESIAN_POINT('Ctrl Pts',(203.101957533513,10.495483957977,28.4346910493673));
#74568=CARTESIAN_POINT('Ctrl Pts',(203.105234695961,10.5396514897336,28.414865376036));
#74569=CARTESIAN_POINT('Ctrl Pts',(203.108511858408,10.5849491342878,28.3978077112538));
#74570=CARTESIAN_POINT('Ctrl Pts',(203.111685810739,10.6288201864082,28.3812872562042));
#74571=CARTESIAN_POINT('Ctrl Pts',(203.11485976307,10.6737506530024,28.3673632470349));
#74572=CARTESIAN_POINT('Ctrl Pts',(203.118033715402,10.7194033322925,28.3561640971838));
#74573=CARTESIAN_POINT('Ctrl Pts',(203.12120454277,10.7650110635441,28.3449759736256));
#74574=CARTESIAN_POINT('Ctrl Pts',(203.124375370138,10.8113390615666,28.3365075311969));
#74575=CARTESIAN_POINT('Ctrl Pts',(203.127546197506,10.8580344934006,28.330837540187));
#74576=CARTESIAN_POINT('Ctrl Pts',(203.130715294451,10.9047044420218,28.3251706434753));
#74577=CARTESIAN_POINT('Ctrl Pts',(203.133884391396,10.9517408753356,28.3222992396827));
#74578=CARTESIAN_POINT('Ctrl Pts',(203.137053488341,10.9987829745916,28.3222506288055));
#74579=CARTESIAN_POINT('Ctrl Pts',(203.140222246404,11.0458200434745,28.3222020231264));
#74580=CARTESIAN_POINT('Ctrl Pts',(203.143391004466,11.0928622205722,28.3249756093529));
#74581=CARTESIAN_POINT('Ctrl Pts',(203.146559762528,11.1395485381747,28.330546594347));
#74582=CARTESIAN_POINT('Ctrl Pts',(203.149731706964,11.186281801618,28.3361231812945));
#74583=CARTESIAN_POINT('Ctrl Pts',(203.152903651399,11.2326579380935,28.3445027114324));
#74584=CARTESIAN_POINT('Ctrl Pts',(203.156075595834,11.2783229579594,28.3556087235684));
#74585=CARTESIAN_POINT('Ctrl Pts',(203.159249485104,11.3240159767128,28.3667215452051));
#74586=CARTESIAN_POINT('Ctrl Pts',(203.162423374374,11.368996478961,28.3805640115672));
#74587=CARTESIAN_POINT('Ctrl Pts',(203.165597263644,11.412926014196,28.3970098961005));
#74588=CARTESIAN_POINT('Ctrl Pts',(203.168776768122,11.4569332690573,28.4134848765027));
#74589=CARTESIAN_POINT('Ctrl Pts',(203.1719562726,11.4998853413804,28.4325722333654));
#74590=CARTESIAN_POINT('Ctrl Pts',(203.175135777078,11.5414659166732,28.4540986071425));
#74591=CARTESIAN_POINT('Ctrl Pts',(203.175867941319,11.5510409339599,28.4590556189102));
#74592=CARTESIAN_POINT('Ctrl Pts',(203.17660010556,11.560543342083,28.46414178064));
#74593=CARTESIAN_POINT('Ctrl Pts',(203.177332269801,11.5699694991614,28.4693546524018));
#74594=CARTESIAN_POINT('Ctrl Pts',(203.180609432248,11.6121609178042,28.4926874329833));
#74595=CARTESIAN_POINT('Ctrl Pts',(203.183886594695,11.6530124034109,28.5186678931059));
#74596=CARTESIAN_POINT('Ctrl Pts',(203.187163757143,11.692173863972,28.5471146949742));
#74597=CARTESIAN_POINT('Ctrl Pts',(203.190337709477,11.730101983546,28.5746656005661));
#74598=CARTESIAN_POINT('Ctrl Pts',(203.193511661811,11.766444467378,28.6045294371039));
#74599=CARTESIAN_POINT('Ctrl Pts',(203.196685614146,11.8009085947955,28.636495231465));
#74600=CARTESIAN_POINT('Ctrl Pts',(203.199856441517,11.8353387900332,28.668429553418));
#74601=CARTESIAN_POINT('Ctrl Pts',(203.203027268888,11.8678938829555,28.7024613598172));
#74602=CARTESIAN_POINT('Ctrl Pts',(203.20619809626,11.8983140133927,28.738339317122));
#74603=CARTESIAN_POINT('Ctrl Pts',(203.209367193208,11.9287175425775,28.774197694661));
#74604=CARTESIAN_POINT('Ctrl Pts',(203.212536290156,11.9569880579436,28.8118998031371));
#74605=CARTESIAN_POINT('Ctrl Pts',(203.215705387104,11.9829042910962,28.8511593284598));
#74606=CARTESIAN_POINT('Ctrl Pts',(203.218874145169,12.008817752937,28.8904146556267));
#74607=CARTESIAN_POINT('Ctrl Pts',(203.222042903235,12.0323771277062,28.9312266032784));
#74608=CARTESIAN_POINT('Ctrl Pts',(203.2252116613,12.0534045696077,28.9732800789512));
#74609=CARTESIAN_POINT('Ctrl Pts',(203.228383605738,12.0744531558397,29.0153758418691));
#74610=CARTESIAN_POINT('Ctrl Pts',(203.231555550177,12.0929644817139,29.0587151240289));
#74611=CARTESIAN_POINT('Ctrl Pts',(203.234727494615,12.1088076892772,29.1029602404045));
#74612=CARTESIAN_POINT('Ctrl Pts',(203.237901383888,12.1246606108883,29.1472324850727));
#74613=CARTESIAN_POINT('Ctrl Pts',(203.241075273161,12.1378420028837,29.1924111345289));
#74614=CARTESIAN_POINT('Ctrl Pts',(203.244249162434,12.148271115196,29.2381441073672));
#74615=CARTESIAN_POINT('Ctrl Pts',(203.247428666915,12.1587186785731,29.2839579904519));
#74616=CARTESIAN_POINT('Ctrl Pts',(203.250608171396,12.1664041621707,29.3303276039395));
#74617=CARTESIAN_POINT('Ctrl Pts',(203.253787675877,12.1712983540684,29.3768934272404));
#74618=CARTESIAN_POINT('Ctrl Pts',(203.254519840097,12.1724253699953,29.3876164282187));
#74619=CARTESIAN_POINT('Ctrl Pts',(203.255252004316,12.1734045900643,29.3983498304063));
#74620=CARTESIAN_POINT('Ctrl Pts',(203.255984168535,12.1742360487072,29.4090892502693));
#74621=CARTESIAN_POINT('Ctrl Pts',(203.259261330982,12.1779576523707,29.4571588261297));
#74622=CARTESIAN_POINT('Ctrl Pts',(203.26253849343,12.1787310658024,29.5055657472966));
#74623=CARTESIAN_POINT('Ctrl Pts',(203.265815655877,12.1765151605395,29.5539178961072));
#74624=CARTESIAN_POINT('Ctrl Pts',(203.268989608204,12.1743690424332,29.6007472546453));
#74625=CARTESIAN_POINT('Ctrl Pts',(203.272163560531,12.169419143217,29.6475246354218));
#74626=CARTESIAN_POINT('Ctrl Pts',(203.275337512858,12.1616806410386,29.6938895323014));
#74627=CARTESIAN_POINT('Ctrl Pts',(203.278508340222,12.15394975792,29.7402087799183));
#74628=CARTESIAN_POINT('Ctrl Pts',(203.281679167586,12.1434357976166,29.7861158006402));
#74629=CARTESIAN_POINT('Ctrl Pts',(203.28484999495,12.1302057194786,29.8312553307614));
#74630=CARTESIAN_POINT('Ctrl Pts',(203.28801909189,12.1169828614235,29.8763702267764));
#74631=CARTESIAN_POINT('Ctrl Pts',(203.291188188831,12.1010469783912,29.9207179284697));
#74632=CARTESIAN_POINT('Ctrl Pts',(203.294357285772,12.0825154705478,29.9639561601323));
#74633=CARTESIAN_POINT('Ctrl Pts',(203.29752604383,12.0639859443418,30.0071897681831));
#74634=CARTESIAN_POINT('Ctrl Pts',(203.300694801888,12.0428615657284,30.0493136311309));
#74635=CARTESIAN_POINT('Ctrl Pts',(203.303863559947,12.0193076532744,30.0900059071537));
#74636=CARTESIAN_POINT('Ctrl Pts',(203.307035504378,11.9957300559739,30.130739101657));
#74637=CARTESIAN_POINT('Ctrl Pts',(203.310207448809,11.9697183315038,30.1700373553653));
#74638=CARTESIAN_POINT('Ctrl Pts',(203.31337939324,11.9414825119482,30.2076056403081));
#74639=CARTESIAN_POINT('Ctrl Pts',(203.316553282506,11.9132293799822,30.2451969597358));
#74640=CARTESIAN_POINT('Ctrl Pts',(203.319727171772,11.8827498000311,30.2810557753601));
#74641=CARTESIAN_POINT('Ctrl Pts',(203.322901061038,11.850293389007,30.3149209870356));
#74642=CARTESIAN_POINT('Ctrl Pts',(203.326080565512,11.8177795564741,30.3488461126536));
#74643=CARTESIAN_POINT('Ctrl Pts',(203.329260069987,11.7832823272527,30.3807702239048));
#74644=CARTESIAN_POINT('Ctrl Pts',(203.332439574461,11.7470858796401,30.410471169748));
#74645=CARTESIAN_POINT('Ctrl Pts',(203.33317173873,11.7387506985348,30.417310591264));
#74646=CARTESIAN_POINT('Ctrl Pts',(203.333903903,11.730325535536,30.4240323052374));
#74647=CARTESIAN_POINT('Ctrl Pts',(203.334636067269,11.7218140704041,30.4306339292475));
#74648=CARTESIAN_POINT('Ctrl Pts',(203.337913229716,11.6837168085328,30.4601827548366));
#74649=CARTESIAN_POINT('Ctrl Pts',(203.341190392164,11.6437161593219,30.4874550163208));
#74650=CARTESIAN_POINT('Ctrl Pts',(203.344467554611,11.6021169691323,30.5122006806868));
#74651=CARTESIAN_POINT('Ctrl Pts',(203.347641506941,11.5618278932114,30.536167011421));
#74652=CARTESIAN_POINT('Ctrl Pts',(203.350815459271,11.5200399979202,30.5577632301916));
#74653=CARTESIAN_POINT('Ctrl Pts',(203.353989411602,11.4770627014955,30.5768037153269));
#74654=CARTESIAN_POINT('Ctrl Pts',(203.357160238969,11.434127719021,30.5958254538633));
#74655=CARTESIAN_POINT('Ctrl Pts',(203.360331066337,11.390006160252,30.612296214871));
#74656=CARTESIAN_POINT('Ctrl Pts',(203.363501893704,11.345031547709,30.6260765043218));
#74657=CARTESIAN_POINT('Ctrl Pts',(203.366670990648,11.3000814792725,30.6398492734212));
#74658=CARTESIAN_POINT('Ctrl Pts',(203.369840087592,11.2542798108653,30.6509343168706));
#74659=CARTESIAN_POINT('Ctrl Pts',(203.373009184536,11.2079769634536,30.659241409359));
#74660=CARTESIAN_POINT('Ctrl Pts',(203.376177942597,11.161679067365,30.6675476135414));
#74661=CARTESIAN_POINT('Ctrl Pts',(203.379346700658,11.1148806468559,30.6730763605161));
#74662=CARTESIAN_POINT('Ctrl Pts',(203.38251545872,11.0679414155913,30.6757886827774));
#74663=CARTESIAN_POINT('Ctrl Pts',(203.385687403154,11.020954984167,30.6785037324384));
#74664=CARTESIAN_POINT('Ctrl Pts',(203.388859347588,10.9738280163311,30.6783966765544));
#74665=CARTESIAN_POINT('Ctrl Pts',(203.392031292022,10.9269224274933,30.6754806382483));
#74666=CARTESIAN_POINT('Ctrl Pts',(203.395205181291,10.8799880791304,30.6725628120128));
#74667=CARTESIAN_POINT('Ctrl Pts',(203.39837907056,10.8332759326326,30.666832643974));
#74668=CARTESIAN_POINT('Ctrl Pts',(203.401552959829,10.7871413430124,30.6583549778222));
#74669=CARTESIAN_POINT('Ctrl Pts',(203.404732464306,10.7409251326099,30.6498623130815));
#74670=CARTESIAN_POINT('Ctrl Pts',(203.407911968783,10.6952890563117,30.6386125909654));
#74671=CARTESIAN_POINT('Ctrl Pts',(203.41109147326,10.6505749521543,30.6247209424733));
#74672=CARTESIAN_POINT('Ctrl Pts',(203.411823637508,10.6402783576154,30.6215220262768));
#74673=CARTESIAN_POINT('Ctrl Pts',(203.412555801755,10.6300305693733,30.6181832181594));
#74674=CARTESIAN_POINT('Ctrl Pts',(203.413287966003,10.6198356011203,30.6147062807414));
#74675=CARTESIAN_POINT('Ctrl Pts',(203.416467664206,10.5755601228656,30.5996063742758));
#74676=CARTESIAN_POINT('Ctrl Pts',(203.419647362409,10.532088782024,30.581831442884));
#74677=CARTESIAN_POINT('Ctrl Pts',(203.422827060611,10.4897656725798,30.5614876323453));
#74678=CARTESIAN_POINT('Ctrl Pts',(203.426001128801,10.447517500954,30.5411798428079));
#74679=CARTESIAN_POINT('Ctrl Pts',(203.429175196991,10.4064140282021,30.5183124306163));
#74680=CARTESIAN_POINT('Ctrl Pts',(203.432349265181,10.3667811326855,30.493040245195));
#74681=CARTESIAN_POINT('Ctrl Pts',(203.435520065421,10.32718904231,30.4677940794495));
#74682=CARTESIAN_POINT('Ctrl Pts',(203.438690865662,10.2890649986719,30.4401483408109));
#74683=CARTESIAN_POINT('Ctrl Pts',(203.441861665902,10.2527098003953,30.4103034769102));
#74684=CARTESIAN_POINT('Ctrl Pts',(203.445031001829,10.2163713913887,30.3804723957283));
#74685=CARTESIAN_POINT('Ctrl Pts',(203.448200337755,10.1818006428641,30.3484445493972));
#74686=CARTESIAN_POINT('Ctrl Pts',(203.451369673682,10.1492667758389,30.3144618123697));
#74687=CARTESIAN_POINT('Ctrl Pts',(203.452928436518,10.1332657636376,30.2977482077621));
#74688=CARTESIAN_POINT('Ctrl Pts',(203.454487199354,10.1177569400978,30.2805623355414));
#74689=CARTESIAN_POINT('Ctrl Pts',(203.45604596219,10.1027690874833,30.2629362700282));
#74690=CARTESIAN_POINT('Origin',(197.762132885264,11.,29.5));
#74691=CARTESIAN_POINT('',(204.05505724195,10.1027693394584,30.2629365663567));
#74692=CARTESIAN_POINT('',(203.956022491041,10.1027690874833,30.2629362700282));
#74693=CARTESIAN_POINT('',(197.762132885264,10.1027690874833,30.2629362700282));
#74694=CARTESIAN_POINT('Ctrl Pts',(204.05505724195,10.1027693394584,30.2629365663567));
#74695=CARTESIAN_POINT('Ctrl Pts',(204.052835907548,10.1224928512846,30.2861318624328));
#74696=CARTESIAN_POINT('Ctrl Pts',(204.050599460949,10.1431218690039,30.3085694322674));
#74697=CARTESIAN_POINT('Ctrl Pts',(204.045520212742,10.1919703511427,30.3577233259098));
#74698=CARTESIAN_POINT('Ctrl Pts',(204.042683703823,10.2206723739991,30.383883470213));
#74699=CARTESIAN_POINT('Ctrl Pts',(204.03831536764,10.2676776166748,30.4226527885049));
#74700=CARTESIAN_POINT('Ctrl Pts',(204.036748192096,10.2851345060036,30.4362434041408));
#74701=CARTESIAN_POINT('Ctrl Pts',(204.034667807352,10.3092399669662,30.4539424724109));
#74702=CARTESIAN_POINT('Ctrl Pts',(204.0341298239,10.3155606200916,30.4584875624022));
#74703=CARTESIAN_POINT('Ctrl Pts',(204.033232260932,10.3262604567308,30.4660218383061));
#74704=CARTESIAN_POINT('Ctrl Pts',(204.032870542089,10.3306155304966,30.4690446845855));
#74705=CARTESIAN_POINT('Ctrl Pts',(204.032120436399,10.3397394541981,30.4752867139556));
#74706=CARTESIAN_POINT('Ctrl Pts',(204.031732385785,10.344511703729,30.4785005159385));
#74707=CARTESIAN_POINT('Ctrl Pts',(204.030679028501,10.3576023131747,30.4871774455548));
#74708=CARTESIAN_POINT('Ctrl Pts',(204.030018057272,10.3659668776202,30.4925704573194));
#74709=CARTESIAN_POINT('Ctrl Pts',(204.025683092899,10.421740904041,30.5275376711661));
#74710=CARTESIAN_POINT('Ctrl Pts',(204.022183556766,10.4711411201107,30.5538154917262));
#74711=CARTESIAN_POINT('Ctrl Pts',(204.015955961827,10.5627996408373,30.5944959511124));
#74712=CARTESIAN_POINT('Ctrl Pts',(204.013222538309,10.6043583198254,30.6101951036616));
#74713=CARTESIAN_POINT('Ctrl Pts',(204.007192911502,10.69653095015,30.6391794649589));
#74714=CARTESIAN_POINT('Ctrl Pts',(204.003888197558,10.7473399243291,30.6515143383119));
#74715=CARTESIAN_POINT('Ctrl Pts',(203.999511750217,10.8133781756465,30.6629644837922));
#74716=CARTESIAN_POINT('Ctrl Pts',(203.998537584715,10.8280061894554,30.6652176592421));
#74717=CARTESIAN_POINT('Ctrl Pts',(203.996910657824,10.8522883987296,30.6684906912002));
#74718=CARTESIAN_POINT('Ctrl Pts',(203.996262797415,10.8619199334116,30.6696679436373));
#74719=CARTESIAN_POINT('Ctrl Pts',(203.994985575199,10.880826251221,30.6717420745074));
#74720=CARTESIAN_POINT('Ctrl Pts',(203.994356547724,10.8900993188943,30.672648158375));
#74721=CARTESIAN_POINT('Ctrl Pts',(203.99296443976,10.9105318464105,30.6744001645528));
#74722=CARTESIAN_POINT('Ctrl Pts',(203.992199916843,10.9216944707229,30.6751972286528));
#74723=CARTESIAN_POINT('Ctrl Pts',(203.989514138873,10.960693826931,30.6774238723756));
#74724=CARTESIAN_POINT('Ctrl Pts',(203.987568176793,10.9885666916492,30.6780241974024));
#74725=CARTESIAN_POINT('Ctrl Pts',(203.979790269153,11.0984359735785,30.6764910801662));
#74726=CARTESIAN_POINT('Ctrl Pts',(203.973753597248,11.1800872767338,30.6667845832605));
#74727=CARTESIAN_POINT('Ctrl Pts',(203.965335421973,11.2923175536204,30.6413762400088));
#74728=CARTESIAN_POINT('Ctrl Pts',(203.96292842024,11.3242598418333,30.6327157985599));
#74729=CARTESIAN_POINT('Ctrl Pts',(203.959581246976,11.3688992429543,30.6185693214331));
#74730=CARTESIAN_POINT('Ctrl Pts',(203.958606391311,11.3819286241893,30.6141878380162));
#74731=CARTESIAN_POINT('Ctrl Pts',(203.956891795463,11.4049406915171,30.6059982645015));
#74732=CARTESIAN_POINT('Ctrl Pts',(203.956148186608,11.4149537704856,30.6022805962369));
#74733=CARTESIAN_POINT('Ctrl Pts',(203.955004517532,11.4304250027757,30.5962957077719));
#74734=CARTESIAN_POINT('Ctrl Pts',(203.954599455425,11.4359187268129,30.5941228584001));
#74735=CARTESIAN_POINT('Ctrl Pts',(203.953839642912,11.446254854153,30.5899445554007));
#74736=CARTESIAN_POINT('Ctrl Pts',(203.953484442784,11.4511003623981,30.5879480653001));
#74737=CARTESIAN_POINT('Ctrl Pts',(203.952630905518,11.4627730538088,30.5830471840331));
#74738=CARTESIAN_POINT('Ctrl Pts',(203.952134444027,11.4695863957594,30.580110515698));
#74739=CARTESIAN_POINT('Ctrl Pts',(203.950440373318,11.4928973983994,30.569800791019));
#74740=CARTESIAN_POINT('Ctrl Pts',(203.949259529218,11.5092537130237,30.5621121956177));
#74741=CARTESIAN_POINT('Ctrl Pts',(203.943522976248,11.5888194709494,30.5224498878186));
#74742=CARTESIAN_POINT('Ctrl Pts',(203.93918448111,11.6492374879105,30.4851927492431));
#74743=CARTESIAN_POINT('Ctrl Pts',(203.933802172331,11.7187221801916,30.4331603741348));
#74744=CARTESIAN_POINT('Ctrl Pts',(203.932810685901,11.7313031602659,30.4233339223295));
#74745=CARTESIAN_POINT('Ctrl Pts',(203.929616232122,11.7710091199807,30.3910006246545));
#74746=CARTESIAN_POINT('Ctrl Pts',(203.927397715491,11.7973235121348,30.3675322093738));
#74747=CARTESIAN_POINT('Ctrl Pts',(203.923534135699,11.840455371847,30.325442959711));
#74748=CARTESIAN_POINT('Ctrl Pts',(203.921910457725,11.8578031578968,30.307400095851));
#74749=CARTESIAN_POINT('Ctrl Pts',(203.919493210379,11.8823909608635,30.2801396548811));
#74750=CARTESIAN_POINT('Ctrl Pts',(203.918718514852,11.8900898117696,30.2713441513764));
#74751=CARTESIAN_POINT('Ctrl Pts',(203.917325874911,11.9035988716057,30.2554392153952));
#74752=CARTESIAN_POINT('Ctrl Pts',(203.916710022165,11.9094593350438,30.2483735957153));
#74753=CARTESIAN_POINT('Ctrl Pts',(203.915390968403,11.9217667525383,30.2331771790416));
#74754=CARTESIAN_POINT('Ctrl Pts',(203.914686904711,11.9281900105031,30.2250282853295));
#74755=CARTESIAN_POINT('Ctrl Pts',(203.91277652855,11.9452215795612,30.2028238034947));
#74756=CARTESIAN_POINT('Ctrl Pts',(203.911562487059,11.9556233451436,30.1886138962142));
#74757=CARTESIAN_POINT('Ctrl Pts',(203.904310815562,12.0152532824935,30.1031989686845));
#74758=CARTESIAN_POINT('Ctrl Pts',(203.89799623503,12.056820281184,30.0269859066105));
#74759=CARTESIAN_POINT('Ctrl Pts',(203.888624797964,12.1053225714124,29.9087311631785));
#74760=CARTESIAN_POINT('Ctrl Pts',(203.885602710583,12.1189693922557,29.8697390872537));
#74761=CARTESIAN_POINT('Ctrl Pts',(203.880991448339,12.1369773225309,29.8080664523042));
#74762=CARTESIAN_POINT('Ctrl Pts',(203.879362734056,12.1427680908482,29.7858384538874));
#74763=CARTESIAN_POINT('Ctrl Pts',(203.877215491364,12.1496700214736,29.7557657575486));
#74764=CARTESIAN_POINT('Ctrl Pts',(203.876670199822,12.1513572600192,29.7480599710953));
#74765=CARTESIAN_POINT('Ctrl Pts',(203.87576403892,12.1540526460263,29.7351294446682));
#74766=CARTESIAN_POINT('Ctrl Pts',(203.875400939565,12.1551030205704,29.729913857477));
#74767=CARTESIAN_POINT('Ctrl Pts',(203.874651891722,12.1572086176434,29.7190797888695));
#74768=CARTESIAN_POINT('Ctrl Pts',(203.87426623755,12.1582583356723,29.713460464498));
#74769=CARTESIAN_POINT('Ctrl Pts',(203.873226638282,12.1609928143643,29.6982079179623));
#74770=CARTESIAN_POINT('Ctrl Pts',(203.87257684056,12.1625986191563,29.6885607586204));
#74771=CARTESIAN_POINT('Ctrl Pts',(203.868742400214,12.1714383554727,29.6310396713103));
#74772=CARTESIAN_POINT('Ctrl Pts',(203.865688100292,12.1758355501235,29.5827711883056));
#74773=CARTESIAN_POINT('Ctrl Pts',(203.860150221329,12.1784281613573,29.493953129332));
#74774=CARTESIAN_POINT('Ctrl Pts',(203.857659456515,12.1775262443206,29.453507930113));
#74775=CARTESIAN_POINT('Ctrl Pts',(203.852547969694,12.1714579467391,29.3714044367933));
#74776=CARTESIAN_POINT('Ctrl Pts',(203.849929299999,12.1661423026335,29.3298168255078));
#74777=CARTESIAN_POINT('Ctrl Pts',(203.845459489568,12.1535738992326,29.2609320240257));
#74778=CARTESIAN_POINT('Ctrl Pts',(203.843640725555,12.1475358541894,29.2334526133792));
#74779=CARTESIAN_POINT('Ctrl Pts',(203.840989934214,12.1374778843301,29.1944056697384));
#74780=CARTESIAN_POINT('Ctrl Pts',(203.840182620614,12.1342521823018,29.1826424716073));
#74781=CARTESIAN_POINT('Ctrl Pts',(203.83875356189,12.1282629986583,29.1620606103496));
#74782=CARTESIAN_POINT('Ctrl Pts',(203.838134337998,12.1255772942379,29.1532202835904));
#74783=CARTESIAN_POINT('Ctrl Pts',(203.836830782244,12.1197369194628,29.1347789561071));
#74784=CARTESIAN_POINT('Ctrl Pts',(203.836145845869,12.1165621390541,29.1251851678169));
#74785=CARTESIAN_POINT('Ctrl Pts',(203.83431411122,12.1077942299657,29.0997901210721));
#74786=CARTESIAN_POINT('Ctrl Pts',(203.833160476738,12.1019867382816,29.0840658920285));
#74787=CARTESIAN_POINT('Ctrl Pts',(203.825417290153,12.0611464596619,28.9803539356571));
#74788=CARTESIAN_POINT('Ctrl Pts',(203.818485152985,12.0159507545616,28.896757569094));
#74789=CARTESIAN_POINT('Ctrl Pts',(203.807576859357,11.9299213255743,28.7752370866083));
#74790=CARTESIAN_POINT('Ctrl Pts',(203.803625604819,11.8955703283721,28.7331949691175));
#74791=CARTESIAN_POINT('Ctrl Pts',(203.799139462438,11.85171295339,28.6865034232678));
#74792=CARTESIAN_POINT('Ctrl Pts',(203.798456546617,11.8448952405991,28.6794247850486));
#74793=CARTESIAN_POINT('Ctrl Pts',(203.797385499418,11.8339655522644,28.6683574601672));
#74794=CARTESIAN_POINT('Ctrl Pts',(203.796993294494,11.8299118805489,28.6643121812518));
#74795=CARTESIAN_POINT('Ctrl Pts',(203.79624572188,11.8220833295916,28.6566129842009));
#74796=CARTESIAN_POINT('Ctrl Pts',(203.795890034974,11.8183132806606,28.6529545259866));
#74797=CARTESIAN_POINT('Ctrl Pts',(203.795010306112,11.8088791553193,28.6439214173039));
#74798=CARTESIAN_POINT('Ctrl Pts',(203.794488512221,11.8031857431121,28.6385775149027));
#74799=CARTESIAN_POINT('Ctrl Pts',(203.792595947004,11.7821961472855,28.6192654729975));
#74800=CARTESIAN_POINT('Ctrl Pts',(203.791247643051,11.7665844536462,28.605644078208));
#74801=CARTESIAN_POINT('Ctrl Pts',(203.784959508864,11.6911229421945,28.5432316742109));
#74802=CARTESIAN_POINT('Ctrl Pts',(203.780258051014,11.6269257956876,28.499988674596));
#74803=CARTESIAN_POINT('Ctrl Pts',(203.771837629189,11.5077780226486,28.4357459103207));
#74804=CARTESIAN_POINT('Ctrl Pts',(203.76817662595,11.4546361471705,28.4119834172088));
#74805=CARTESIAN_POINT('Ctrl Pts',(203.763395159632,11.3857055034298,28.3870956720097));
#74806=CARTESIAN_POINT('Ctrl Pts',(203.762398171474,11.3713523744983,28.3822244595857));
#74807=CARTESIAN_POINT('Ctrl Pts',(203.760743522307,11.3475943235182,28.3746694702944));
#74808=CARTESIAN_POINT('Ctrl Pts',(203.760091120343,11.3382426180778,28.3718233575652));
#74809=CARTESIAN_POINT('Ctrl Pts',(203.758812489884,11.319952583571,28.3665047877925));
#74810=CARTESIAN_POINT('Ctrl Pts',(203.758186682504,11.3110183235955,28.3640208426989));
#74811=CARTESIAN_POINT('Ctrl Pts',(203.756674219465,11.2894742010538,28.3583042465817));
#74812=CARTESIAN_POINT('Ctrl Pts',(203.755784378132,11.2768384965162,28.3551747164221));
#74813=CARTESIAN_POINT('Ctrl Pts',(203.752717227279,11.233436851311,28.3451858083869));
#74814=CARTESIAN_POINT('Ctrl Pts',(203.750508796845,11.2024510190121,28.3393528307842));
#74815=CARTESIAN_POINT('Ctrl Pts',(203.741640262798,11.0790772476091,28.3212187858246));
#74816=CARTESIAN_POINT('Ctrl Pts',(203.734722214072,10.9856059829233,28.3186586185084));
#74817=CARTESIAN_POINT('Ctrl Pts',(203.726298741185,10.8700141789542,28.3292209538258));
#74818=CARTESIAN_POINT('Ctrl Pts',(203.724649453458,10.8472644778638,28.3319709472456));
#74819=CARTESIAN_POINT('Ctrl Pts',(203.721919083114,10.8092137993591,28.3377013924152));
#74820=CARTESIAN_POINT('Ctrl Pts',(203.720825586205,10.7938658891871,28.3403249541164));
#74821=CARTESIAN_POINT('Ctrl Pts',(203.719273222351,10.7718617555778,28.3445370173452));
#74822=CARTESIAN_POINT('Ctrl Pts',(203.718802557287,10.7651609576225,28.3458802520192));
#74823=CARTESIAN_POINT('Ctrl Pts',(203.717981222747,10.7534096418494,28.3483424941947));
#74824=CARTESIAN_POINT('Ctrl Pts',(203.717629245643,10.7483542769184,28.3494365515412));
#74825=CARTESIAN_POINT('Ctrl Pts',(203.716855605197,10.7371988963229,28.3519277902144));
#74826=CARTESIAN_POINT('Ctrl Pts',(203.716434785891,10.7311026133432,28.3533403212785));
#74827=CARTESIAN_POINT('Ctrl Pts',(203.715212571445,10.7133246152663,28.3576091308158));
#74828=CARTESIAN_POINT('Ctrl Pts',(203.714417957363,10.7016746624216,28.3605959039402));
#74829=CARTESIAN_POINT('Ctrl Pts',(203.709399505872,10.6276820027327,28.3807786243057));
#74830=CARTESIAN_POINT('Ctrl Pts',(203.705395097199,10.5667917834196,28.4029084588218));
#74831=CARTESIAN_POINT('Ctrl Pts',(203.697985457178,10.4580805483938,28.4528898842018));
#74832=CARTESIAN_POINT('Ctrl Pts',(203.694589657529,10.4098106535687,28.4793176947714));
#74833=CARTESIAN_POINT('Ctrl Pts',(203.688992701592,10.3355682931643,28.5269981148427));
#74834=CARTESIAN_POINT('Ctrl Pts',(203.686852409059,10.3083483483887,28.5461552264396));
#74835=CARTESIAN_POINT('Ctrl Pts',(203.683821088964,10.2717210603782,28.5743260452145));
#74836=CARTESIAN_POINT('Ctrl Pts',(203.682966166023,10.2615956642631,28.5823827050844));
#74837=CARTESIAN_POINT('Ctrl Pts',(203.681482048412,10.2443837828455,28.5965473635551));
#74838=CARTESIAN_POINT('Ctrl Pts',(203.680856017061,10.2372334207898,28.6025760917583));
#74839=CARTESIAN_POINT('Ctrl Pts',(203.6795654824,10.2227228708218,28.6151091642517));
#74840=CARTESIAN_POINT('Ctrl Pts',(203.678900676885,10.2153707526306,28.621621686916));
#74841=CARTESIAN_POINT('Ctrl Pts',(203.677184731048,10.1967133510109,28.6385696140709));
#74842=CARTESIAN_POINT('Ctrl Pts',(203.676128229257,10.1855298413182,28.6491356909623));
#74843=CARTESIAN_POINT('Ctrl Pts',(203.671064714263,10.1333862115855,28.7003706481116));
#74844=CARTESIAN_POINT('Ctrl Pts',(203.666940687652,10.0952508996848,28.7437897819964));
#74845=CARTESIAN_POINT('Ctrl Pts',(203.658781687065,10.0276121823865,28.8332739161955));
#74846=CARTESIAN_POINT('Ctrl Pts',(203.654765239416,9.99782340616605,28.8789495952375));
#74847=CARTESIAN_POINT('Ctrl Pts',(203.648805453967,9.9580081664312,28.950369631282));
#74848=CARTESIAN_POINT('Ctrl Pts',(203.646829669774,9.94554602352513,28.97467390172));
#74849=CARTESIAN_POINT('Ctrl Pts',(203.643632441726,9.92646163779091,29.0153146031872));
#74850=CARTESIAN_POINT('Ctrl Pts',(203.642393110891,9.91934120111442,29.0314050920125));
#74851=CARTESIAN_POINT('Ctrl Pts',(203.640675382206,9.90983359434278,29.0542606892761));
#74852=CARTESIAN_POINT('Ctrl Pts',(203.640181642921,9.90714391360983,29.0608964745907));
#74853=CARTESIAN_POINT('Ctrl Pts',(203.639334940366,9.90260374745161,29.0723978282189));
#74854=CARTESIAN_POINT('Ctrl Pts',(203.638980383895,9.90072473963864,29.0772517788513));
#74855=CARTESIAN_POINT('Ctrl Pts',(203.638218330027,9.89673375227158,29.0877680675223));
#74856=CARTESIAN_POINT('Ctrl Pts',(203.637811471064,9.89463309380784,29.0934344011043));
#74857=CARTESIAN_POINT('Ctrl Pts',(203.636669573462,9.88882640578398,29.1094751463394));
#74858=CARTESIAN_POINT('Ctrl Pts',(203.635940039191,9.88522207797972,29.119886038787));
#74859=CARTESIAN_POINT('Ctrl Pts',(203.630110313355,9.85733701312374,29.2042409030244));
#74860=CARTESIAN_POINT('Ctrl Pts',(203.625340366416,9.84029112482895,29.2803849877759));
#74861=CARTESIAN_POINT('Ctrl Pts',(203.617583335211,9.82515975734209,29.4046696685909));
#74862=CARTESIAN_POINT('Ctrl Pts',(203.61463894431,9.82227727926294,29.4519766908943));
#74863=CARTESIAN_POINT('Ctrl Pts',(203.609726484388,9.82223312669742,29.5291590023504));
#74864=CARTESIAN_POINT('Ctrl Pts',(203.607802566791,9.82334956396589,29.5589795058165));
#74865=CARTESIAN_POINT('Ctrl Pts',(203.605089726457,9.82646342739179,29.6001965699306));
#74866=CARTESIAN_POINT('Ctrl Pts',(203.604329777116,9.82749822288538,29.611655754157));
#74867=CARTESIAN_POINT('Ctrl Pts',(203.602996712311,9.82959343789739,29.6315921579023));
#74868=CARTESIAN_POINT('Ctrl Pts',(203.602425938396,9.83057853046149,29.6400765390137));
#74869=CARTESIAN_POINT('Ctrl Pts',(203.601217926214,9.83284714279946,29.6579192389235));
#74870=CARTESIAN_POINT('Ctrl Pts',(203.60058009458,9.83415113342793,29.6672742942761));
#74871=CARTESIAN_POINT('Ctrl Pts',(203.599024255667,9.83758704461222,29.689927778203));
#74872=CARTESIAN_POINT('Ctrl Pts',(203.598102729704,9.83983478581976,29.7032070119741));
#74873=CARTESIAN_POINT('Ctrl Pts',(203.594586116635,9.84920781646309,29.7533403066453));
#74874=CARTESIAN_POINT('Ctrl Pts',(203.591944676557,9.85786512263747,29.7898816350214));
#74875=CARTESIAN_POINT('Ctrl Pts',(203.58433082435,9.88731369403648,29.8921334534756));
#74876=CARTESIAN_POINT('Ctrl Pts',(203.579260920003,9.91214480609692,29.9565183643017));
#74877=CARTESIAN_POINT('Ctrl Pts',(203.570611870851,9.96416475895057,30.0626485218357));
#74878=CARTESIAN_POINT('Ctrl Pts',(203.567029387455,9.9886372126498,30.1055363949191));
#74879=CARTESIAN_POINT('Ctrl Pts',(203.562888958763,10.021107804077,30.1549511729283));
#74880=CARTESIAN_POINT('Ctrl Pts',(203.562208453497,10.0265879033658,30.1630685302341));
#74881=CARTESIAN_POINT('Ctrl Pts',(203.561140296925,10.0354278933322,30.1758168572441));
#74882=CARTESIAN_POINT('Ctrl Pts',(203.560748607466,10.0387212291433,30.1804931312233));
#74883=CARTESIAN_POINT('Ctrl Pts',(203.559997109199,10.0451426591428,30.1894713983153));
#74884=CARTESIAN_POINT('Ctrl Pts',(203.559637035781,10.0482660175161,30.1937764613178));
#74885=CARTESIAN_POINT('Ctrl Pts',(203.558748256438,10.0560885847851,30.2044064067175));
#74886=CARTESIAN_POINT('Ctrl Pts',(203.55822182526,10.0608224117722,30.2107057138403));
#74887=CARTESIAN_POINT('Ctrl Pts',(203.556391910927,10.0776154301364,30.2325913604401));
#74888=CARTESIAN_POINT('Ctrl Pts',(203.555108328926,10.0900025848589,30.2479225641033));
#74889=CARTESIAN_POINT('Ctrl Pts',(203.553841401988,10.1027690875417,30.2629362700969));
#74890=CARTESIAN_POINT('',(203.512132885208,9.82225044284812,29.5010213366495));
#74891=CARTESIAN_POINT('Ctrl Pts',(203.45604596219,10.1027690874833,30.2629362700282));
#74892=CARTESIAN_POINT('Ctrl Pts',(203.45921737708,10.0722752253946,30.2270747744055));
#74893=CARTESIAN_POINT('Ctrl Pts',(203.46238879197,10.0439406535874,30.1893892494117));
#74894=CARTESIAN_POINT('Ctrl Pts',(203.46556020686,10.0179771118165,30.1501739071846));
#74895=CARTESIAN_POINT('Ctrl Pts',(203.468732893903,9.99200315525983,30.1109428344617));
#74896=CARTESIAN_POINT('Ctrl Pts',(203.471905580946,9.96840240753564,30.0701812021462));
#74897=CARTESIAN_POINT('Ctrl Pts',(203.47507826799,9.94734179825937,30.0282099703794));
#74898=CARTESIAN_POINT('Ctrl Pts',(203.478257091189,9.92624045657508,29.9861575638795));
#74899=CARTESIAN_POINT('Ctrl Pts',(203.481435914388,9.90768928947866,29.9428913969871));
#74900=CARTESIAN_POINT('Ctrl Pts',(203.484614737587,9.89180735454263,29.8987532107133));
#74901=CARTESIAN_POINT('Ctrl Pts',(203.487056446638,9.87960816577514,29.8648499068415));
#74902=CARTESIAN_POINT('Ctrl Pts',(203.489498155688,9.86898284931918,29.8304325616935));
#74903=CARTESIAN_POINT('Ctrl Pts',(203.491939864738,9.85996497249551,29.7956606138173));
#74904=CARTESIAN_POINT('Ctrl Pts',(203.495988552475,9.84501209868252,29.7380039659176));
#74905=CARTESIAN_POINT('Ctrl Pts',(203.500037240213,9.83442672707395,29.6791717338297));
#74906=CARTESIAN_POINT('Ctrl Pts',(203.50408592795,9.82835314494067,29.619744350721));
#74907=CARTESIAN_POINT('Ctrl Pts',(203.506768247036,9.82432930157885,29.5803727779349));
#74908=CARTESIAN_POINT('Ctrl Pts',(203.509450566122,9.82228488691305,29.5407403482437));
#74909=CARTESIAN_POINT('Ctrl Pts',(203.512132885208,9.82225044284812,29.5010213366495));
#74910=CARTESIAN_POINT('Ctrl Pts',(203.512132885264,9.8222504428474,29.5010213358201));
#74911=CARTESIAN_POINT('Ctrl Pts',(203.515270544845,9.82221015171904,29.4545597727904));
#74912=CARTESIAN_POINT('Ctrl Pts',(203.518408204426,9.82492346972817,29.40803242817));
#74913=CARTESIAN_POINT('Ctrl Pts',(203.521545864007,9.83038714755937,29.361794218986));
#74914=CARTESIAN_POINT('Ctrl Pts',(203.524681486004,9.83584727729981,29.315586036712));
#74915=CARTESIAN_POINT('Ctrl Pts',(203.527817108002,9.84405416548516,29.2696671832549));
#74916=CARTESIAN_POINT('Ctrl Pts',(203.530952729999,9.85495262916811,29.2243887138541));
#74917=CARTESIAN_POINT('Ctrl Pts',(203.534087766409,9.86584905752816,29.1791187003521));
#74918=CARTESIAN_POINT('Ctrl Pts',(203.537222802819,9.87943592937715,29.1344893872576));
#74919=CARTESIAN_POINT('Ctrl Pts',(203.540357839229,9.8956073301553,29.090840015039));
#74920=CARTESIAN_POINT('Ctrl Pts',(203.543495829822,9.91179396944655,29.0471495114713));
#74921=CARTESIAN_POINT('Ctrl Pts',(203.546633820416,9.93056979619447,29.0044413257409));
#74922=CARTESIAN_POINT('Ctrl Pts',(203.54977181101,9.95178028604199,28.9630358542977));
#74923=CARTESIAN_POINT('Ctrl Pts',(203.552911636061,9.97300317545919,28.9216061773774));
#74924=CARTESIAN_POINT('Ctrl Pts',(203.556051461112,9.99666326771046,28.8814812196115));
#74925=CARTESIAN_POINT('Ctrl Pts',(203.559191286163,10.0225613570507,28.8429545207755));
#74926=CARTESIAN_POINT('Ctrl Pts',(203.562336629387,10.0485049617121,28.8043601121154));
#74927=CARTESIAN_POINT('Ctrl Pts',(203.565481972611,10.0766940559281,28.7673700115092));
#74928=CARTESIAN_POINT('Ctrl Pts',(203.568627315836,10.1068889991453,28.732244959214));
#74929=CARTESIAN_POINT('Ctrl Pts',(203.569282131714,10.1131751583546,28.7249324211717));
#74930=CARTESIAN_POINT('Ctrl Pts',(203.569936947593,10.1195481297463,28.7177005859782));
#74931=CARTESIAN_POINT('Ctrl Pts',(203.570591763472,10.1260055620902,28.7105515944643));
#74932=CARTESIAN_POINT('Ctrl Pts',(203.573868925919,10.1583231271821,28.6747729774718));
#74933=CARTESIAN_POINT('Ctrl Pts',(203.577146088366,10.1929142128349,28.6409013821579));
#74934=CARTESIAN_POINT('Ctrl Pts',(203.580423250814,10.2295226065395,28.6092364799419));
#74935=CARTESIAN_POINT('Ctrl Pts',(203.583597203154,10.2649780649534,28.5785688239731));
#74936=CARTESIAN_POINT('Ctrl Pts',(203.586771155494,10.3023251845411,28.5499713149255));
#74937=CARTESIAN_POINT('Ctrl Pts',(203.589945107834,10.341291943156,28.5236810160871));
#74938=CARTESIAN_POINT('Ctrl Pts',(203.59311593521,10.3802203364505,28.4974166017659));
#74939=CARTESIAN_POINT('Ctrl Pts',(203.596286762587,10.4207647527763,28.4734552113849));
#74940=CARTESIAN_POINT('Ctrl Pts',(203.599457589964,10.4626213414356,28.4519927291189));
#74941=CARTESIAN_POINT('Ctrl Pts',(203.602626686916,10.5044550875888,28.4305419596299));
#74942=CARTESIAN_POINT('Ctrl Pts',(203.605795783869,10.547599092752,28.4115876502471));
#74943=CARTESIAN_POINT('Ctrl Pts',(203.608964880821,10.5917242201031,28.3952801486125));
#74944=CARTESIAN_POINT('Ctrl Pts',(203.612133638891,10.635844628995,28.3789743907979));
#74945=CARTESIAN_POINT('Ctrl Pts',(203.615302396961,10.6809454289694,28.3653150695729));
#74946=CARTESIAN_POINT('Ctrl Pts',(203.61847115503,10.7266793354574,28.3544037025051));
#74947=CARTESIAN_POINT('Ctrl Pts',(203.621643099472,10.7724592300683,28.3434813634184));
#74948=CARTESIAN_POINT('Ctrl Pts',(203.624815043913,10.8188729585003,28.3353126192441));
#74949=CARTESIAN_POINT('Ctrl Pts',(203.627986988355,10.865561923027,28.3299480926216));
#74950=CARTESIAN_POINT('Ctrl Pts',(203.631160877631,10.9122795142515,28.3245802768132));
#74951=CARTESIAN_POINT('Ctrl Pts',(203.634334766906,10.9592721212958,28.3220201302267));
#74952=CARTESIAN_POINT('Ctrl Pts',(203.637508656182,11.0061785242847,28.322266206506));
#74953=CARTESIAN_POINT('Ctrl Pts',(203.640688160665,11.0531679135282,28.3225127181407));
#74954=CARTESIAN_POINT('Ctrl Pts',(203.643867665148,11.1000702398532,28.3255753159026));
#74955=CARTESIAN_POINT('Ctrl Pts',(203.647047169632,11.1465287613955,28.3314006740615));
#74956=CARTESIAN_POINT('Ctrl Pts',(203.647779333823,11.1572270529188,28.3327421153675));
#74957=CARTESIAN_POINT('Ctrl Pts',(203.648511498015,11.1679018572594,28.3342298445736));
#74958=CARTESIAN_POINT('Ctrl Pts',(203.649243662206,11.178548913606,28.3358628311277));
#74959=CARTESIAN_POINT('Ctrl Pts',(203.652520824653,11.2262050727579,28.3431720689655));
#74960=CARTESIAN_POINT('Ctrl Pts',(203.6557979871,11.2735191772522,28.3534289543614));
#74961=CARTESIAN_POINT('Ctrl Pts',(203.659075149548,11.3201000321551,28.3665843516546));
#74962=CARTESIAN_POINT('Ctrl Pts',(203.66224910206,11.3652138840976,28.3793254369559));
#74963=CARTESIAN_POINT('Ctrl Pts',(203.665423054572,11.4096394077614,28.3947849953841));
#74964=CARTESIAN_POINT('Ctrl Pts',(203.668597007084,11.4530289979444,28.412866250399));
#74965=CARTESIAN_POINT('Ctrl Pts',(203.671767834634,11.4963758682539,28.4309297032424));
#74966=CARTESIAN_POINT('Ctrl Pts',(203.674938662183,11.5386883121724,28.4516095301784));
#74967=CARTESIAN_POINT('Ctrl Pts',(203.678109489733,11.5796356070272,28.4747597230082));
#74968=CARTESIAN_POINT('Ctrl Pts',(203.681278586858,11.620560555614,28.4978972820263));
#74969=CARTESIAN_POINT('Ctrl Pts',(203.684447683984,11.6601213471134,28.5235022625312));
#74970=CARTESIAN_POINT('Ctrl Pts',(203.68761678111,11.6980113790721,28.5513824916301));
#74971=CARTESIAN_POINT('Ctrl Pts',(203.690785539353,11.7358973593143,28.5792597393965));
#74972=CARTESIAN_POINT('Ctrl Pts',(203.693954297597,11.7721124878349,28.6094114210323));
#74973=CARTESIAN_POINT('Ctrl Pts',(203.69712305584,11.8063809594186,28.6416033488025));
#74974=CARTESIAN_POINT('Ctrl Pts',(203.700295000453,11.840683889944,28.6738276474287));
#74975=CARTESIAN_POINT('Ctrl Pts',(203.703466945067,11.873035852828,28.7080959022972));
#74976=CARTESIAN_POINT('Ctrl Pts',(203.706638889681,11.9031973238985,28.7441364828208));
#74977=CARTESIAN_POINT('Ctrl Pts',(203.709812779129,11.9333772880552,28.7801991611247));
#74978=CARTESIAN_POINT('Ctrl Pts',(203.712986668576,11.9613637566435,28.8180358797258));
#74979=CARTESIAN_POINT('Ctrl Pts',(203.716160558024,11.9869592475456,28.857344177507));
#74980=CARTESIAN_POINT('Ctrl Pts',(203.719340062676,12.0126000216661,28.8967220190307));
#74981=CARTESIAN_POINT('Ctrl Pts',(203.722519567329,12.0358411085791,28.9375761477844));
#74982=CARTESIAN_POINT('Ctrl Pts',(203.725699071981,12.0565308153257,28.9795793059772));
#74983=CARTESIAN_POINT('Ctrl Pts',(203.726431234967,12.0612951541561,28.9892516169495));
#74984=CARTESIAN_POINT('Ctrl Pts',(203.727163397954,12.0659244048403,28.9989847789349));
#74985=CARTESIAN_POINT('Ctrl Pts',(203.72789556094,12.0704170843594,29.0087746667653));
#74986=CARTESIAN_POINT('Ctrl Pts',(203.731172723387,12.0905263235356,29.0525942170029));
#74987=CARTESIAN_POINT('Ctrl Pts',(203.734449885835,12.1079857460662,29.0977494691135));
#74988=CARTESIAN_POINT('Ctrl Pts',(203.737727048282,12.1226212086448,29.1438866972425));
#74989=CARTESIAN_POINT('Ctrl Pts',(203.740901000165,12.1367957437058,29.1885708849965));
#74990=CARTESIAN_POINT('Ctrl Pts',(203.744074952048,12.148321384721,29.2341755326984));
#74991=CARTESIAN_POINT('Ctrl Pts',(203.747248903931,12.1570877514646,29.2803571127702));
#74992=CARTESIAN_POINT('Ctrl Pts',(203.750419730852,12.1658454871523,29.3264932240856));
#74993=CARTESIAN_POINT('Ctrl Pts',(203.753590557774,12.1718492225175,29.3732045987342));
#74994=CARTESIAN_POINT('Ctrl Pts',(203.756761384696,12.1750389784448,29.420134728227));
#74995=CARTESIAN_POINT('Ctrl Pts',(203.759930481197,12.1782269936212,29.4670392464605));
#74996=CARTESIAN_POINT('Ctrl Pts',(203.763099577698,12.1786040339559,29.5141617283881));
#74997=CARTESIAN_POINT('Ctrl Pts',(203.766268674199,12.1761619412433,29.5611404160168));
#74998=CARTESIAN_POINT('Ctrl Pts',(203.769437431821,12.1737201096694,29.608114080105));
#74999=CARTESIAN_POINT('Ctrl Pts',(203.772606189443,12.1684597747374,29.6549434247692));
#75000=CARTESIAN_POINT('Ctrl Pts',(203.775774947065,12.1604248061988,29.7012693013313));
#75001=CARTESIAN_POINT('Ctrl Pts',(203.778946891068,12.1523817580038,29.7476417614194));
#75002=CARTESIAN_POINT('Ctrl Pts',(203.782118835072,12.1415586066478,29.7935091941591));
#75003=CARTESIAN_POINT('Ctrl Pts',(203.785290779075,12.1280504480154,29.8385221547139));
#75004=CARTESIAN_POINT('Ctrl Pts',(203.788464667918,12.1145340070186,29.8835627144226));
#75005=CARTESIAN_POINT('Ctrl Pts',(203.79163855676,12.0983294745641,29.9277472365617));
#75006=CARTESIAN_POINT('Ctrl Pts',(203.794812445603,12.0795808193802,29.9707444284603));
#75007=CARTESIAN_POINT('Ctrl Pts',(203.797991949664,12.0607989942246,30.013817690649));
#75008=CARTESIAN_POINT('Ctrl Pts',(203.801171453726,12.0394643237894,30.055698938682));
#75009=CARTESIAN_POINT('Ctrl Pts',(203.804350957787,12.0157666716959,30.0960814803127));
#75010=CARTESIAN_POINT('Ctrl Pts',(203.805083125083,12.0103096427031,30.1053806589661));
#75011=CARTESIAN_POINT('Ctrl Pts',(203.805815292378,12.0047274881293,30.1146004918079));
#75012=CARTESIAN_POINT('Ctrl Pts',(203.806547459674,11.9990228373354,30.1237374712028));
#75013=CARTESIAN_POINT('Ctrl Pts',(203.809824622121,11.9734889634953,30.1646343617529));
#75014=CARTESIAN_POINT('Ctrl Pts',(203.813101784569,11.9453820663439,30.2040530175907));
#75015=CARTESIAN_POINT('Ctrl Pts',(203.816378947016,11.9149017648864,30.2416534386813));
#75016=CARTESIAN_POINT('Ctrl Pts',(203.819552899594,11.8853813999498,30.278069684561));
#75017=CARTESIAN_POINT('Ctrl Pts',(203.822726852172,11.8536352991124,30.3127800606325));
#75018=CARTESIAN_POINT('Ctrl Pts',(203.825900804751,11.8198896376673,30.3455034266907));
#75019=CARTESIAN_POINT('Ctrl Pts',(203.829071632361,11.7861772010776,30.3781945744115));
#75020=CARTESIAN_POINT('Ctrl Pts',(203.832242459971,11.750469498702,30.408902198503));
#75021=CARTESIAN_POINT('Ctrl Pts',(203.835413287581,11.7130312698498,30.4373801100495));
#75022=CARTESIAN_POINT('Ctrl Pts',(203.838582384763,11.6756134723184,30.4658424802265));
#75023=CARTESIAN_POINT('Ctrl Pts',(203.841751481944,11.6364674617191,30.4920772119245));
#75024=CARTESIAN_POINT('Ctrl Pts',(203.844920579125,11.5958908656149,30.5158785059133));
#75025=CARTESIAN_POINT('Ctrl Pts',(203.848089337418,11.5553186085821,30.5396772547032));
#75026=CARTESIAN_POINT('Ctrl Pts',(203.851258095711,11.513316550963,30.5610428028245));
#75027=CARTESIAN_POINT('Ctrl Pts',(203.854426854004,11.4702087593309,30.5798142364076));
#75028=CARTESIAN_POINT('Ctrl Pts',(203.857598798659,11.4270576204216,30.5986045457091));
#75029=CARTESIAN_POINT('Ctrl Pts',(203.860770743314,11.3827990411416,30.6147953150461));
#75030=CARTESIAN_POINT('Ctrl Pts',(203.863942687969,11.3377771611781,30.6282737486472));
#75031=CARTESIAN_POINT('Ctrl Pts',(203.867116577453,11.2927276767451,30.6417604463414));
#75032=CARTESIAN_POINT('Ctrl Pts',(203.870290466937,11.2469145024704,30.6525313715803));
#75033=CARTESIAN_POINT('Ctrl Pts',(203.873464356421,11.2006935012809,30.660524528411));
#75034=CARTESIAN_POINT('Ctrl Pts',(203.876643861103,11.1543907265893,30.6685318266149));
#75035=CARTESIAN_POINT('Ctrl Pts',(203.879823365784,11.1076792388029,30.6737514955824));
#75036=CARTESIAN_POINT('Ctrl Pts',(203.883002870466,11.0609196009251,30.6761733990884));
#75037=CARTESIAN_POINT('Ctrl Pts',(203.883735033113,11.050151992858,30.6767311045992));
#75038=CARTESIAN_POINT('Ctrl Pts',(203.884467195761,11.0393818232111,30.6771406714871));
#75039=CARTESIAN_POINT('Ctrl Pts',(203.885199358408,11.0286134675187,30.6774023662183));
#75040=CARTESIAN_POINT('Ctrl Pts',(203.888378113557,10.9818616068113,30.6785385392771));
#75041=CARTESIAN_POINT('Ctrl Pts',(203.891556868707,10.9349396859611,30.676888279367));
#75042=CARTESIAN_POINT('Ctrl Pts',(203.894735623856,10.8882069579571,30.6724322488958));
#75043=CARTESIAN_POINT('Ctrl Pts',(203.897909711837,10.8415428447053,30.6679827609364));
#75044=CARTESIAN_POINT('Ctrl Pts',(203.901083799818,10.795067924098,30.6607357068325));
#75045=CARTESIAN_POINT('Ctrl Pts',(203.904257887799,10.7491415207722,30.6507237226631));
#75046=CARTESIAN_POINT('Ctrl Pts',(203.907428708611,10.7032623906616,30.6407220440836));
#75047=CARTESIAN_POINT('Ctrl Pts',(203.910599529423,10.6579312015293,30.6279611886194));
#75048=CARTESIAN_POINT('Ctrl Pts',(203.913770350234,10.6134995096863,30.612525250719));
#75049=CARTESIAN_POINT('Ctrl Pts',(203.916939298735,10.5690940539301,30.5970984274524));
#75050=CARTESIAN_POINT('Ctrl Pts',(203.920108247236,10.5255875676862,30.5789998350351));
#75051=CARTESIAN_POINT('Ctrl Pts',(203.923277195737,10.4833161705163,30.5583633038093));
#75052=CARTESIAN_POINT('Ctrl Pts',(203.926447272807,10.4410297190819,30.5377194232214));
#75053=CARTESIAN_POINT('Ctrl Pts',(203.929617349877,10.3999797404455,30.5145360339655));
#75054=CARTESIAN_POINT('Ctrl Pts',(203.932787426947,10.3604800787254,30.4889941014955));
#75055=CARTESIAN_POINT('Ctrl Pts',(203.93595812237,10.3209727122315,30.4634471868357));
#75056=CARTESIAN_POINT('Ctrl Pts',(203.939128817793,10.2830167219262,30.4355411317108));
#75057=CARTESIAN_POINT('Ctrl Pts',(203.942299513216,10.2468962926746,30.4054997893499));
#75058=CARTESIAN_POINT('Ctrl Pts',(203.945474436867,10.2107276956168,30.3754183858495));
#75059=CARTESIAN_POINT('Ctrl Pts',(203.948649360519,10.1763999577101,30.3431963866487));
#75060=CARTESIAN_POINT('Ctrl Pts',(203.951824284171,10.1441620501808,30.3090960796773));
#75061=CARTESIAN_POINT('Ctrl Pts',(203.953223686461,10.1299526371139,30.294065781975));
#75062=CARTESIAN_POINT('Ctrl Pts',(203.954623088751,10.1161487176961,30.2786710283514));
#75063=CARTESIAN_POINT('Ctrl Pts',(203.956022491041,10.1027690874833,30.2629362700282));
#75064=CARTESIAN_POINT('Origin',(197.762132885264,11.,29.5));
#75065=CARTESIAN_POINT('',(204.55557810053,10.1027691095676,30.2629362959998));
#75066=CARTESIAN_POINT('',(204.456095751509,10.1027690874833,30.2629362700282));
#75067=CARTESIAN_POINT('',(197.762132885264,10.1027690874833,30.2629362700282));
#75068=CARTESIAN_POINT('',(204.109784405193,9.82224970774337,29.4997795333053));
#75069=CARTESIAN_POINT('Ctrl Pts',(204.55557810053,10.1027691095676,30.2629362959998));
#75070=CARTESIAN_POINT('Ctrl Pts',(204.554745776962,10.1111980219123,30.2728488936414));
#75071=CARTESIAN_POINT('Ctrl Pts',(204.553908087797,10.1197925935299,30.2826234406836));
#75072=CARTESIAN_POINT('Ctrl Pts',(204.551884317315,10.1407946177784,30.3057248486708));
#75073=CARTESIAN_POINT('Ctrl Pts',(204.550693062403,10.1533497353789,30.318907621637));
#75074=CARTESIAN_POINT('Ctrl Pts',(204.548803084603,10.1735280718412,30.3391345148177));
#75075=CARTESIAN_POINT('Ctrl Pts',(204.548113103554,10.1809477838916,30.3463781884366));
#75076=CARTESIAN_POINT('Ctrl Pts',(204.546807871193,10.1950758178344,30.3598112650973));
#75077=CARTESIAN_POINT('Ctrl Pts',(204.546193618398,10.2017623608044,30.3660225251029));
#75078=CARTESIAN_POINT('Ctrl Pts',(204.544794249705,10.2170758317143,30.3799194789959));
#75079=CARTESIAN_POINT('Ctrl Pts',(204.544007222387,10.225744917043,30.3875570927461));
#75080=CARTESIAN_POINT('Ctrl Pts',(204.541539198746,10.2530953389058,30.4109476351716));
#75081=CARTESIAN_POINT('Ctrl Pts',(204.539840473675,10.2721544739678,30.4262466764234));
#75082=CARTESIAN_POINT('Ctrl Pts',(204.532031285784,10.3607694339367,30.4929546206106));
#75083=CARTESIAN_POINT('Ctrl Pts',(204.525669634465,10.4353752218609,30.5371929714194));
#75084=CARTESIAN_POINT('Ctrl Pts',(204.516822567785,10.5454123843986,30.5870253237653));
#75085=CARTESIAN_POINT('Ctrl Pts',(204.514320324364,10.5772958717402,30.599816096644));
#75086=CARTESIAN_POINT('Ctrl Pts',(204.510858149916,10.6229478750447,30.615851282649));
#75087=CARTESIAN_POINT('Ctrl Pts',(204.509860917012,10.6362842472105,30.6202692878998));
#75088=CARTESIAN_POINT('Ctrl Pts',(204.508112092945,10.6600540619066,30.6276743766632));
#75089=CARTESIAN_POINT('Ctrl Pts',(204.507356378825,10.6704556117793,30.6307578244591));
#75090=CARTESIAN_POINT('Ctrl Pts',(204.506199788064,10.6865983859883,30.6353015241072));
#75091=CARTESIAN_POINT('Ctrl Pts',(204.505793668175,10.6923102162764,30.6368628426981));
#75092=CARTESIAN_POINT('Ctrl Pts',(204.50503434556,10.7030763376691,30.6397186575149));
#75093=CARTESIAN_POINT('Ctrl Pts',(204.504680659137,10.7081276187083,30.641022696464));
#75094=CARTESIAN_POINT('Ctrl Pts',(204.503835791482,10.7202778874684,30.6440734431089));
#75095=CARTESIAN_POINT('Ctrl Pts',(204.503346398639,10.7273847615884,30.6457876947001));
#75096=CARTESIAN_POINT('Ctrl Pts',(204.501623789972,10.7526240125976,30.6516275303393));
#75097=CARTESIAN_POINT('Ctrl Pts',(204.500408692096,10.7708386157387,30.655389976436));
#75098=CARTESIAN_POINT('Ctrl Pts',(204.497297648052,10.8182915405941,30.6640254743173));
#75099=CARTESIAN_POINT('Ctrl Pts',(204.495426641045,10.8476390295869,30.6682292694141));
#75100=CARTESIAN_POINT('Ctrl Pts',(204.487523861422,10.9733374894133,30.6814164112386));
#75101=CARTESIAN_POINT('Ctrl Pts',(204.481661909588,11.0704308629258,30.6796163736572));
#75102=CARTESIAN_POINT('Ctrl Pts',(204.474023883215,11.1878534656056,30.6628774906809));
#75103=CARTESIAN_POINT('Ctrl Pts',(204.472600695937,11.2094047910487,30.6591904593781));
#75104=CARTESIAN_POINT('Ctrl Pts',(204.470416310092,11.2418881050987,30.6526977677804));
#75105=CARTESIAN_POINT('Ctrl Pts',(204.469668656499,11.2529036117014,30.6503311471025));
#75106=CARTESIAN_POINT('Ctrl Pts',(204.468304134126,11.272810370177,30.645754542507));
#75107=CARTESIAN_POINT('Ctrl Pts',(204.467688991975,11.2817131062426,30.6435981319967));
#75108=CARTESIAN_POINT('Ctrl Pts',(204.46634805724,11.3009595690559,30.6386979002208));
#75109=CARTESIAN_POINT('Ctrl Pts',(204.465621123966,11.3112927935014,30.6359165259502));
#75110=CARTESIAN_POINT('Ctrl Pts',(204.463546764024,11.3404865582047,30.6276302411897));
#75111=CARTESIAN_POINT('Ctrl Pts',(204.462188993247,11.3592484873497,30.6217938769279));
#75112=CARTESIAN_POINT('Ctrl Pts',(204.459057046591,11.4017200237634,30.6074073265689));
#75113=CARTESIAN_POINT('Ctrl Pts',(204.457274372454,11.4253181903111,30.5985600804324));
#75114=CARTESIAN_POINT('Ctrl Pts',(204.450615775465,11.5113982158899,30.5630982546894));
#75115=CARTESIAN_POINT('Ctrl Pts',(204.445621875268,11.5718244254159,30.5318533729823));
#75116=CARTESIAN_POINT('Ctrl Pts',(204.436977362713,11.6716886138843,30.4687383079762));
#75117=CARTESIAN_POINT('Ctrl Pts',(204.433326630719,11.7124043028962,30.4392021364571));
#75118=CARTESIAN_POINT('Ctrl Pts',(204.429121042398,11.7586677153507,30.4008965438966));
#75119=CARTESIAN_POINT('Ctrl Pts',(204.428439463496,11.7661451169688,30.3945462315567));
#75120=CARTESIAN_POINT('Ctrl Pts',(204.427369443249,11.7778642775782,30.3843387780364));
#75121=CARTESIAN_POINT('Ctrl Pts',(204.426976964063,11.7821585383281,30.3805429762643));
#75122=CARTESIAN_POINT('Ctrl Pts',(204.426224165178,11.790390030381,30.3731592256754));
#75123=CARTESIAN_POINT('Ctrl Pts',(204.42586357981,11.7943308738264,30.3695756997327));
#75124=CARTESIAN_POINT('Ctrl Pts',(204.424973120861,11.8040538041751,30.3606130987966));
#75125=CARTESIAN_POINT('Ctrl Pts',(204.424445532006,11.8098064879895,30.3552022487109));
#75126=CARTESIAN_POINT('Ctrl Pts',(204.422395599075,11.8321038574246,30.3338030694266));
#75127=CARTESIAN_POINT('Ctrl Pts',(204.420901667475,11.8482341201247,30.317388173009));
#75128=CARTESIAN_POINT('Ctrl Pts',(204.416778776716,11.8920152867722,30.2701415163189));
#75129=CARTESIAN_POINT('Ctrl Pts',(204.414199423287,11.9185372869186,30.238308152145));
#75130=CARTESIAN_POINT('Ctrl Pts',(204.406279980061,11.9949899273806,30.1360309127493));
#75131=CARTESIAN_POINT('Ctrl Pts',(204.400982168585,12.0388945956149,30.0614593749804));
#75132=CARTESIAN_POINT('Ctrl Pts',(204.394240122505,12.0814877453746,29.9666800598424));
#75133=CARTESIAN_POINT('Ctrl Pts',(204.39308534383,12.088353533864,29.9504359610527));
#75134=CARTESIAN_POINT('Ctrl Pts',(204.391231512937,12.098678702535,29.9243913290238));
#75135=CARTESIAN_POINT('Ctrl Pts',(204.390540361116,12.1023776808149,29.9146882310558));
#75136=CARTESIAN_POINT('Ctrl Pts',(204.389230013585,12.1091051380097,29.8963145020388));
#75137=CARTESIAN_POINT('Ctrl Pts',(204.388611784007,12.1121614564469,29.8876548443636));
#75138=CARTESIAN_POINT('Ctrl Pts',(204.387199105754,12.1188769449826,29.8678940807945));
#75139=CARTESIAN_POINT('Ctrl Pts',(204.386402675847,12.1224726985126,29.8567726122705));
#75140=CARTESIAN_POINT('Ctrl Pts',(204.38388570204,12.1332391259366,29.8216975213308));
#75141=CARTESIAN_POINT('Ctrl Pts',(204.382146591257,12.1398125036699,29.7975693319459));
#75142=CARTESIAN_POINT('Ctrl Pts',(204.377905842197,12.1537776953688,29.7390200180092));
#75143=CARTESIAN_POINT('Ctrl Pts',(204.375384110328,12.1604035985836,29.704442315802));
#75144=CARTESIAN_POINT('Ctrl Pts',(204.371726201364,12.1676713334131,29.6545058840086));
#75145=CARTESIAN_POINT('Ctrl Pts',(204.370613920137,12.1695770324573,29.6393483319633));
#75146=CARTESIAN_POINT('Ctrl Pts',(204.364423258903,12.1785130936366,29.5550543202146));
#75147=CARTESIAN_POINT('Ctrl Pts',(204.359281618865,12.1797086750246,29.4854362752628));
#75148=CARTESIAN_POINT('Ctrl Pts',(204.352907200928,12.173357620497,29.3964909665236));
#75149=CARTESIAN_POINT('Ctrl Pts',(204.35151623384,12.1714644858877,29.3769013034547));
#75150=CARTESIAN_POINT('Ctrl Pts',(204.349614468664,12.1681522977836,29.3497531863812));
#75151=CARTESIAN_POINT('Ctrl Pts',(204.349084582911,12.1671489888399,29.3421483561042));
#75152=CARTESIAN_POINT('Ctrl Pts',(204.348200036601,12.165336838816,29.3293762641083));
#75153=CARTESIAN_POINT('Ctrl Pts',(204.34784329957,12.1645677601495,29.3242036874267));
#75154=CARTESIAN_POINT('Ctrl Pts',(204.347096619893,12.1628766886828,29.3133285397174));
#75155=CARTESIAN_POINT('Ctrl Pts',(204.346707085192,12.1619471601479,29.3076273727663));
#75156=CARTESIAN_POINT('Ctrl Pts',(204.34564465038,12.1592827137057,29.2920096295967));
#75157=CARTESIAN_POINT('Ctrl Pts',(204.344976216975,12.1574624955683,29.2821078424359));
#75158=CARTESIAN_POINT('Ctrl Pts',(204.34012046097,12.1431968627417,29.2097358231912));
#75159=CARTESIAN_POINT('Ctrl Pts',(204.336160702075,12.1258269466844,29.1483351257714));
#75160=CARTESIAN_POINT('Ctrl Pts',(204.327127904238,12.074908913771,29.0117370654091));
#75161=CARTESIAN_POINT('Ctrl Pts',(204.322075742681,12.0382896372784,28.9380544029841));
#75162=CARTESIAN_POINT('Ctrl Pts',(204.315588171637,11.9846576902123,28.8535723292387));
#75163=CARTESIAN_POINT('Ctrl Pts',(204.314409377392,11.974656844726,28.8385897791776));
#75164=CARTESIAN_POINT('Ctrl Pts',(204.312526326095,11.9583121467903,28.8152794121022));
#75165=CARTESIAN_POINT('Ctrl Pts',(204.31183043347,11.9521938712117,28.806796368924));
#75166=CARTESIAN_POINT('Ctrl Pts',(204.310522725908,11.9405576354677,28.791107379467));
#75167=CARTESIAN_POINT('Ctrl Pts',(204.309912015226,11.9350677556221,28.7838815058672));
#75168=CARTESIAN_POINT('Ctrl Pts',(204.308520137631,11.9224340268286,28.7676457634479));
#75169=CARTESIAN_POINT('Ctrl Pts',(204.307737080301,11.9152407256599,28.7586757392233));
#75170=CARTESIAN_POINT('Ctrl Pts',(204.3053067895,11.8926611795702,28.73134874348));
#75171=CARTESIAN_POINT('Ctrl Pts',(204.303642749872,11.8768462267564,28.7133556787146));
#75172=CARTESIAN_POINT('Ctrl Pts',(204.299629325177,11.837890852275,28.6716703727502));
#75173=CARTESIAN_POINT('Ctrl Pts',(204.297262655316,11.8142789620539,28.648448175744));
#75174=CARTESIAN_POINT('Ctrl Pts',(204.291506543989,11.755234017991,28.5950813708977));
#75175=CARTESIAN_POINT('Ctrl Pts',(204.288094326118,11.7189320233866,28.5659804464613));
#75176=CARTESIAN_POINT('Ctrl Pts',(204.280823855644,11.6380105098521,28.5086297599253));
#75177=CARTESIAN_POINT('Ctrl Pts',(204.276974534597,11.5930129744244,28.4810746042428));
#75178=CARTESIAN_POINT('Ctrl Pts',(204.272376929497,11.5352478572156,28.4508284592319));
#75179=CARTESIAN_POINT('Ctrl Pts',(204.271503771116,11.5240862654587,28.4452086426314));
#75180=CARTESIAN_POINT('Ctrl Pts',(204.270206900487,11.5071900733611,28.4370359187963));
#75181=CARTESIAN_POINT('Ctrl Pts',(204.269775948708,11.5015214381559,28.434349653983));
#75182=CARTESIAN_POINT('Ctrl Pts',(204.268998162646,11.4911873108329,28.4295532229692));
#75183=CARTESIAN_POINT('Ctrl Pts',(204.268650488276,11.4865292862608,28.4274280759828));
#75184=CARTESIAN_POINT('Ctrl Pts',(204.267846729463,11.4756722661313,28.4225600236078));
#75185=CARTESIAN_POINT('Ctrl Pts',(204.267391994105,11.4694632548893,28.4198401667947));
#75186=CARTESIAN_POINT('Ctrl Pts',(204.265924122469,11.4492180507266,28.411179306674));
#75187=CARTESIAN_POINT('Ctrl Pts',(204.264922739257,11.4350893387576,28.4054568630078));
#75188=CARTESIAN_POINT('Ctrl Pts',(204.258345572308,11.3405077118606,28.3692702274533));
#75189=CARTESIAN_POINT('Ctrl Pts',(204.25312642971,11.2570277139934,28.3474222297287));
#75190=CARTESIAN_POINT('Ctrl Pts',(204.244231415542,11.1156167382245,28.3265584344973));
#75191=CARTESIAN_POINT('Ctrl Pts',(204.240646943057,11.058807524477,28.322344320574));
#75192=CARTESIAN_POINT('Ctrl Pts',(204.235935295069,10.9865590564877,28.3222265188801));
#75193=CARTESIAN_POINT('Ctrl Pts',(204.234925193039,10.9711993712725,28.3225020083185));
#75194=CARTESIAN_POINT('Ctrl Pts',(204.233254494822,10.9460388005098,28.3234458589001));
#75195=CARTESIAN_POINT('Ctrl Pts',(204.232599365507,10.9362328234938,28.3239365682666));
#75196=CARTESIAN_POINT('Ctrl Pts',(204.231312439351,10.9170952848175,28.325134292428));
#75197=CARTESIAN_POINT('Ctrl Pts',(204.230681036085,10.907763735471,28.325830044027));
#75198=CARTESIAN_POINT('Ctrl Pts',(204.22916693346,10.8855308215203,28.3277543734305));
#75199=CARTESIAN_POINT('Ctrl Pts',(204.228281169237,10.8726397385016,28.3290848269138));
#75200=CARTESIAN_POINT('Ctrl Pts',(204.22508806256,10.8265967731223,28.3346061106229));
#75201=CARTESIAN_POINT('Ctrl Pts',(204.22274485365,10.7936072879412,28.3399942792959));
#75202=CARTESIAN_POINT('Ctrl Pts',(204.216420672344,10.7066693616982,28.3580197395405));
#75203=CARTESIAN_POINT('Ctrl Pts',(204.212380613469,10.65330986838,28.3730720118885));
#75204=CARTESIAN_POINT('Ctrl Pts',(204.203631289139,10.5410138016058,28.4134827070862));
#75205=CARTESIAN_POINT('Ctrl Pts',(204.198928860319,10.4826759569628,28.4400163528347));
#75206=CARTESIAN_POINT('Ctrl Pts',(204.193570689384,10.4162452711662,28.4770284121859));
#75207=CARTESIAN_POINT('Ctrl Pts',(204.192728490488,10.4058022506269,28.4830587454804));
#75208=CARTESIAN_POINT('Ctrl Pts',(204.19146244962,10.39007627934,28.4924647045212));
#75209=CARTESIAN_POINT('Ctrl Pts',(204.191032031073,10.3847249487371,28.4957236772754));
#75210=CARTESIAN_POINT('Ctrl Pts',(204.190251186479,10.3750033523339,28.5017510277007));
#75211=CARTESIAN_POINT('Ctrl Pts',(204.189899966324,10.3706250968491,28.5045056236173));
#75212=CARTESIAN_POINT('Ctrl Pts',(204.189089486471,10.3605105440549,28.5109626372211));
#75213=CARTESIAN_POINT('Ctrl Pts',(204.188631582506,10.3547881010653,28.514686202123));
#75214=CARTESIAN_POINT('Ctrl Pts',(204.18714186702,10.336158999619,28.5270399612884));
#75215=CARTESIAN_POINT('Ctrl Pts',(204.186122297674,10.3233900014001,28.5358760062349));
#75216=CARTESIAN_POINT('Ctrl Pts',(204.183633203972,10.2922933699872,28.5583168382468));
#75217=CARTESIAN_POINT('Ctrl Pts',(204.182177797436,10.2741789379744,28.5722070501096));
#75218=CARTESIAN_POINT('Ctrl Pts',(204.174928251564,10.1850764330714,28.6447390773026));
#75219=CARTESIAN_POINT('Ctrl Pts',(204.169367996765,10.1207357642974,28.7110341144688));
#75220=CARTESIAN_POINT('Ctrl Pts',(204.161468371099,10.0450624434254,28.8098979704313));
#75221=CARTESIAN_POINT('Ctrl Pts',(204.159382572204,10.0264264430857,28.8364483460071));
#75222=CARTESIAN_POINT('Ctrl Pts',(204.156394129913,10.0018017531591,28.8748052513019));
#75223=CARTESIAN_POINT('Ctrl Pts',(204.155525123391,9.99487921469159,28.8859964184365));
#75224=CARTESIAN_POINT('Ctrl Pts',(204.154030610076,9.98338809670228,28.9052885241774));
#75225=CARTESIAN_POINT('Ctrl Pts',(204.153408527385,9.97872520973934,28.9133320395185));
#75226=CARTESIAN_POINT('Ctrl Pts',(204.15212813132,9.96937612431642,28.9299085619115));
#75227=CARTESIAN_POINT('Ctrl Pts',(204.151469541064,9.96469952930371,28.9384461321075));
#75228=CARTESIAN_POINT('Ctrl Pts',(204.149789657626,9.9531079909186,28.9602446530653));
#75229=CARTESIAN_POINT('Ctrl Pts',(204.148763436784,9.94633899082173,28.9735808175985));
#75230=CARTESIAN_POINT('Ctrl Pts',(204.143949116277,9.91603758825061,29.0362072755362));
#75231=CARTESIAN_POINT('Ctrl Pts',(204.140056653699,9.89570132312146,29.0869610898323));
#75232=CARTESIAN_POINT('Ctrl Pts',(204.131732373736,9.86054078064419,29.1961283208153));
#75233=CARTESIAN_POINT('Ctrl Pts',(204.127296777677,9.8465242743122,29.2546457658897));
#75234=CARTESIAN_POINT('Ctrl Pts',(204.121446219523,9.83383472865169,29.3339760672685));
#75235=CARTESIAN_POINT('Ctrl Pts',(204.119979435993,9.83115164405392,29.354058315545));
#75236=CARTESIAN_POINT('Ctrl Pts',(204.116999983028,9.82671004016305,29.3954032695704));
#75237=CARTESIAN_POINT('Ctrl Pts',(204.115489471811,9.82500838341042,29.4166655094815));
#75238=CARTESIAN_POINT('Ctrl Pts',(204.1134667947,9.8234774545883,29.4456896073132));
#75239=CARTESIAN_POINT('Ctrl Pts',(204.112931883378,9.82314606023393,29.453419628203));
#75240=CARTESIAN_POINT('Ctrl Pts',(204.11204068262,9.82271770775898,29.4663990733415));
#75241=CARTESIAN_POINT('Ctrl Pts',(204.111682272025,9.82257963375483,29.4716468161139));
#75242=CARTESIAN_POINT('Ctrl Pts',(204.111039268964,9.82239385946823,29.4811148265866));
#75243=CARTESIAN_POINT('Ctrl Pts',(204.110753978788,9.82233374819688,29.485334641075));
#75244=CARTESIAN_POINT('Ctrl Pts',(204.110240427777,9.82226609048611,29.4929630738052));
#75245=CARTESIAN_POINT('Ctrl Pts',(204.110011756713,9.82225065704661,29.496371537964));
#75246=CARTESIAN_POINT('Ctrl Pts',(204.109783827458,9.82225002053532,29.4997800660184));
#75247=CARTESIAN_POINT('Ctrl Pts',(204.10978386549,9.82225002064167,29.4997794972763));
#75248=CARTESIAN_POINT('Ctrl Pts',(204.109493826047,9.82224920858832,29.5041168396691));
#75249=CARTESIAN_POINT('Ctrl Pts',(204.109204990594,9.82227235645611,29.5084542433456));
#75250=CARTESIAN_POINT('Ctrl Pts',(204.108379855853,9.82240746594007,29.520893416986));
#75251=CARTESIAN_POINT('Ctrl Pts',(204.107846393483,9.82257907222981,29.5289944467413));
#75252=CARTESIAN_POINT('Ctrl Pts',(204.101471028651,9.82564897302465,29.6264185570605));
#75253=CARTESIAN_POINT('Ctrl Pts',(204.09605367425,9.83862196096357,29.7151449027121));
#75254=CARTESIAN_POINT('Ctrl Pts',(204.088069294272,9.8714905643461,29.8392354012598));
#75255=CARTESIAN_POINT('Ctrl Pts',(204.085625935575,9.88333385118579,29.876391552533));
#75256=CARTESIAN_POINT('Ctrl Pts',(204.081419446639,9.90639465079352,29.9379966397552));
#75257=CARTESIAN_POINT('Ctrl Pts',(204.079683576393,9.91664662027715,29.9627731652066));
#75258=CARTESIAN_POINT('Ctrl Pts',(204.077131784329,9.93269249009064,29.9980897641917));
#75259=CARTESIAN_POINT('Ctrl Pts',(204.076337999482,9.93781677914765,30.0089258511647));
#75260=CARTESIAN_POINT('Ctrl Pts',(204.074924237649,9.9471701139909,30.0279480570959));
#75261=CARTESIAN_POINT('Ctrl Pts',(204.074306603485,9.95133156268224,30.0361664110164));
#75262=CARTESIAN_POINT('Ctrl Pts',(204.072997524398,9.96030649845121,30.053386549645));
#75263=CARTESIAN_POINT('Ctrl Pts',(204.072305374689,9.9651414476128,30.0623762226366));
#75264=CARTESIAN_POINT('Ctrl Pts',(204.070431971251,9.97846348767142,30.0863923763004));
#75265=CARTESIAN_POINT('Ctrl Pts',(204.06924331685,9.98716473063975,30.1012965391982));
#75266=CARTESIAN_POINT('Ctrl Pts',(204.063826114451,10.027910747529,30.1676943165029));
#75267=CARTESIAN_POINT('Ctrl Pts',(204.059474275311,10.0635499361904,30.2168136609253));
#75268=CARTESIAN_POINT('Ctrl Pts',(204.05505724195,10.1027693394584,30.2629365663567));
#75269=CARTESIAN_POINT('',(204.012132885318,9.82225017882538,29.4993509829379));
#75270=CARTESIAN_POINT('Ctrl Pts',(203.956022491041,10.1027690874833,30.2629362700282));
#75271=CARTESIAN_POINT('Ctrl Pts',(203.958632079741,10.0778189126353,30.2335942803683));
#75272=CARTESIAN_POINT('Ctrl Pts',(203.961241668442,10.0543454181236,30.2030692919077));
#75273=CARTESIAN_POINT('Ctrl Pts',(203.963851257142,10.0324550016372,30.1715294026647));
#75274=CARTESIAN_POINT('Ctrl Pts',(203.967065387968,10.005493410941,30.1326829245767));
#75275=CARTESIAN_POINT('Ctrl Pts',(203.970279518795,9.98081770306318,30.0921278837912));
#75276=CARTESIAN_POINT('Ctrl Pts',(203.973493649621,9.95864549626695,30.0501598495482));
#75277=CARTESIAN_POINT('Ctrl Pts',(203.976713585924,9.93643324124246,30.0081160111496));
#75278=CARTESIAN_POINT('Ctrl Pts',(203.979933522228,9.91673389153112,29.9646544914047));
#75279=CARTESIAN_POINT('Ctrl Pts',(203.983153458532,9.89972341279482,29.9201029566048));
#75280=CARTESIAN_POINT('Ctrl Pts',(203.986357215351,9.88279840803636,29.8757752836349));
#75281=CARTESIAN_POINT('Ctrl Pts',(203.989560972171,9.86853554105832,29.8303690191676));
#75282=CARTESIAN_POINT('Ctrl Pts',(203.992764728991,9.85706155550171,29.7842301437002));
#75283=CARTESIAN_POINT('Ctrl Pts',(203.995992755036,9.84550065175501,29.7377417551949));
#75284=CARTESIAN_POINT('Ctrl Pts',(203.999220781082,9.83677128654062,29.6905101206683));
#75285=CARTESIAN_POINT('Ctrl Pts',(204.002448807127,9.83095203688582,29.6429052918495));
#75286=CARTESIAN_POINT('Ctrl Pts',(204.005676833173,9.82513278723102,29.5953004630307));
#75287=CARTESIAN_POINT('Ctrl Pts',(204.008904859218,9.82222374314532,29.547322997184));
#75288=CARTESIAN_POINT('Ctrl Pts',(204.012132885264,9.82225017882494,29.499350983736));
#75289=CARTESIAN_POINT('Ctrl Pts',(204.012132885318,9.82225017882538,29.4993509829379));
#75290=CARTESIAN_POINT('Ctrl Pts',(204.015663251205,9.82227909053024,29.4468858672742));
#75291=CARTESIAN_POINT('Ctrl Pts',(204.019193617093,9.82581787908988,29.3945447125145));
#75292=CARTESIAN_POINT('Ctrl Pts',(204.022723982981,9.8327924956972,29.3427686278148));
#75293=CARTESIAN_POINT('Ctrl Pts',(204.026279617378,9.8398170329567,29.2906219570227));
#75294=CARTESIAN_POINT('Ctrl Pts',(204.029835251775,9.8503266225995,29.2390487802656));
#75295=CARTESIAN_POINT('Ctrl Pts',(204.033390886173,9.8641956238876,29.1884819721045));
#75296=CARTESIAN_POINT('Ctrl Pts',(204.036428309407,9.87604330619742,29.1452849555299));
#75297=CARTESIAN_POINT('Ctrl Pts',(204.039465732642,9.8903416381416,29.1028221357794));
#75298=CARTESIAN_POINT('Ctrl Pts',(204.042503155876,9.90698494103074,29.0613507741185));
#75299=CARTESIAN_POINT('Ctrl Pts',(204.045780318324,9.92494187459465,29.0166061407299));
#75300=CARTESIAN_POINT('Ctrl Pts',(204.049057480771,9.94569139827068,28.972865032023));
#75301=CARTESIAN_POINT('Ctrl Pts',(204.052334643218,9.96909668806319,28.9304972134065));
#75302=CARTESIAN_POINT('Ctrl Pts',(204.055508599211,9.99176488379466,28.8894636686982));
#75303=CARTESIAN_POINT('Ctrl Pts',(204.058682555204,10.0169237484024,28.8497187236338));
#75304=CARTESIAN_POINT('Ctrl Pts',(204.061856511196,10.0443999796418,28.8115788617486));
#75305=CARTESIAN_POINT('Ctrl Pts',(204.065027342179,10.071849158366,28.7734765515635));
#75306=CARTESIAN_POINT('Ctrl Pts',(204.068198173162,10.1016108634411,28.7369766463296));
#75307=CARTESIAN_POINT('Ctrl Pts',(204.071369004145,10.133467691192,28.7023679919337));
#75308=CARTESIAN_POINT('Ctrl Pts',(204.074538104651,10.1653071331192,28.6677782251675));
#75309=CARTESIAN_POINT('Ctrl Pts',(204.077707205157,10.1992390560383,28.6350780734984));
#75310=CARTESIAN_POINT('Ctrl Pts',(204.080876305663,10.2350065876053,28.6045223947564));
#75311=CARTESIAN_POINT('Ctrl Pts',(204.084045067226,10.2707702937499,28.5739699840169));
#75312=CARTESIAN_POINT('Ctrl Pts',(204.087213828789,10.308368794137,28.5455619505807));
#75313=CARTESIAN_POINT('Ctrl Pts',(204.090382590352,10.3475113074931,28.5195136060859));
#75314=CARTESIAN_POINT('Ctrl Pts',(204.093554538174,10.3866931795006,28.4934390694122));
#75315=CARTESIAN_POINT('Ctrl Pts',(204.096726485996,10.4274216967813,28.4697292630943));
#75316=CARTESIAN_POINT('Ctrl Pts',(204.099898433818,10.4693778685642,28.4485556523855));
#75317=CARTESIAN_POINT('Ctrl Pts',(204.103072326411,10.511359764341,28.4273690598004));
#75318=CARTESIAN_POINT('Ctrl Pts',(204.106246219005,10.5545703010809,28.4087219777471));
#75319=CARTESIAN_POINT('Ctrl Pts',(204.109420111598,10.5986700278209,28.3927379190405));
#75320=CARTESIAN_POINT('Ctrl Pts',(204.112599619276,10.6428477734905,28.3767255821734));
#75321=CARTESIAN_POINT('Ctrl Pts',(204.115779126955,10.6879173127942,28.3633858205434));
#75322=CARTESIAN_POINT('Ctrl Pts',(204.118958634633,10.7335254625529,28.352791918006));
#75323=CARTESIAN_POINT('Ctrl Pts',(204.119690774625,10.7440275760287,28.3503524775291));
#75324=CARTESIAN_POINT('Ctrl Pts',(204.120422914618,10.754558218417,28.3480584158965));
#75325=CARTESIAN_POINT('Ctrl Pts',(204.121155054611,10.7651130357751,28.3459102389601));
#75326=CARTESIAN_POINT('Ctrl Pts',(204.124432217058,10.812357895264,28.336294694316));
#75327=CARTESIAN_POINT('Ctrl Pts',(204.127709379505,10.8603007492285,28.3295633197699));
#75328=CARTESIAN_POINT('Ctrl Pts',(204.130986541953,10.9085575354729,28.3258052383948));
#75329=CARTESIAN_POINT('Ctrl Pts',(204.134160503933,10.9552946769115,28.3221655020087));
#75330=CARTESIAN_POINT('Ctrl Pts',(204.137334465913,11.0023256673031,28.3213146073809));
#75331=CARTESIAN_POINT('Ctrl Pts',(204.140508427893,11.0492908750336,28.3232819062586));
#75332=CARTESIAN_POINT('Ctrl Pts',(204.143679264962,11.0962098433739,28.3252472682408));
#75333=CARTESIAN_POINT('Ctrl Pts',(204.146850102032,11.1430626033167,28.3300253084613));
#75334=CARTESIAN_POINT('Ctrl Pts',(204.150020939101,11.1894883463443,28.3375933460704));
#75335=CARTESIAN_POINT('Ctrl Pts',(204.15319004578,11.2358887538872,28.3451572536455));
#75336=CARTESIAN_POINT('Ctrl Pts',(204.156359152458,11.2818620574893,28.3555080528606));
#75337=CARTESIAN_POINT('Ctrl Pts',(204.159528259136,11.3270541233728,28.3685714061927));
#75338=CARTESIAN_POINT('Ctrl Pts',(204.162697026945,11.3722413569009,28.3816333626697));
#75339=CARTESIAN_POINT('Ctrl Pts',(204.165865794753,11.4166469845708,28.3974071406536));
#75340=CARTESIAN_POINT('Ctrl Pts',(204.169034562561,11.4599312472217,28.4157683317994));
#75341=CARTESIAN_POINT('Ctrl Pts',(204.172206516686,11.5032590338526,28.4341479858244));
#75342=CARTESIAN_POINT('Ctrl Pts',(204.175378470811,11.5454626930871,28.4551200244726));
#75343=CARTESIAN_POINT('Ctrl Pts',(204.178550424936,11.5862235665511,28.4785123630116));
#75344=CARTESIAN_POINT('Ctrl Pts',(204.181724323873,11.6270094316214,28.5019190440331));
#75345=CARTESIAN_POINT('Ctrl Pts',(204.18489822281,11.6663502850955,28.5277486722163));
#75346=CARTESIAN_POINT('Ctrl Pts',(204.188072121747,11.7039562609683,28.5557856995663));
#75347=CARTESIAN_POINT('Ctrl Pts',(204.191251635763,11.741628767168,28.5838723284104));
#75348=CARTESIAN_POINT('Ctrl Pts',(204.19443114978,11.777559850823,28.6141737848394));
#75349=CARTESIAN_POINT('Ctrl Pts',(204.197610663796,11.8114940402065,28.6464354241129));
#75350=CARTESIAN_POINT('Ctrl Pts',(204.198342760312,11.8193075304778,28.653863802665));
#75351=CARTESIAN_POINT('Ctrl Pts',(204.199074856829,11.8270153154154,28.6613959601647));
#75352=CARTESIAN_POINT('Ctrl Pts',(204.199806953345,11.8346145781743,28.6690285393596));
#75353=CARTESIAN_POINT('Ctrl Pts',(204.203084115792,11.8686319761315,28.7031950752653));
#75354=CARTESIAN_POINT('Ctrl Pts',(204.206361278239,11.9006246662942,28.7395309886941));
#75355=CARTESIAN_POINT('Ctrl Pts',(204.209638440687,11.9303069551227,28.7777645593365));
#75356=CARTESIAN_POINT('Ctrl Pts',(204.212812355243,11.9590540953993,28.8147935709767));
#75357=CARTESIAN_POINT('Ctrl Pts',(204.2159862698,11.9856338928332,28.8536019554062));
#75358=CARTESIAN_POINT('Ctrl Pts',(204.219160184356,12.009824020999,28.8939055278973));
#75359=CARTESIAN_POINT('Ctrl Pts',(204.222330974031,12.0339903327477,28.9341694194622));
#75360=CARTESIAN_POINT('Ctrl Pts',(204.225501763707,12.0557713468835,28.9759251098867));
#75361=CARTESIAN_POINT('Ctrl Pts',(204.228672553382,12.0749875432816,29.0188588104419));
#75362=CARTESIAN_POINT('Ctrl Pts',(204.231841612791,12.094193253605,29.0617690825318));
#75363=CARTESIAN_POINT('Ctrl Pts',(204.2350106722,12.110836691774,29.1058555838299));
#75364=CARTESIAN_POINT('Ctrl Pts',(204.238179731609,12.1247851490231,29.1507816857078));
#75365=CARTESIAN_POINT('Ctrl Pts',(204.241348452368,12.138732115721,29.1957029867213));
#75366=CARTESIAN_POINT('Ctrl Pts',(204.244517173128,12.1499845104401,29.2414631779945));
#75367=CARTESIAN_POINT('Ctrl Pts',(204.247685893887,12.1584593468386,29.2877100939229));
#75368=CARTESIAN_POINT('Ctrl Pts',(204.250857801636,12.1669427069349,29.3340035234022));
#75369=CARTESIAN_POINT('Ctrl Pts',(204.254029709385,12.1726428363341,29.3807841053537));
#75370=CARTESIAN_POINT('Ctrl Pts',(204.257201617133,12.1755281712391,29.4276910716214));
#75371=CARTESIAN_POINT('Ctrl Pts',(204.260375470041,12.1784152755635,29.4746268033869));
#75372=CARTESIAN_POINT('Ctrl Pts',(204.263549322949,12.1784841496943,29.5216885167714));
#75373=CARTESIAN_POINT('Ctrl Pts',(204.266723175857,12.1757553646369,29.5685155823705));
#75374=CARTESIAN_POINT('Ctrl Pts',(204.269902644799,12.1730217510792,29.6154255070054));
#75375=CARTESIAN_POINT('Ctrl Pts',(204.273082113741,12.1674806730412,29.6620994038791));
#75376=CARTESIAN_POINT('Ctrl Pts',(204.276261582683,12.1592042709851,29.7081838625587));
#75377=CARTESIAN_POINT('Ctrl Pts',(204.276994005815,12.1572977172724,29.7187998881216));
#75378=CARTESIAN_POINT('Ctrl Pts',(204.277726428947,12.1552462220558,29.7293846924416));
#75379=CARTESIAN_POINT('Ctrl Pts',(204.278458852079,12.1530510414502,29.7399340707581));
#75380=CARTESIAN_POINT('Ctrl Pts',(204.281736014526,12.1432289002165,29.7871363298747));
#75381=CARTESIAN_POINT('Ctrl Pts',(204.285013176974,12.1304813671924,29.8338409394038));
#75382=CARTESIAN_POINT('Ctrl Pts',(204.288290339421,12.114878222444,29.8796598630618));
#75383=CARTESIAN_POINT('Ctrl Pts',(204.291464336444,12.0997662663612,29.9240364021023));
#75384=CARTESIAN_POINT('Ctrl Pts',(204.294638333467,12.0819760303894,29.9675816226212));
#75385=CARTESIAN_POINT('Ctrl Pts',(204.297812330489,12.0616225628927,30.0099535238206));
#75386=CARTESIAN_POINT('Ctrl Pts',(204.300983202136,12.0412891370782,30.0522837021944));
#75387=CARTESIAN_POINT('Ctrl Pts',(204.304154073783,12.0183977156809,30.0934423483772));
#75388=CARTESIAN_POINT('Ctrl Pts',(204.30732494543,11.9931116157764,30.1331069270747));
#75389=CARTESIAN_POINT('Ctrl Pts',(204.310494086156,11.9678393190922,30.1727498536028));
#75390=CARTESIAN_POINT('Ctrl Pts',(204.313663226882,11.9401752324205,30.2108998596238));
#75391=CARTESIAN_POINT('Ctrl Pts',(204.316832367608,11.9103274957914,30.2472609403054));
#75392=CARTESIAN_POINT('Ctrl Pts',(204.320001168869,11.8804829563256,30.2836181261418));
#75393=CARTESIAN_POINT('Ctrl Pts',(204.32316997013,11.8484555861549,30.318186338393));
#75394=CARTESIAN_POINT('Ctrl Pts',(204.326338771391,11.8144938508834,30.3507025504683));
#75395=CARTESIAN_POINT('Ctrl Pts',(204.329510757855,11.7804979780832,30.3832514470666));
#75396=CARTESIAN_POINT('Ctrl Pts',(204.33268274432,11.7445642648754,30.4137438438669));
#75397=CARTESIAN_POINT('Ctrl Pts',(204.335854730785,11.7069766465997,30.4419549265558));
#75398=CARTESIAN_POINT('Ctrl Pts',(204.339028661442,11.669365989896,30.4701833005503));
#75399=CARTESIAN_POINT('Ctrl Pts',(204.3422025921,11.6300998755446,30.4961272709943));
#75400=CARTESIAN_POINT('Ctrl Pts',(204.345376522757,11.5894908009597,30.5196056385112));
#75401=CARTESIAN_POINT('Ctrl Pts',(204.348556067293,11.5488098992197,30.5431255333065));
#75402=CARTESIAN_POINT('Ctrl Pts',(204.35173561183,11.5067817979646,30.5641708805389));
#75403=CARTESIAN_POINT('Ctrl Pts',(204.354915156366,11.4637413329924,30.5826075182514));
#75404=CARTESIAN_POINT('Ctrl Pts',(204.355647021181,11.45383431593,30.5868512476002));
#75405=CARTESIAN_POINT('Ctrl Pts',(204.356378885997,11.4438737289345,30.5909569686217));
#75406=CARTESIAN_POINT('Ctrl Pts',(204.357110750813,11.433863764695,30.5949234202376));
#75407=CARTESIAN_POINT('Ctrl Pts',(204.36038791326,11.3890408982376,30.6126844957851));
#75408=CARTESIAN_POINT('Ctrl Pts',(204.363665075708,11.3430245285796,30.6277287261434));
#75409=CARTESIAN_POINT('Ctrl Pts',(204.366942238155,11.2961771025132,30.6399009546653));
#75410=CARTESIAN_POINT('Ctrl Pts',(204.370116251076,11.2508042111568,30.6516900591832));
#75411=CARTESIAN_POINT('Ctrl Pts',(204.373290263998,11.2046523925093,30.6607851362038));
#75412=CARTESIAN_POINT('Ctrl Pts',(204.37646427692,11.1580705506583,30.6670941536631));
#75413=CARTESIAN_POINT('Ctrl Pts',(204.379635165468,11.111534562129,30.6733969607753));
#75414=CARTESIAN_POINT('Ctrl Pts',(204.382806054017,11.064569937647,30.6769190623471));
#75415=CARTESIAN_POINT('Ctrl Pts',(204.385976942566,11.0175358741519,30.6776194443103));
#75416=CARTESIAN_POINT('Ctrl Pts',(204.389146101151,10.9705274713647,30.6783194441611));
#75417=CARTESIAN_POINT('Ctrl Pts',(204.392315259736,10.9234502604559,30.676200765931));
#75418=CARTESIAN_POINT('Ctrl Pts',(204.39548441832,10.8766659357925,30.6712744217757));
#75419=CARTESIAN_POINT('Ctrl Pts',(204.398653238351,10.8298866089832,30.6663486038897));
#75420=CARTESIAN_POINT('Ctrl Pts',(204.401822058383,10.7834006594968,30.6586157761273));
#75421=CARTESIAN_POINT('Ctrl Pts',(204.404990878414,10.7375644207131,30.6481387674076));
#75422=CARTESIAN_POINT('Ctrl Pts',(204.40816288483,10.6916820916273,30.6376512236068));
#75423=CARTESIAN_POINT('Ctrl Pts',(204.411334891245,10.6464513199307,30.624414119431));
#75424=CARTESIAN_POINT('Ctrl Pts',(204.414506897661,10.6022160361884,30.6085409242037));
#75425=CARTESIAN_POINT('Ctrl Pts',(204.41768084898,10.5579536297547,30.5926579963887));
#75426=CARTESIAN_POINT('Ctrl Pts',(204.420854800299,10.5146884378187,30.5741359803831));
#75427=CARTESIAN_POINT('Ctrl Pts',(204.424028751618,10.4727436766404,30.5531361887132));
#75428=CARTESIAN_POINT('Ctrl Pts',(204.427208317625,10.4307247155982,30.5320992486213));
#75429=CARTESIAN_POINT('Ctrl Pts',(204.430387883632,10.3900313241586,30.5085760712266));
#75430=CARTESIAN_POINT('Ctrl Pts',(204.433567449639,10.3509597229013,30.482772497175));
#75431=CARTESIAN_POINT('Ctrl Pts',(204.434299182942,10.3419679322715,30.4768341601756));
#75432=CARTESIAN_POINT('Ctrl Pts',(204.435030916245,10.3330618999511,30.4707752177292));
#75433=CARTESIAN_POINT('Ctrl Pts',(204.435762649547,10.324244983437,30.4645984760977));
#75434=CARTESIAN_POINT('Ctrl Pts',(204.438927171542,10.2861145250704,30.4378859639348));
#75435=CARTESIAN_POINT('Ctrl Pts',(204.442091693537,10.2494829341546,30.4088476656972));
#75436=CARTESIAN_POINT('Ctrl Pts',(204.445256215531,10.2146494857929,30.3776785472681));
#75437=CARTESIAN_POINT('Ctrl Pts',(204.448415347126,10.1798753722143,30.3465625218564));
#75438=CARTESIAN_POINT('Ctrl Pts',(204.45157447872,10.1468937495134,30.3133232391173));
#75439=CARTESIAN_POINT('Ctrl Pts',(204.454733610315,10.1159730560568,30.2781975487513));
#75440=CARTESIAN_POINT('Ctrl Pts',(204.455187657379,10.111528970814,30.2731490991613));
#75441=CARTESIAN_POINT('Ctrl Pts',(204.455641704444,10.1071274017728,30.2680617496528));
#75442=CARTESIAN_POINT('Ctrl Pts',(204.456095751509,10.1027690874833,30.2629362700282));
#75443=CARTESIAN_POINT('Origin',(201.825,11.,29.5));
#75444=CARTESIAN_POINT('',(198.847155100818,9.5357120419226,29.5003329957075));
#75445=CARTESIAN_POINT('',(198.6865,11.6340070945751,30.8190402776369));
#75446=CARTESIAN_POINT('Ctrl Pts',(198.847155045843,9.5340043049682,29.5003343903779));
#75447=CARTESIAN_POINT('Ctrl Pts',(198.846037963051,9.53394303232492,29.5207934613441));
#75448=CARTESIAN_POINT('Ctrl Pts',(198.84492088026,9.53434377109394,29.541249874511));
#75449=CARTESIAN_POINT('Ctrl Pts',(198.81758649789,9.55565955034218,30.041323968822));
#75450=CARTESIAN_POINT('Ctrl Pts',(198.765151898734,10.1147327781393,30.9788657994748));
#75451=CARTESIAN_POINT('Ctrl Pts',(198.712717299578,11.1994409611895,31.0279179110948));
#75452=CARTESIAN_POINT('Ctrl Pts',(198.6865,11.6340070945751,30.8190402776369));
#75453=CARTESIAN_POINT('',(198.6865,10.3659929054241,30.8190402776365));
#75454=CARTESIAN_POINT('Origin',(198.6865,11.,29.5));
#75455=CARTESIAN_POINT('',(198.775844954157,9.53646362701638,29.5011978292248));
#75456=CARTESIAN_POINT('Ctrl Pts',(198.6865,10.3659929054241,30.8190402776365));
#75457=CARTESIAN_POINT('Ctrl Pts',(198.712748879998,9.93090330924719,30.6099110376662));
#75458=CARTESIAN_POINT('Ctrl Pts',(198.742530531383,9.56801055501681,30.1110552949604));
#75459=CARTESIAN_POINT('Ctrl Pts',(198.772312182769,9.53498328393008,29.5659452088545));
#75460=CARTESIAN_POINT('Ctrl Pts',(198.775844954157,9.53549762207678,29.5011986198501));
#75461=CARTESIAN_POINT('',(199.275844954108,9.5365000054828,29.5001266813354));
#75462=CARTESIAN_POINT('Ctrl Pts',(198.775844954157,9.53650049016837,29.5011977990542));
#75463=CARTESIAN_POINT('Ctrl Pts',(198.778791649872,9.53645632016616,29.4472298347593));
#75464=CARTESIAN_POINT('Ctrl Pts',(198.781738345587,9.53940154252127,29.3931370361555));
#75465=CARTESIAN_POINT('Ctrl Pts',(198.784685041302,9.54535112027514,29.3392863206967));
#75466=CARTESIAN_POINT('Ctrl Pts',(198.787628183599,9.55129352343638,29.2855005437868));
#75467=CARTESIAN_POINT('Ctrl Pts',(198.790571325895,9.56023305821482,29.2319568159945));
#75468=CARTESIAN_POINT('Ctrl Pts',(198.793514468191,9.57213268319622,29.1790215340501));
#75469=CARTESIAN_POINT('Ctrl Pts',(198.796455329146,9.58402308432575,29.1261272842558));
#75470=CARTESIAN_POINT('Ctrl Pts',(198.799396190101,9.59886891553508,29.0738410828827));
#75471=CARTESIAN_POINT('Ctrl Pts',(198.802337051055,9.6165817291683,29.0225210602246));
#75472=CARTESIAN_POINT('Ctrl Pts',(198.805276898398,9.63428843781035,28.9712187257945));
#75473=CARTESIAN_POINT('Ctrl Pts',(198.80821674574,9.65485999115351,28.920882430529));
#75474=CARTESIAN_POINT('Ctrl Pts',(198.811156593082,9.67815831354728,28.8718544707189));
#75475=CARTESIAN_POINT('Ctrl Pts',(198.814098759117,9.70147501160776,28.822787841968));
#75476=CARTESIAN_POINT('Ctrl Pts',(198.817040925152,9.72752254036119,28.7750321098689));
#75477=CARTESIAN_POINT('Ctrl Pts',(198.819983091187,9.75611570679522,28.7289071942247));
#75478=CARTESIAN_POINT('Ctrl Pts',(198.822926399207,9.78471997149858,28.6827643754658));
#75479=CARTESIAN_POINT('Ctrl Pts',(198.825869707226,9.81587152468746,28.6382540854398));
#75480=CARTESIAN_POINT('Ctrl Pts',(198.828813015246,9.8493424183292,28.5956663338438));
#75481=CARTESIAN_POINT('Ctrl Pts',(198.831761738694,9.88287489548651,28.5530002245113));
#75482=CARTESIAN_POINT('Ctrl Pts',(198.834710462143,9.91873486644139,28.5122641281858));
#75483=CARTESIAN_POINT('Ctrl Pts',(198.837659185592,9.95665580113758,28.4737129384523));
#75484=CARTESIAN_POINT('Ctrl Pts',(198.83977055039,9.98380820386801,28.4461092562708));
#75485=CARTESIAN_POINT('Ctrl Pts',(198.841881915188,10.0120164483374,28.4196249997495));
#75486=CARTESIAN_POINT('Ctrl Pts',(198.843993279985,10.041172772022,28.3943406506125));
#75487=CARTESIAN_POINT('Ctrl Pts',(198.847005328754,10.0827668484904,28.3582702885587));
#75488=CARTESIAN_POINT('Ctrl Pts',(198.850017377523,10.1264862950172,28.3244747310288));
#75489=CARTESIAN_POINT('Ctrl Pts',(198.853029426292,10.1720526307868,28.2932127760815));
#75490=CARTESIAN_POINT('Ctrl Pts',(198.856036078144,10.2175373218911,28.2620068355537));
#75491=CARTESIAN_POINT('Ctrl Pts',(198.859042729996,10.2648619033235,28.2333257839958));
#75492=CARTESIAN_POINT('Ctrl Pts',(198.862049381848,10.3137146782264,28.2073884159895));
#75493=CARTESIAN_POINT('Ctrl Pts',(198.865053031751,10.3625186767598,28.1814769447853));
#75494=CARTESIAN_POINT('Ctrl Pts',(198.868056681654,10.4128473825597,28.1583039762517));
#75495=CARTESIAN_POINT('Ctrl Pts',(198.871060331557,10.4643615234754,28.1380441738197));
#75496=CARTESIAN_POINT('Ctrl Pts',(198.874062164677,10.51584450563,28.1177966256995));
#75497=CARTESIAN_POINT('Ctrl Pts',(198.877063997796,10.5685110118662,28.100458943567));
#75498=CARTESIAN_POINT('Ctrl Pts',(198.880065830916,10.6220007529088,28.08615813501));
#75499=CARTESIAN_POINT('Ctrl Pts',(198.883067029728,10.6754791911956,28.0718603483136));
#75500=CARTESIAN_POINT('Ctrl Pts',(198.886068228539,10.7297800096696,28.0605982969217));
#75501=CARTESIAN_POINT('Ctrl Pts',(198.889069427351,10.7845289073962,28.052448806345));
#75502=CARTESIAN_POINT('Ctrl Pts',(198.892073285715,10.8393263215893,28.0442920939884));
#75503=CARTESIAN_POINT('Ctrl Pts',(198.895077144079,10.8945720856757,28.039253531007));
#75504=CARTESIAN_POINT('Ctrl Pts',(198.898081002443,10.9498843807075,28.0373583232032));
#75505=CARTESIAN_POINT('Ctrl Pts',(198.901086191942,11.0052211869347,28.0354622755534));
#75506=CARTESIAN_POINT('Ctrl Pts',(198.904091381442,11.0606240547654,28.0367123485731));
#75507=CARTESIAN_POINT('Ctrl Pts',(198.907096570941,11.1157120452941,28.0410815743936));
#75508=CARTESIAN_POINT('Ctrl Pts',(198.91010727564,11.1709011346923,28.0454588187275));
#75509=CARTESIAN_POINT('Ctrl Pts',(198.913117980339,11.2257736687237,28.0529665793148));
#75510=CARTESIAN_POINT('Ctrl Pts',(198.916128685038,11.2799559003873,28.0635262119209));
#75511=CARTESIAN_POINT('Ctrl Pts',(198.918332430018,11.3196156588098,28.0712555443114));
#75512=CARTESIAN_POINT('Ctrl Pts',(198.920536174999,11.3589057330949,28.0806189165104));
#75513=CARTESIAN_POINT('Ctrl Pts',(198.922739919979,11.3976850882574,28.0915686667154));
#75514=CARTESIAN_POINT('Ctrl Pts',(198.925755713335,11.4507540788644,28.1065532426153));
#75515=CARTESIAN_POINT('Ctrl Pts',(198.928771506691,11.5030816332125,28.1245715079638));
#75516=CARTESIAN_POINT('Ctrl Pts',(198.931787300047,11.5542979605813,28.1455310926804));
#75517=CARTESIAN_POINT('Ctrl Pts',(198.934797919014,11.6054264128316,28.1664547157012));
#75518=CARTESIAN_POINT('Ctrl Pts',(198.937808537981,11.6554469393322,28.1903094442393));
#75519=CARTESIAN_POINT('Ctrl Pts',(198.940819156949,11.7040051552978,28.2169532388435));
#75520=CARTESIAN_POINT('Ctrl Pts',(198.943826907058,11.7525170995114,28.2435716442313));
#75521=CARTESIAN_POINT('Ctrl Pts',(198.946834657167,11.7995690352762,28.2729735980771));
#75522=CARTESIAN_POINT('Ctrl Pts',(198.949842407277,11.8448285280044,28.3049698713966));
#75523=CARTESIAN_POINT('Ctrl Pts',(198.952848465744,11.8900625655311,28.3369481491192));
#75524=CARTESIAN_POINT('Ctrl Pts',(198.955854524211,11.9335057300886,28.3715175507233));
#75525=CARTESIAN_POINT('Ctrl Pts',(198.958860582677,11.9748540492909,28.4084452223635));
#75526=CARTESIAN_POINT('Ctrl Pts',(198.961866124186,12.0161952577378,28.445366543476));
#75527=CARTESIAN_POINT('Ctrl Pts',(198.964871665695,12.0554419447302,28.4846449787968));
#75528=CARTESIAN_POINT('Ctrl Pts',(198.967877207204,12.0923245227013,28.5260085282174));
#75529=CARTESIAN_POINT('Ctrl Pts',(198.970885554931,12.1292415372513,28.5674106980167));
#75530=CARTESIAN_POINT('Ctrl Pts',(198.973893902658,12.1637896829338,28.6109014775952));
#75531=CARTESIAN_POINT('Ctrl Pts',(198.976902250385,12.1957384829353,28.6561743483232));
#75532=CARTESIAN_POINT('Ctrl Pts',(198.979912017522,12.22770235714,28.7014685798678));
#75533=CARTESIAN_POINT('Ctrl Pts',(198.982921784659,12.257064162318,28.7485461318182));
#75534=CARTESIAN_POINT('Ctrl Pts',(198.985931551796,12.2836375865475,28.7970726947953));
#75535=CARTESIAN_POINT('Ctrl Pts',(198.988946921717,12.3102604781084,28.8456895916167));
#75536=CARTESIAN_POINT('Ctrl Pts',(198.991962291638,12.3340843938176,28.8957604118083));
#75537=CARTESIAN_POINT('Ctrl Pts',(198.994977661559,12.3549702085235,28.9469285904932));
#75538=CARTESIAN_POINT('Ctrl Pts',(198.997147294363,12.3699980657755,28.9837453532556));
#75539=CARTESIAN_POINT('Ctrl Pts',(198.999316927167,12.3835058329917,29.0211297861003));
#75540=CARTESIAN_POINT('Ctrl Pts',(199.001486559972,12.3954578171697,29.0589447534605));
#75541=CARTESIAN_POINT('Ctrl Pts',(199.004495371137,12.4120326326725,29.1113859295786));
#75542=CARTESIAN_POINT('Ctrl Pts',(199.007504182302,12.4256822793691,29.1648736097929));
#75543=CARTESIAN_POINT('Ctrl Pts',(199.010512993467,12.4362797294248,29.2190502022719));
#75544=CARTESIAN_POINT('Ctrl Pts',(199.013516438647,12.4468582797364,29.2731301749294));
#75545=CARTESIAN_POINT('Ctrl Pts',(199.016519883827,12.4543953348941,29.3278961071117));
#75546=CARTESIAN_POINT('Ctrl Pts',(199.019523329007,12.4588137565104,29.382975755435));
#75547=CARTESIAN_POINT('Ctrl Pts',(199.022523793782,12.4632277936006,29.4380007466478));
#75548=CARTESIAN_POINT('Ctrl Pts',(199.025524258558,12.4645292853747,29.4933383129887));
#75549=CARTESIAN_POINT('Ctrl Pts',(199.028524723333,12.4626925424559,29.5486083968457));
#75550=CARTESIAN_POINT('Ctrl Pts',(199.031523398684,12.4608568949383,29.6038455185937));
#75551=CARTESIAN_POINT('Ctrl Pts',(199.034522074035,12.4558867397765,29.6590147103353));
#75552=CARTESIAN_POINT('Ctrl Pts',(199.037520749386,12.4478084716962,29.7137355358491));
#75553=CARTESIAN_POINT('Ctrl Pts',(199.040518823625,12.4397318229771,29.7684453920833));
#75554=CARTESIAN_POINT('Ctrl Pts',(199.043516897864,12.4285483758565,29.822706537908));
#75555=CARTESIAN_POINT('Ctrl Pts',(199.046514972104,12.4143361450525,29.8761456085057));
#75556=CARTESIAN_POINT('Ctrl Pts',(199.049515782481,12.4001109437173,29.9296334492888));
#75557=CARTESIAN_POINT('Ctrl Pts',(199.052516592857,12.3828515726585,29.9822972040417));
#75558=CARTESIAN_POINT('Ctrl Pts',(199.055517403234,12.3626864066177,30.0337771138024));
#75559=CARTESIAN_POINT('Ctrl Pts',(199.058519582831,12.3425120395483,30.0852805129867));
#75560=CARTESIAN_POINT('Ctrl Pts',(199.061521762427,12.3194294554494,30.1355985091639));
#75561=CARTESIAN_POINT('Ctrl Pts',(199.064523942024,12.2936145477954,30.1843929074238));
#75562=CARTESIAN_POINT('Ctrl Pts',(199.067531736411,12.2677513601204,30.2332785628213));
#75563=CARTESIAN_POINT('Ctrl Pts',(199.070539530797,12.2391459153857,30.2806344749031));
#75564=CARTESIAN_POINT('Ctrl Pts',(199.073547325184,12.2080186595901,30.3261496039351));
#75565=CARTESIAN_POINT('Ctrl Pts',(199.075775950111,12.1849549227622,30.3598740338873));
#75566=CARTESIAN_POINT('Ctrl Pts',(199.078004575038,12.1605076313727,30.3925884404986));
#75567=CARTESIAN_POINT('Ctrl Pts',(199.080233199965,12.1347802346372,30.4241785915486));
#75568=CARTESIAN_POINT('Ctrl Pts',(199.083244840677,12.1000136507694,30.4668677779892));
#75569=CARTESIAN_POINT('Ctrl Pts',(199.086256481389,12.0627625870014,30.5076811369861));
#75570=CARTESIAN_POINT('Ctrl Pts',(199.089268122101,12.0232570704895,30.5463160219041));
#75571=CARTESIAN_POINT('Ctrl Pts',(199.09227444723,11.9838212817127,30.5848827157628));
#75572=CARTESIAN_POINT('Ctrl Pts',(199.095280772358,11.9421393112584,30.6212782004769));
#75573=CARTESIAN_POINT('Ctrl Pts',(199.098287097487,11.898480765214,30.6552335541095));
#75574=CARTESIAN_POINT('Ctrl Pts',(199.101290470819,11.8548650858309,30.6891555682754));
#75575=CARTESIAN_POINT('Ctrl Pts',(199.104293844151,11.8092770899249,30.7206418754746));
#75576=CARTESIAN_POINT('Ctrl Pts',(199.107297217484,11.7620211020091,30.7494623203974));
#75577=CARTESIAN_POINT('Ctrl Pts',(199.110298824626,11.7147929038641,30.7782658169165));
#75578=CARTESIAN_POINT('Ctrl Pts',(199.113300431768,11.6658991074839,30.8044062845581));
#75579=CARTESIAN_POINT('Ctrl Pts',(199.116302038911,11.6156728951277,30.8276969293499));
#75580=CARTESIAN_POINT('Ctrl Pts',(199.119303062839,11.5654564417592,30.8509830487533));
#75581=CARTESIAN_POINT('Ctrl Pts',(199.122304086767,11.5139085648906,30.8714202233517));
#75582=CARTESIAN_POINT('Ctrl Pts',(199.125305110695,11.461384832269,30.8888687074566));
#75583=CARTESIAN_POINT('Ctrl Pts',(199.128308874831,11.4088131406859,30.9063331236198));
#75584=CARTESIAN_POINT('Ctrl Pts',(199.131312638968,11.3552643148979,30.9208032309239));
#75585=CARTESIAN_POINT('Ctrl Pts',(199.134316403105,11.3011101646474,30.9321888558238));
#75586=CARTESIAN_POINT('Ctrl Pts',(199.137321543191,11.2469312077315,30.9435796961945));
#75587=CARTESIAN_POINT('Ctrl Pts',(199.140326683277,11.1921468959952,30.9518831584158));
#75588=CARTESIAN_POINT('Ctrl Pts',(199.143331823363,11.1371370863662,30.9570606265846));
#75589=CARTESIAN_POINT('Ctrl Pts',(199.146342552568,11.0820249665871,30.9622477240821));
#75590=CARTESIAN_POINT('Ctrl Pts',(199.149353281772,11.0266870394626,30.9642971944789));
#75591=CARTESIAN_POINT('Ctrl Pts',(199.152364010976,10.9715049136464,30.9632225668208));
#75592=CARTESIAN_POINT('Ctrl Pts',(199.154569287303,10.9310855243646,30.9624354316207));
#75593=CARTESIAN_POINT('Ctrl Pts',(199.15677456363,10.8907497479876,30.9599732718661));
#75594=CARTESIAN_POINT('Ctrl Pts',(199.158979839957,10.8506449528868,30.9558589629156));
#75595=CARTESIAN_POINT('Ctrl Pts',(199.161991606742,10.7958734540428,30.9502400121802));
#75596=CARTESIAN_POINT('Ctrl Pts',(199.165003373527,10.7413059434149,30.9415142471686));
#75597=CARTESIAN_POINT('Ctrl Pts',(199.168015140312,10.6873216990735,30.9297078478241));
#75598=CARTESIAN_POINT('Ctrl Pts',(199.171021608774,10.6334324242169,30.9179222183852));
#75599=CARTESIAN_POINT('Ctrl Pts',(199.174028077236,10.5801248904549,30.90306682183));
#75600=CARTESIAN_POINT('Ctrl Pts',(199.177034545698,10.5277719071787,30.885219433285));
#75601=CARTESIAN_POINT('Ctrl Pts',(199.180038072841,10.4754701424236,30.8673895053848));
#75602=CARTESIAN_POINT('Ctrl Pts',(199.183041599983,10.4241215749087,30.8465735537857));
#75603=CARTESIAN_POINT('Ctrl Pts',(199.186045127125,10.3740856613946,30.8228996525543));
#75604=CARTESIAN_POINT('Ctrl Pts',(199.189046898269,10.3240790011582,30.7992395921655));
#75605=CARTESIAN_POINT('Ctrl Pts',(199.192048669412,10.2753839495258,30.772725119322));
#75606=CARTESIAN_POINT('Ctrl Pts',(199.195050440555,10.2283395540161,30.7435322296201));
#75607=CARTESIAN_POINT('Ctrl Pts',(199.198051638403,10.1813041433144,30.7143449153434));
#75608=CARTESIAN_POINT('Ctrl Pts',(199.201052836251,10.1359192104467,30.6824804782212));
#75609=CARTESIAN_POINT('Ctrl Pts',(199.204054034099,10.0924967602004,30.6481594487497));
#75610=CARTESIAN_POINT('Ctrl Pts',(199.207057986182,10.0490344606516,30.6138069224585));
#75611=CARTESIAN_POINT('Ctrl Pts',(199.210061938265,10.007538656223,30.5769936278358));
#75612=CARTESIAN_POINT('Ctrl Pts',(199.213065890349,9.96828882932279,30.5379808814713));
#75613=CARTESIAN_POINT('Ctrl Pts',(199.216071226479,9.92902091837477,30.4989501602919));
#75614=CARTESIAN_POINT('Ctrl Pts',(199.219076562609,9.89200140066081,30.4577183604341));
#75615=CARTESIAN_POINT('Ctrl Pts',(199.22208189874,9.85747107758766,30.4145818232675));
#75616=CARTESIAN_POINT('Ctrl Pts',(199.225092834847,9.82287641261668,30.3713649078588));
#75617=CARTESIAN_POINT('Ctrl Pts',(199.228103770955,9.79078051364795,30.3262365963112));
#75618=CARTESIAN_POINT('Ctrl Pts',(199.231114707063,9.76138155605344,30.2795233160819));
#75619=CARTESIAN_POINT('Ctrl Pts',(199.233318631359,9.73986230935198,30.245330450629));
#75620=CARTESIAN_POINT('Ctrl Pts',(199.235522555654,9.71978713192138,30.2102890081123));
#75621=CARTESIAN_POINT('Ctrl Pts',(199.23772647995,9.70121767855363,30.1745344553827));
#75622=CARTESIAN_POINT('Ctrl Pts',(199.240908966812,9.67440321786568,30.1229045538666));
#75623=CARTESIAN_POINT('Ctrl Pts',(199.244091453674,9.65062931503385,30.0695931020557));
#75624=CARTESIAN_POINT('Ctrl Pts',(199.247273940537,9.63009563156702,30.0149701654933));
#75625=CARTESIAN_POINT('Ctrl Pts',(199.250449576398,9.60960615135481,29.9604648167753));
#75626=CARTESIAN_POINT('Ctrl Pts',(199.25362521226,9.59234318165365,29.9046539981085));
#75627=CARTESIAN_POINT('Ctrl Pts',(199.256800848122,9.578459727853,29.8479303158166));
#75628=CARTESIAN_POINT('Ctrl Pts',(199.259974865786,9.56458334859381,29.7912355380068));
#75629=CARTESIAN_POINT('Ctrl Pts',(199.26314888345,9.5540832325529,29.7336292250163));
#75630=CARTESIAN_POINT('Ctrl Pts',(199.266322901115,9.547063630942,29.6755225269547));
#75631=CARTESIAN_POINT('Ctrl Pts',(199.269496918779,9.5400440293311,29.617415828893));
#75632=CARTESIAN_POINT('Ctrl Pts',(199.272670936444,9.53650508507005,29.5588091690068));
#75633=CARTESIAN_POINT('Ctrl Pts',(199.275844954108,9.5365000054828,29.5001266813354));
#75634=CARTESIAN_POINT('',(199.775844954107,9.53650044565997,29.49885787631));
#75635=CARTESIAN_POINT('Ctrl Pts',(199.275844954157,9.53650000548272,29.5001266804286));
#75636=CARTESIAN_POINT('Ctrl Pts',(199.278966002871,9.5364950107009,29.4424235035644));
#75637=CARTESIAN_POINT('Ctrl Pts',(199.282087051584,9.53990702549526,29.3847749920601));
#75638=CARTESIAN_POINT('Ctrl Pts',(199.285208100298,9.5466909013332,29.3275908536872));
#75639=CARTESIAN_POINT('Ctrl Pts',(199.288336991433,9.5534918233685,29.2702630257582));
#75640=CARTESIAN_POINT('Ctrl Pts',(199.291465882567,9.56368146852732,29.2134023618349));
#75641=CARTESIAN_POINT('Ctrl Pts',(199.294594773702,9.5771632283295,29.1574101998274));
#75642=CARTESIAN_POINT('Ctrl Pts',(199.297727987064,9.59066361173449,29.1013406906634));
#75643=CARTESIAN_POINT('Ctrl Pts',(199.300861200426,9.60746503472237,29.0461425161852));
#75644=CARTESIAN_POINT('Ctrl Pts',(199.303994413788,9.62742142305117,28.9922005316061));
#75645=CARTESIAN_POINT('Ctrl Pts',(199.30713558909,9.64742852339869,28.9381214727786));
#75646=CARTESIAN_POINT('Ctrl Pts',(199.310276764392,9.67060641654856,28.8853054040128));
#75647=CARTESIAN_POINT('Ctrl Pts',(199.313417939694,9.6967616592254,28.8341155677334));
#75648=CARTESIAN_POINT('Ctrl Pts',(199.31443633311,9.70524139192979,28.8175194254534));
#75649=CARTESIAN_POINT('Ctrl Pts',(199.315454726526,9.71403372900158,28.8010940000388));
#75650=CARTESIAN_POINT('Ctrl Pts',(199.316473119942,9.72313110523733,28.7848510116154));
#75651=CARTESIAN_POINT('Ctrl Pts',(199.319484515685,9.75003210403694,28.7368203925931));
#75652=CARTESIAN_POINT('Ctrl Pts',(199.322495911428,9.77970288332518,28.6902098620291));
#75653=CARTESIAN_POINT('Ctrl Pts',(199.32550730717,9.81196895974587,28.6453570936393));
#75654=CARTESIAN_POINT('Ctrl Pts',(199.32851339067,9.84417811730354,28.6005834476239));
#75655=CARTESIAN_POINT('Ctrl Pts',(199.331519474171,9.87897318052574,28.557561834934));
#75656=CARTESIAN_POINT('Ctrl Pts',(199.334525557671,9.91613487312491,28.5166035200673));
#75657=CARTESIAN_POINT('Ctrl Pts',(199.337528691627,9.95326010298587,28.4756853931524));
#75658=CARTESIAN_POINT('Ctrl Pts',(199.340531825584,9.99274700919291,28.4368269422737));
#75659=CARTESIAN_POINT('Ctrl Pts',(199.34353495954,10.0343354438467,28.4003072179062));
#75660=CARTESIAN_POINT('Ctrl Pts',(199.34653633001,10.0758994571236,28.3638089384898));
#75661=CARTESIAN_POINT('Ctrl Pts',(199.349537700479,10.1195621570822,28.3296470108104));
#75662=CARTESIAN_POINT('Ctrl Pts',(199.352539070949,10.1650275077834,28.2980627357297));
#75663=CARTESIAN_POINT('Ctrl Pts',(199.355539861361,10.210484071654,28.2664845647628));
#75664=CARTESIAN_POINT('Ctrl Pts',(199.358540651772,10.2577421612415,28.2374833577421));
#75665=CARTESIAN_POINT('Ctrl Pts',(199.361541442184,10.3064755950602,28.2112579196159));
#75666=CARTESIAN_POINT('Ctrl Pts',(199.364544979613,10.3552536409925,28.1850084739011));
#75667=CARTESIAN_POINT('Ctrl Pts',(199.367548517043,10.4055092636874,28.1615401238871));
#75668=CARTESIAN_POINT('Ctrl Pts',(199.370552054472,10.4568917539653,28.1410056353726));
#75669=CARTESIAN_POINT('Ctrl Pts',(199.373556971309,10.5082978422191,28.1204617161675));
#75670=CARTESIAN_POINT('Ctrl Pts',(199.376561888146,10.5608313286254,28.1028545122959));
#75671=CARTESIAN_POINT('Ctrl Pts',(199.379566804983,10.6141247099964,28.0882873838615));
#75672=CARTESIAN_POINT('Ctrl Pts',(199.382577319389,10.6675173664533,28.0736931197323));
#75673=CARTESIAN_POINT('Ctrl Pts',(199.385587833795,10.7216722283061,28.0621503534102));
#75674=CARTESIAN_POINT('Ctrl Pts',(199.388598348201,10.7762110987655,28.0537113781529));
#75675=CARTESIAN_POINT('Ctrl Pts',(199.390805485446,10.8161958841069,28.0475244034077));
#75676=CARTESIAN_POINT('Ctrl Pts',(199.393012622691,10.8563868605222,28.0430046284988));
#75677=CARTESIAN_POINT('Ctrl Pts',(199.395219759936,10.8966345341256,28.0401548607936));
#75678=CARTESIAN_POINT('Ctrl Pts',(199.398231136404,10.9515477016101,28.0362666914342));
#75679=CARTESIAN_POINT('Ctrl Pts',(199.401242512873,11.0067947442693,28.0354731412825));
#75680=CARTESIAN_POINT('Ctrl Pts',(199.404253889341,11.0619976415287,28.0378137798335));
#75681=CARTESIAN_POINT('Ctrl Pts',(199.407259954687,11.1171031782137,28.0401502902331));
#75682=CARTESIAN_POINT('Ctrl Pts',(199.410266020033,11.1721642010943,28.0456099969915));
#75683=CARTESIAN_POINT('Ctrl Pts',(199.413272085379,11.2268001683379,28.0541805321404));
#75684=CARTESIAN_POINT('Ctrl Pts',(199.416275201884,11.2813825396793,28.0627426599051));
#75685=CARTESIAN_POINT('Ctrl Pts',(199.419278318388,11.3355401627154,28.0744094892951));
#75686=CARTESIAN_POINT('Ctrl Pts',(199.422281434893,11.3888969792225,28.0891168051353));
#75687=CARTESIAN_POINT('Ctrl Pts',(199.425282788647,11.4422224766638,28.103815488163));
#75688=CARTESIAN_POINT('Ctrl Pts',(199.4282841424,11.4947475916853,28.1215509801459));
#75689=CARTESIAN_POINT('Ctrl Pts',(199.431285496154,11.5461081125882,28.14220834464));
#75690=CARTESIAN_POINT('Ctrl Pts',(199.434286270619,11.5974587204478,28.1628617220766));
#75691=CARTESIAN_POINT('Ctrl Pts',(199.437287045084,11.6476446914489,28.1864356551269));
#75692=CARTESIAN_POINT('Ctrl Pts',(199.440287819549,11.6963207803285,28.2127666797031));
#75693=CARTESIAN_POINT('Ctrl Pts',(199.443291342359,11.7450414505932,28.2391218202995));
#75694=CARTESIAN_POINT('Ctrl Pts',(199.446294865169,11.7922490111345,28.2682388454497));
#75695=CARTESIAN_POINT('Ctrl Pts',(199.449298387979,11.8376232289154,28.2999085133285));
#75696=CARTESIAN_POINT('Ctrl Pts',(199.452303290915,11.8830182962553,28.3315927334937));
#75697=CARTESIAN_POINT('Ctrl Pts',(199.455308193851,11.9265779260924,28.3658316079328));
#75698=CARTESIAN_POINT('Ctrl Pts',(199.458313096787,11.968013957783,28.4023747326445));
#75699=CARTESIAN_POINT('Ctrl Pts',(199.461323598643,12.009527195645,28.4389859467613));
#75700=CARTESIAN_POINT('Ctrl Pts',(199.464334100499,12.048908555423,28.4779096156836));
#75701=CARTESIAN_POINT('Ctrl Pts',(199.467344602356,12.0859066865429,28.5188583598066));
#75702=CARTESIAN_POINT('Ctrl Pts',(199.469551868213,12.1130332971587,28.548881515123));
#75703=CARTESIAN_POINT('Ctrl Pts',(199.471759134071,12.138879554346,28.5799925085115));
#75704=CARTESIAN_POINT('Ctrl Pts',(199.473966399929,12.1633610186832,28.6120679135157));
#75705=CARTESIAN_POINT('Ctrl Pts',(199.476977703779,12.1967603156363,28.6558273864732));
#75706=CARTESIAN_POINT('Ctrl Pts',(199.47998900763,12.22775667217,28.7015649777552));
#75707=CARTESIAN_POINT('Ctrl Pts',(199.483000311481,12.2561094566838,28.7489864962403));
#75708=CARTESIAN_POINT('Ctrl Pts',(199.486006301957,12.284412213379,28.796324340576));
#75709=CARTESIAN_POINT('Ctrl Pts',(199.489012292434,12.310080386523,28.8453397662176));
#75710=CARTESIAN_POINT('Ctrl Pts',(199.49201828291,12.3329153668911,28.8957079557816));
#75711=CARTESIAN_POINT('Ctrl Pts',(199.495021323225,12.3557279363834,28.9460267126237));
#75712=CARTESIAN_POINT('Ctrl Pts',(199.49802436354,12.3757126047435,28.9976951250544));
#75713=CARTESIAN_POINT('Ctrl Pts',(199.501027403855,12.392716556171,29.0503636534184));
#75714=CARTESIAN_POINT('Ctrl Pts',(199.50402868024,12.4097105197968,29.103001245278));
#75715=CARTESIAN_POINT('Ctrl Pts',(199.507029956626,12.4237270751371,29.1566372875299));
#75716=CARTESIAN_POINT('Ctrl Pts',(199.510031233011,12.4346623019812,29.2109042904607));
#75717=CARTESIAN_POINT('Ctrl Pts',(199.513031929071,12.4455954143938,29.2651608003435));
#75718=CARTESIAN_POINT('Ctrl Pts',(199.51603262513,12.453448277553,29.3200475116519));
#75719=CARTESIAN_POINT('Ctrl Pts',(199.51903332119,12.4581679431271,29.3751861400463));
#75720=CARTESIAN_POINT('Ctrl Pts',(199.522036764616,12.4628919299148,29.4303752520582));
#75721=CARTESIAN_POINT('Ctrl Pts',(199.525040208041,12.4644769431849,29.4858162151371));
#75722=CARTESIAN_POINT('Ctrl Pts',(199.528043651467,12.4629220279571,29.5411265135622));
#75723=CARTESIAN_POINT('Ctrl Pts',(199.531048474355,12.461366398567,29.5964622156431));
#75724=CARTESIAN_POINT('Ctrl Pts',(199.534053297242,12.4566680107546,29.6516666068551));
#75725=CARTESIAN_POINT('Ctrl Pts',(199.537058120129,12.4488779219585,29.7063613754104));
#75726=CARTESIAN_POINT('Ctrl Pts',(199.540068541841,12.4410733180506,29.7611580555994));
#75727=CARTESIAN_POINT('Ctrl Pts',(199.543078963553,12.4301656101571,29.8154426979028));
#75728=CARTESIAN_POINT('Ctrl Pts',(199.546089385265,12.416256970448,29.8688474530988));
#75729=CARTESIAN_POINT('Ctrl Pts',(199.548297270151,12.4060561818776,29.9080152385761));
#75730=CARTESIAN_POINT('Ctrl Pts',(199.550505155036,12.3942422832989,29.9467099708587));
#75731=CARTESIAN_POINT('Ctrl Pts',(199.552713039922,12.3808721213668,29.9847931872787));
#75732=CARTESIAN_POINT('Ctrl Pts',(199.555724386742,12.3626364810578,30.0367351039119));
#75733=CARTESIAN_POINT('Ctrl Pts',(199.558735733561,12.3414281238509,30.08775471955));
#75734=CARTESIAN_POINT('Ctrl Pts',(199.561747080381,12.3173608222,30.137489383545));
#75735=CARTESIAN_POINT('Ctrl Pts',(199.564753114759,12.293335978676,30.1871363085526));
#75736=CARTESIAN_POINT('Ctrl Pts',(199.567759149137,12.2664624280492,30.2355023094808));
#75737=CARTESIAN_POINT('Ctrl Pts',(199.570765183515,12.2369026119477,30.2822430431503));
#75738=CARTESIAN_POINT('Ctrl Pts',(199.573768268267,12.2073718009655,30.3289379131867));
#75739=CARTESIAN_POINT('Ctrl Pts',(199.57677135302,12.1751602269147,30.3740102315267));
#75740=CARTESIAN_POINT('Ctrl Pts',(199.579774437772,12.1404761365253,30.4171403556798));
#75741=CARTESIAN_POINT('Ctrl Pts',(199.582775759048,12.1058124133867,30.4602451528876));
#75742=CARTESIAN_POINT('Ctrl Pts',(199.585777080323,12.0686793818517,30.501409606242));
#75743=CARTESIAN_POINT('Ctrl Pts',(199.588778401599,12.029327136875,30.540345084716));
#75744=CARTESIAN_POINT('Ctrl Pts',(199.59177914292,11.9899824960625,30.579273039559));
#75745=CARTESIAN_POINT('Ctrl Pts',(199.59477988424,11.9484198683968,30.6159725041514));
#75746=CARTESIAN_POINT('Ctrl Pts',(199.597780625561,11.9049263567014,30.6501915227244));
#75747=CARTESIAN_POINT('Ctrl Pts',(199.600784114457,11.8613930209423,30.6844418733358));
#75748=CARTESIAN_POINT('Ctrl Pts',(199.603787603353,11.815925684731,30.7162069138282));
#75749=CARTESIAN_POINT('Ctrl Pts',(199.60679109225,11.7688435342395,30.7452758207956));
#75750=CARTESIAN_POINT('Ctrl Pts',(199.609795960792,11.7217397566593,30.7743580805055));
#75751=CARTESIAN_POINT('Ctrl Pts',(199.612800829335,11.6730201508957,30.8007414863127));
#75752=CARTESIAN_POINT('Ctrl Pts',(199.615805697878,11.6230289469955,30.8242609943684));
#75753=CARTESIAN_POINT('Ctrl Pts',(199.618816164981,11.5729446013205,30.8478243231077));
#75754=CARTESIAN_POINT('Ctrl Pts',(199.621826632084,11.5215844154539,30.8685128978839));
#75755=CARTESIAN_POINT('Ctrl Pts',(199.624837099188,11.4693119396476,30.8862101403843));
#75756=CARTESIAN_POINT('Ctrl Pts',(199.627044626097,11.4309813773204,30.8991872425057));
#75757=CARTESIAN_POINT('Ctrl Pts',(199.629252153005,11.3921606682031,30.9105569200359));
#75758=CARTESIAN_POINT('Ctrl Pts',(199.631459679914,11.3529966746977,30.9202906736483));
#75759=CARTESIAN_POINT('Ctrl Pts',(199.634471020875,11.299572121942,30.9335687228673));
#75760=CARTESIAN_POINT('Ctrl Pts',(199.637482361835,11.2452862201099,30.9438558378596));
#75761=CARTESIAN_POINT('Ctrl Pts',(199.640493702795,11.1905045331431,30.9510479912298));
#75762=CARTESIAN_POINT('Ctrl Pts',(199.643499731343,11.1358194884645,30.9582274566709));
#75763=CARTESIAN_POINT('Ctrl Pts',(199.646505759891,11.0806409133706,30.9623227279793));
#75764=CARTESIAN_POINT('Ctrl Pts',(199.64951178844,11.025345793023,30.963280506525));
#75765=CARTESIAN_POINT('Ctrl Pts',(199.652514867386,10.9701049298448,30.9642373452707));
#75766=CARTESIAN_POINT('Ctrl Pts',(199.655517946332,10.9147482729346,30.9620627810189));
#75767=CARTESIAN_POINT('Ctrl Pts',(199.658521025279,10.8596573127426,30.9567553604272));
#75768=CARTESIAN_POINT('Ctrl Pts',(199.661522340783,10.8045987025918,30.9514510564135));
#75769=CARTESIAN_POINT('Ctrl Pts',(199.664523656287,10.7498060040383,30.9430175930706));
#75770=CARTESIAN_POINT('Ctrl Pts',(199.667524971791,10.6956577657883,30.9315055202391));
#75771=CARTESIAN_POINT('Ctrl Pts',(199.670525707385,10.6415199899855,30.9199956717543));
#75772=CARTESIAN_POINT('Ctrl Pts',(199.673526442978,10.5880269429317,30.9054085049404));
#75773=CARTESIAN_POINT('Ctrl Pts',(199.676527178573,10.5355468402103,30.8878456370798));
#75774=CARTESIAN_POINT('Ctrl Pts',(199.679530661859,10.483018682877,30.8702666873756));
#75775=CARTESIAN_POINT('Ctrl Pts',(199.682534145145,10.431505824191,30.8497067610724));
#75776=CARTESIAN_POINT('Ctrl Pts',(199.685537628432,10.3813597175766,30.8263168742661));
#75777=CARTESIAN_POINT('Ctrl Pts',(199.688542491422,10.3311905754607,30.8029162429014));
#75778=CARTESIAN_POINT('Ctrl Pts',(199.691547354411,10.2823899024228,30.776683309883));
#75779=CARTESIAN_POINT('Ctrl Pts',(199.694552217401,10.2352846405451,30.747815158192));
#75780=CARTESIAN_POINT('Ctrl Pts',(199.697562679114,10.1880916111693,30.7188932187638));
#75781=CARTESIAN_POINT('Ctrl Pts',(199.700573140826,10.1426007374354,30.6873265542632));
#75782=CARTESIAN_POINT('Ctrl Pts',(199.703583602539,10.0991090625624,30.6533550055568));
#75783=CARTESIAN_POINT('Ctrl Pts',(199.705791174995,10.0672166046345,30.6284436589363));
#75784=CARTESIAN_POINT('Ctrl Pts',(199.707998747451,10.0363985309859,30.6022400324764));
#75785=CARTESIAN_POINT('Ctrl Pts',(199.710206319907,10.0067593032422,30.5748512307776));
#75786=CARTESIAN_POINT('Ctrl Pts',(199.713172329925,9.96693716911701,30.538052683116));
#75787=CARTESIAN_POINT('Ctrl Pts',(199.716138339944,9.92906818386051,30.4989503247606));
#75788=CARTESIAN_POINT('Ctrl Pts',(199.719104349962,9.89343564648049,30.4577826379299));
#75789=CARTESIAN_POINT('Ctrl Pts',(199.722066214401,9.85785291254795,30.4166724910018));
#75790=CARTESIAN_POINT('Ctrl Pts',(199.72502807884,9.82450079510673,30.3735031346316));
#75791=CARTESIAN_POINT('Ctrl Pts',(199.727989943279,9.79362724051211,30.3285511542238));
#75792=CARTESIAN_POINT('Ctrl Pts',(199.730948918977,9.76278379725795,30.2836430160105));
#75793=CARTESIAN_POINT('Ctrl Pts',(199.733907894675,9.73441443835141,30.2369561423422));
#75794=CARTESIAN_POINT('Ctrl Pts',(199.736866870372,9.70872648068688,30.1887996430899));
#75795=CARTESIAN_POINT('Ctrl Pts',(199.739824209263,9.68305273274946,30.1406697824175));
#75796=CARTESIAN_POINT('Ctrl Pts',(199.742781548153,9.66005770248644,30.0910723869667));
#75797=CARTESIAN_POINT('Ctrl Pts',(199.745738887044,9.63990370325761,30.0403427741607));
#75798=CARTESIAN_POINT('Ctrl Pts',(199.748697257538,9.61974267373835,29.9895954654171));
#75799=CARTESIAN_POINT('Ctrl Pts',(199.751655628033,9.60242486459018,29.9377156537215));
#75800=CARTESIAN_POINT('Ctrl Pts',(199.754613998528,9.58806436995143,29.8850584716629));
#75801=CARTESIAN_POINT('Ctrl Pts',(199.75757296662,9.57370097446109,29.8323906527373));
#75802=CARTESIAN_POINT('Ctrl Pts',(199.760531934712,9.56229620567979,29.7789456819502));
#75803=CARTESIAN_POINT('Ctrl Pts',(199.763490902804,9.55391339084591,29.725090579157));
#75804=CARTESIAN_POINT('Ctrl Pts',(199.766453613072,9.54551997435425,29.6711673663815));
#75805=CARTESIAN_POINT('Ctrl Pts',(199.769416323339,9.54015619498495,29.6168335284714));
#75806=CARTESIAN_POINT('Ctrl Pts',(199.772379033607,9.53783350335657,29.5624610766275));
#75807=CARTESIAN_POINT('Ctrl Pts',(199.77353434044,9.53692777135211,29.5412585763928));
#75808=CARTESIAN_POINT('Ctrl Pts',(199.774689647274,9.5364839070462,29.5200501990782));
#75809=CARTESIAN_POINT('Ctrl Pts',(199.775844954107,9.53650044565997,29.49885787631));
#75810=CARTESIAN_POINT('',(200.275844954197,9.53650048976732,29.5011973089453));
#75811=CARTESIAN_POINT('Ctrl Pts',(199.775844954157,9.53650044566069,29.4988578753877));
#75812=CARTESIAN_POINT('Ctrl Pts',(199.780214289405,9.53656299424463,29.4187091562833));
#75813=CARTESIAN_POINT('Ctrl Pts',(199.784583624652,9.54321187874569,29.3388148236768));
#75814=CARTESIAN_POINT('Ctrl Pts',(199.788952959899,9.55630950416147,29.2600208296008));
#75815=CARTESIAN_POINT('Ctrl Pts',(199.791964298979,9.56533636729763,29.2057161310087));
#75816=CARTESIAN_POINT('Ctrl Pts',(199.79497563806,9.57745028612169,29.1518085046576));
#75817=CARTESIAN_POINT('Ctrl Pts',(199.79798697714,9.59260158197756,29.0986747666195));
#75818=CARTESIAN_POINT('Ctrl Pts',(199.800993003692,9.60772614829929,29.0456347657823));
#75819=CARTESIAN_POINT('Ctrl Pts',(199.803999030244,9.62587731386913,28.9933664471136));
#75820=CARTESIAN_POINT('Ctrl Pts',(199.807005056796,9.64695430672566,28.9422369661659));
#75821=CARTESIAN_POINT('Ctrl Pts',(199.810008133676,9.66801061772365,28.8911576561654));
#75822=CARTESIAN_POINT('Ctrl Pts',(199.813011210556,9.69198686835455,28.8412154555126));
#75823=CARTESIAN_POINT('Ctrl Pts',(199.816014287436,9.71873291471523,28.7927610685448));
#75824=CARTESIAN_POINT('Ctrl Pts',(199.819015600807,9.74546325489223,28.744335135633));
#75825=CARTESIAN_POINT('Ctrl Pts',(199.822016914179,9.77495991228419,28.6973957455857));
#75826=CARTESIAN_POINT('Ctrl Pts',(199.825018227551,9.807026183116,28.6522702540142));
#75827=CARTESIAN_POINT('Ctrl Pts',(199.82801896095,9.83908625747709,28.6071534824708));
#75828=CARTESIAN_POINT('Ctrl Pts',(199.83101969435,9.87371465356943,28.5638503430253));
#75829=CARTESIAN_POINT('Ctrl Pts',(199.834020427749,9.91067190144827,28.5226584303808));
#75830=CARTESIAN_POINT('Ctrl Pts',(199.837023908762,9.94766298912868,28.4814288004757));
#75831=CARTESIAN_POINT('Ctrl Pts',(199.840027389774,9.98698683548436,28.4423146527842));
#75832=CARTESIAN_POINT('Ctrl Pts',(199.843030870787,10.0283652886303,28.4055785831493));
#75833=CARTESIAN_POINT('Ctrl Pts',(199.846035731455,10.06976274906,28.3688256387197));
#75834=CARTESIAN_POINT('Ctrl Pts',(199.849040592124,10.1132162831236,28.3344532777201));
#75835=CARTESIAN_POINT('Ctrl Pts',(199.852045452792,10.1584151919626,28.3026833080255));
#75836=CARTESIAN_POINT('Ctrl Pts',(199.855055912134,10.203698315667,28.2708541443418));
#75837=CARTESIAN_POINT('Ctrl Pts',(199.858066371476,10.2507328609209,28.2416373365857));
#75838=CARTESIAN_POINT('Ctrl Pts',(199.861076830817,10.2991807580831,28.2152102739518));
#75839=CARTESIAN_POINT('Ctrl Pts',(199.863284420509,10.3347079206294,28.1958311346122));
#75840=CARTESIAN_POINT('Ctrl Pts',(199.865492010201,10.3709945293636,28.1779512020213));
#75841=CARTESIAN_POINT('Ctrl Pts',(199.867699599893,10.4079008028976,28.1616238231384));
#75842=CARTESIAN_POINT('Ctrl Pts',(199.87071093792,10.4582440642904,28.1393519049994));
#75843=CARTESIAN_POINT('Ctrl Pts',(199.873722275947,10.5099504315498,28.1198781125562));
#75844=CARTESIAN_POINT('Ctrl Pts',(199.876733613973,10.5626776915904,28.1033678191566));
#75845=CARTESIAN_POINT('Ctrl Pts',(199.879739639464,10.6153119313653,28.0868866528514));
#75846=CARTESIAN_POINT('Ctrl Pts',(199.882745664954,10.6689629901461,28.0733587663774));
#75847=CARTESIAN_POINT('Ctrl Pts',(199.885751690445,10.7232686757375,28.0629015259308));
#75848=CARTESIAN_POINT('Ctrl Pts',(199.88875476626,10.7775210736366,28.0524545466974));
#75849=CARTESIAN_POINT('Ctrl Pts',(199.891757842075,10.8324263102265,28.0450723437012));
#75850=CARTESIAN_POINT('Ctrl Pts',(199.894760917889,10.8876088348908,28.0408219861835));
#75851=CARTESIAN_POINT('Ctrl Pts',(199.897762230194,10.9427589544663,28.0365741246229));
#75852=CARTESIAN_POINT('Ctrl Pts',(199.900763542499,10.9981855143398,28.0354545034967));
#75853=CARTESIAN_POINT('Ctrl Pts',(199.903764854804,11.053506914299,28.0374784582365));
#75854=CARTESIAN_POINT('Ctrl Pts',(199.906765587136,11.108817623979,28.0395020218683));
#75855=CARTESIAN_POINT('Ctrl Pts',(199.909766319469,11.1640226871553,28.0446679355206));
#75856=CARTESIAN_POINT('Ctrl Pts',(199.912767051802,11.2187418961886,28.0529394508688));
#75857=CARTESIAN_POINT('Ctrl Pts',(199.915770531757,11.2735112088979,28.0612185400349));
#75858=CARTESIAN_POINT('Ctrl Pts',(199.918774011712,11.3277932559645,28.0726088326987));
#75859=CARTESIAN_POINT('Ctrl Pts',(199.921777491667,11.3812158426026,28.0870220343725));
#75860=CARTESIAN_POINT('Ctrl Pts',(199.924782351281,11.4346629690946,28.1014418568014));
#75861=CARTESIAN_POINT('Ctrl Pts',(199.927787210895,11.4872493465873,28.1188871898068));
#75862=CARTESIAN_POINT('Ctrl Pts',(199.930792070509,11.5386190000547,28.1392201416908));
#75863=CARTESIAN_POINT('Ctrl Pts',(199.933802528815,11.5900843661098,28.1595909781878));
#75864=CARTESIAN_POINT('Ctrl Pts',(199.936812987122,11.6403279998836,28.1828599585515));
#75865=CARTESIAN_POINT('Ctrl Pts',(199.939823445428,11.6890160226327,28.2088419265809));
#75866=CARTESIAN_POINT('Ctrl Pts',(199.942031043581,11.7247194199613,28.2278947546801));
#75867=CARTESIAN_POINT('Ctrl Pts',(199.944238641733,11.7595867779055,28.248405478792));
#75868=CARTESIAN_POINT('Ctrl Pts',(199.946446239885,11.7934967604058,28.2702865613382));
#75869=CARTESIAN_POINT('Ctrl Pts',(199.949457577301,11.8397526421459,28.3001340779681));
#75870=CARTESIAN_POINT('Ctrl Pts',(199.952468914716,11.8844183203329,28.332657189576));
#75871=CARTESIAN_POINT('Ctrl Pts',(199.955480252132,11.9271676837001,28.3676606796979));
#75872=CARTESIAN_POINT('Ctrl Pts',(199.958486276988,11.9698416292416,28.4026024171548));
#75873=CARTESIAN_POINT('Ctrl Pts',(199.961492301845,12.0106055643059,28.4400155173502));
#75874=CARTESIAN_POINT('Ctrl Pts',(199.964498326701,12.0491625315286,28.4796617068656));
#75875=CARTESIAN_POINT('Ctrl Pts',(199.967501401868,12.0876816643742,28.5192689931945));
#75876=CARTESIAN_POINT('Ctrl Pts',(199.970504477035,12.1239977534923,28.5611046514853));
#75877=CARTESIAN_POINT('Ctrl Pts',(199.973507552202,12.1578485443479,28.6048916275939));
#75878=CARTESIAN_POINT('Ctrl Pts',(199.976508863847,12.191679456702,28.6486528902865));
#75879=CARTESIAN_POINT('Ctrl Pts',(199.979510175491,12.223047618373,28.6943627828438));
#75880=CARTESIAN_POINT('Ctrl Pts',(199.982511487136,12.2517306915302,28.7417107900799));
#75881=CARTESIAN_POINT('Ctrl Pts',(199.985512218797,12.2804082218757,28.7890496476308));
#75882=CARTESIAN_POINT('Ctrl Pts',(199.988512950458,12.3064014211035,28.8380255401038));
#75883=CARTESIAN_POINT('Ctrl Pts',(199.991513682119,12.3295322467552,28.8883005191779));
#75884=CARTESIAN_POINT('Ctrl Pts',(199.99451716139,12.352684252072,28.9386215323728));
#75885=CARTESIAN_POINT('Ctrl Pts',(199.997520640662,12.3729684269442,28.9902435281642));
#75886=CARTESIAN_POINT('Ctrl Pts',(200.000524119933,12.3902542098966,29.0428069533941));
#75887=CARTESIAN_POINT('Ctrl Pts',(200.003528978855,12.4075479330914,29.0953945236882));
#75888=CARTESIAN_POINT('Ctrl Pts',(200.006533837778,12.421840382534,29.14892387486));
#75889=CARTESIAN_POINT('Ctrl Pts',(200.009538696701,12.4330513548999,29.2030217782064));
#75890=CARTESIAN_POINT('Ctrl Pts',(200.012549154312,12.4442832156802,29.2572204773977));
#75891=CARTESIAN_POINT('Ctrl Pts',(200.015559611922,12.4524220529524,29.3119893217723));
#75892=CARTESIAN_POINT('Ctrl Pts',(200.018570069533,12.4574392984579,29.366947599381));
#75893=CARTESIAN_POINT('Ctrl Pts',(200.020777672982,12.4611185027226,29.4072491411602));
#75894=CARTESIAN_POINT('Ctrl Pts',(200.02298527643,12.4631201782027,29.4476524048473));
#75895=CARTESIAN_POINT('Ctrl Pts',(200.025192879879,12.4634508669257,29.4880079153393));
#75896=CARTESIAN_POINT('Ctrl Pts',(200.028204217864,12.4639019513418,29.5430558822733));
#75897=CARTESIAN_POINT('Ctrl Pts',(200.031215555848,12.4612437003182,29.5982438389137));
#75898=CARTESIAN_POINT('Ctrl Pts',(200.034226893833,12.4554602187907,29.6531920413002));
#75899=CARTESIAN_POINT('Ctrl Pts',(200.037232919273,12.4496869403711,29.708043305115));
#75900=CARTESIAN_POINT('Ctrl Pts',(200.040238944713,12.4407994281139,29.7626551335608));
#75901=CARTESIAN_POINT('Ctrl Pts',(200.043244970152,12.428833780463,29.8166485082985));
#75902=CARTESIAN_POINT('Ctrl Pts',(200.046248045911,12.4168798741789,29.8705889016991));
#75903=CARTESIAN_POINT('Ctrl Pts',(200.049251121669,12.4018539297456,29.9239115309983));
#75904=CARTESIAN_POINT('Ctrl Pts',(200.052254197427,12.3838435117912,29.9762450890805));
#75905=CARTESIAN_POINT('Ctrl Pts',(200.05525550967,12.3658436702109,30.0285479149895));
#75906=CARTESIAN_POINT('Ctrl Pts',(200.058256821913,12.3448630004139,30.079862323062));
#75907=CARTESIAN_POINT('Ctrl Pts',(200.061258134156,12.3210389498237,30.1298319958915));
#75908=CARTESIAN_POINT('Ctrl Pts',(200.064258866421,12.2972195030237,30.179792012517));
#75909=CARTESIAN_POINT('Ctrl Pts',(200.067259598686,12.2705579937173,30.2284073340654));
#75910=CARTESIAN_POINT('Ctrl Pts',(200.070260330952,12.2412391182358,30.2753436021282));
#75911=CARTESIAN_POINT('Ctrl Pts',(200.073263810832,12.2118933969847,30.3223228472909));
#75912=CARTESIAN_POINT('Ctrl Pts',(200.076267290711,12.1798857287696,30.3676195192098));
#75913=CARTESIAN_POINT('Ctrl Pts',(200.079270770591,12.1454449367162,30.4109270810286));
#75914=CARTESIAN_POINT('Ctrl Pts',(200.082275630126,12.1109883242143,30.4542545362648));
#75915=CARTESIAN_POINT('Ctrl Pts',(200.08528048966,12.0740967118477,30.495590665767));
#75916=CARTESIAN_POINT('Ctrl Pts',(200.088285349195,12.0350380020923,30.5346635125609));
#75917=CARTESIAN_POINT('Ctrl Pts',(200.091295807415,11.995906517736,30.5738091602959));
#75918=CARTESIAN_POINT('Ctrl Pts',(200.094306265636,11.9546002649204,30.6106827496535));
#75919=CARTESIAN_POINT('Ctrl Pts',(200.097316723856,11.911421751148,30.6450513706967));
#75920=CARTESIAN_POINT('Ctrl Pts',(200.099524322528,11.8797585216102,30.6702542191023));
#75921=CARTESIAN_POINT('Ctrl Pts',(200.1017319212,11.8470892182861,30.6941108724835));
#75922=CARTESIAN_POINT('Ctrl Pts',(200.103939519872,11.8135423611787,30.7165447285521));
#75923=CARTESIAN_POINT('Ctrl Pts',(200.106950857697,11.7677818155575,30.7471462686843));
#75924=CARTESIAN_POINT('Ctrl Pts',(200.109962195522,11.7201970630349,30.7752259382833));
#75925=CARTESIAN_POINT('Ctrl Pts',(200.112973533348,11.6710967602429,30.800561951001));
#75926=CARTESIAN_POINT('Ctrl Pts',(200.115979558626,11.6220830793072,30.8258532663883));
#75927=CARTESIAN_POINT('Ctrl Pts',(200.118985583904,11.571559619394,30.8484102908232));
#75928=CARTESIAN_POINT('Ctrl Pts',(200.121991609183,11.5198629781336,30.8680550917145));
#75929=CARTESIAN_POINT('Ctrl Pts',(200.124994684778,11.4682170645481,30.8876806160137));
#75930=CARTESIAN_POINT('Ctrl Pts',(200.127997760374,11.4154007409956,30.9043993913857));
#75931=CARTESIAN_POINT('Ctrl Pts',(200.13100083597,11.3617724181172,30.91808073377));
#75932=CARTESIAN_POINT('Ctrl Pts',(200.13400214805,11.3081755877612,30.9317540419672));
#75933=CARTESIAN_POINT('Ctrl Pts',(200.137003460129,11.2537682134788,30.9423933226096));
#75934=CARTESIAN_POINT('Ctrl Pts',(200.140004772209,11.1989235663055,30.9499178131081));
#75935=CARTESIAN_POINT('Ctrl Pts',(200.14300550431,11.1440895173922,30.9574408495632));
#75936=CARTESIAN_POINT('Ctrl Pts',(200.146006236412,11.0888188858345,30.9618502197319));
#75937=CARTESIAN_POINT('Ctrl Pts',(200.149006968513,11.0334925320831,30.9631167076808));
#75938=CARTESIAN_POINT('Ctrl Pts',(200.15201044823,10.9781155188538,30.9643843552871));
#75939=CARTESIAN_POINT('Ctrl Pts',(200.155013927947,10.9226832100697,30.9625033595698));
#75940=CARTESIAN_POINT('Ctrl Pts',(200.158017407663,10.867577441544,30.9574966607207));
#75941=CARTESIAN_POINT('Ctrl Pts',(200.161022267035,10.8124463600681,30.9524876620339));
#75942=CARTESIAN_POINT('Ctrl Pts',(200.164027126406,10.757642640595,30.9443501757504));
#75943=CARTESIAN_POINT('Ctrl Pts',(200.167031985777,10.7035406744545,30.9331587903289));
#75944=CARTESIAN_POINT('Ctrl Pts',(200.170042443837,10.6493379049152,30.9219465529909));
#75945=CARTESIAN_POINT('Ctrl Pts',(200.173052901896,10.5958400114111,30.9076691867994));
#75946=CARTESIAN_POINT('Ctrl Pts',(200.176063359956,10.5434077505465,30.8904516416399));
#75947=CARTESIAN_POINT('Ctrl Pts',(200.178270959925,10.5049586324358,30.8778258380506));
#75948=CARTESIAN_POINT('Ctrl Pts',(200.180478559895,10.4670822504933,30.863620032738));
#75949=CARTESIAN_POINT('Ctrl Pts',(200.182686159865,10.4299131928923,30.8478995817055));
#75950=CARTESIAN_POINT('Ctrl Pts',(200.185697497642,10.3792117121727,30.8264556658149));
#75951=CARTESIAN_POINT('Ctrl Pts',(200.188708835419,10.3296163752628,30.8021024532849));
#75952=CARTESIAN_POINT('Ctrl Pts',(200.191720173197,10.2814820181045,30.7749761408328));
#75953=CARTESIAN_POINT('Ctrl Pts',(200.194726198425,10.2334325787354,30.7478976841456));
#75954=CARTESIAN_POINT('Ctrl Pts',(200.197732223653,10.1868394599955,30.7180560935339));
#75955=CARTESIAN_POINT('Ctrl Pts',(200.200738248881,10.1420361867845,30.6856349966211));
#75956=CARTESIAN_POINT('Ctrl Pts',(200.203741324425,10.097276877105,30.6532457131409));
#75957=CARTESIAN_POINT('Ctrl Pts',(200.206744399969,10.0543043590039,30.6182822455201));
#75958=CARTESIAN_POINT('Ctrl Pts',(200.209747475513,10.0134246444191,30.5809723945413));
#75959=CARTESIAN_POINT('Ctrl Pts',(200.21274878754,9.97256893592204,30.5436844532937));
#75960=CARTESIAN_POINT('Ctrl Pts',(200.215750099567,9.93380398383163,30.5040532148703));
#75961=CARTESIAN_POINT('Ctrl Pts',(200.218751411593,9.89740223573112,30.4623463099266));
#75962=CARTESIAN_POINT('Ctrl Pts',(200.221752143641,9.86100752197141,30.4206474645019));
#75963=CARTESIAN_POINT('Ctrl Pts',(200.224752875689,9.82697545188296,30.3768741465184));
#75964=CARTESIAN_POINT('Ctrl Pts',(200.227753607736,9.79553955820122,30.331328631855));
#75965=CARTESIAN_POINT('Ctrl Pts',(200.230757087398,9.76407488031213,30.2857414135406));
#75966=CARTESIAN_POINT('Ctrl Pts',(200.233760567059,9.73521142811629,30.2383791919452));
#75967=CARTESIAN_POINT('Ctrl Pts',(200.23676404672,9.70913967861635,30.189573694885));
#75968=CARTESIAN_POINT('Ctrl Pts',(200.239768906036,9.68305595301036,30.1407457789299));
#75969=CARTESIAN_POINT('Ctrl Pts',(200.242773765351,9.6597667084959,30.0904737454787));
#75970=CARTESIAN_POINT('Ctrl Pts',(200.245778624666,9.6394151678175,30.0391114582671));
#75971=CARTESIAN_POINT('Ctrl Pts',(200.248789082669,9.61902570792044,29.9876534722664));
#75972=CARTESIAN_POINT('Ctrl Pts',(200.251799540672,9.6015850520218,29.9351016766448));
#75973=CARTESIAN_POINT('Ctrl Pts',(200.254809998675,9.58718684532642,29.8818261908006));
#75974=CARTESIAN_POINT('Ctrl Pts',(200.257017599069,9.57662848950547,29.8427587188593));
#75975=CARTESIAN_POINT('Ctrl Pts',(200.259225199463,9.56770514020051,29.8033024178133));
#75976=CARTESIAN_POINT('Ctrl Pts',(200.261432799857,9.56043607063758,29.763605658662));
#75977=CARTESIAN_POINT('Ctrl Pts',(200.265901162103,9.54572288428293,29.6832561985266));
#75978=CARTESIAN_POINT('Ctrl Pts',(200.270369524349,9.53773431809565,29.6016400343671));
#75979=CARTESIAN_POINT('Ctrl Pts',(200.274837886595,9.53663226839757,29.5196756729177));
#75980=CARTESIAN_POINT('Ctrl Pts',(200.275173575782,9.53654947605727,29.5135180365446));
#75981=CARTESIAN_POINT('Ctrl Pts',(200.27550926497,9.53650553028377,29.5073584496461));
#75982=CARTESIAN_POINT('Ctrl Pts',(200.275844954157,9.53650048976792,29.5011973096727));
#75983=CARTESIAN_POINT('',(200.775844954206,9.53650002111796,29.4997513792903));
#75984=CARTESIAN_POINT('Ctrl Pts',(200.275844954197,9.53650048976732,29.5011973089453));
#75985=CARTESIAN_POINT('Ctrl Pts',(200.278807267562,9.53645600939984,29.4468278863525));
#75986=CARTESIAN_POINT('Ctrl Pts',(200.281769580928,9.53944553388517,29.3923573443137));
#75987=CARTESIAN_POINT('Ctrl Pts',(200.284731894294,9.54547632636966,29.3381570735284));
#75988=CARTESIAN_POINT('Ctrl Pts',(200.28769134432,9.55150128955749,29.2840091921195));
#75989=CARTESIAN_POINT('Ctrl Pts',(200.290650794347,9.56056164358428,29.2301316035641));
#75990=CARTESIAN_POINT('Ctrl Pts',(200.293610244374,9.5726126399746,29.176893865054));
#75991=CARTESIAN_POINT('Ctrl Pts',(200.296568082553,9.58465707285924,29.1236851221712));
#75992=CARTESIAN_POINT('Ctrl Pts',(200.299525920733,9.59968880213546,29.0711160693902));
#75993=CARTESIAN_POINT('Ctrl Pts',(200.302483758912,9.61761186279543,29.0195467888378));
#75994=CARTESIAN_POINT('Ctrl Pts',(200.305441233927,9.63553272285592,28.9679838399792));
#75995=CARTESIAN_POINT('Ctrl Pts',(200.308398708942,9.65634402898352,28.917420933234));
#75996=CARTESIAN_POINT('Ctrl Pts',(200.311356183957,9.67990054256185,28.8682012405271));
#75997=CARTESIAN_POINT('Ctrl Pts',(200.314316438232,9.7034791931595,28.8189352940617));
#75998=CARTESIAN_POINT('Ctrl Pts',(200.317276692507,9.72980796069768,28.7710155710276));
#75999=CARTESIAN_POINT('Ctrl Pts',(200.320236946782,9.75869499593452,28.7247618837531));
#76000=CARTESIAN_POINT('Ctrl Pts',(200.323198897984,9.78759859027576,28.6784816821746));
#76001=CARTESIAN_POINT('Ctrl Pts',(200.326160849185,9.81906305282296,28.6338698590219));
#76002=CARTESIAN_POINT('Ctrl Pts',(200.329122800386,9.85285438256853,28.5912155467836));
#76003=CARTESIAN_POINT('Ctrl Pts',(200.332089746762,9.8867026996197,28.5484893002845));
#76004=CARTESIAN_POINT('Ctrl Pts',(200.335056693139,9.92288534338377,28.5077275494681));
#76005=CARTESIAN_POINT('Ctrl Pts',(200.338023639515,9.96113064903218,28.4691834684971));
#76006=CARTESIAN_POINT('Ctrl Pts',(200.338742239627,9.9703937355266,28.4598480180456));
#76007=CARTESIAN_POINT('Ctrl Pts',(200.339460839739,9.97977766981178,28.4506424738096));
#76008=CARTESIAN_POINT('Ctrl Pts',(200.34017943985,9.98927831341127,28.4415700673832));
#76009=CARTESIAN_POINT('Ctrl Pts',(200.343190777668,10.0290913428017,28.4035515921175));
#76010=CARTESIAN_POINT('Ctrl Pts',(200.346202115486,10.0711352732911,28.367703518185));
#76011=CARTESIAN_POINT('Ctrl Pts',(200.349213453304,10.1151442102846,28.3342974301276));
#76012=CARTESIAN_POINT('Ctrl Pts',(200.352219478574,10.1590755075026,28.3009502764902));
#76013=CARTESIAN_POINT('Ctrl Pts',(200.355225503844,10.2049645145514,28.2700368754397));
#76014=CARTESIAN_POINT('Ctrl Pts',(200.358231529114,10.2525102672969,28.2417904190861));
#76015=CARTESIAN_POINT('Ctrl Pts',(200.361234604701,10.3000093654457,28.213571679762));
#76016=CARTESIAN_POINT('Ctrl Pts',(200.364237680288,10.3491615373096,28.1880149689842));
#76017=CARTESIAN_POINT('Ctrl Pts',(200.367240755874,10.3996362017358,28.1653106879375));
#76018=CARTESIAN_POINT('Ctrl Pts',(200.370242067944,10.4500812255747,28.1426197396833));
#76019=CARTESIAN_POINT('Ctrl Pts',(200.373243380014,10.5018467223615,28.1227781169169));
#76020=CARTESIAN_POINT('Ctrl Pts',(200.376244692084,10.5545788829705,28.1059296005925));
#76021=CARTESIAN_POINT('Ctrl Pts',(200.379245424176,10.6073008535302,28.089084340103));
#76022=CARTESIAN_POINT('Ctrl Pts',(200.382246156267,10.6609886145945,28.075231197716));
#76023=CARTESIAN_POINT('Ctrl Pts',(200.385246888359,10.7152720119965,28.0644644822062));
#76024=CARTESIAN_POINT('Ctrl Pts',(200.388250368065,10.7696051138822,28.053687908175));
#76025=CARTESIAN_POINT('Ctrl Pts',(200.391253847771,10.8245344230488,28.0460035096159));
#76026=CARTESIAN_POINT('Ctrl Pts',(200.394257327476,10.8796798508475,28.0414543847696));
#76027=CARTESIAN_POINT('Ctrl Pts',(200.397262186836,10.9348506098064,28.0369031702738));
#76028=CARTESIAN_POINT('Ctrl Pts',(200.400267046197,10.9902371569852,28.0354901138159));
#76029=CARTESIAN_POINT('Ctrl Pts',(200.403271905557,11.0454578509173,28.0372061547197));
#76030=CARTESIAN_POINT('Ctrl Pts',(200.406282363604,11.1007814326649,28.0389253929701));
#76031=CARTESIAN_POINT('Ctrl Pts',(200.409292821652,11.1559380171466,28.043785328107));
#76032=CARTESIAN_POINT('Ctrl Pts',(200.4123032797,11.2105507294148,28.0517249431331));
#76033=CARTESIAN_POINT('Ctrl Pts',(200.414510879747,11.2505987966152,28.0575471450144));
#76034=CARTESIAN_POINT('Ctrl Pts',(200.416718479795,11.2903545139687,28.065024328512));
#76035=CARTESIAN_POINT('Ctrl Pts',(200.418926079842,11.3296740555719,28.074115268655));
#76036=CARTESIAN_POINT('Ctrl Pts',(200.421937417657,11.3833089622339,28.0865160166333));
#76037=CARTESIAN_POINT('Ctrl Pts',(200.424948755472,11.4363547761409,28.101972992898));
#76038=CARTESIAN_POINT('Ctrl Pts',(200.427960093287,11.488438519647,28.1204130826494));
#76039=CARTESIAN_POINT('Ctrl Pts',(200.430966118554,11.5404303779458,28.1388206407247));
#76040=CARTESIAN_POINT('Ctrl Pts',(200.433972143821,11.5914630407979,28.1602006932887));
#76041=CARTESIAN_POINT('Ctrl Pts',(200.436978169088,11.6411763631297,28.1844297352996));
#76042=CARTESIAN_POINT('Ctrl Pts',(200.439981244671,11.6908409039203,28.2086350023956));
#76043=CARTESIAN_POINT('Ctrl Pts',(200.442984320255,11.7391881969001,28.2356834907018));
#76044=CARTESIAN_POINT('Ctrl Pts',(200.445987395839,11.7858775995091,28.2654034470363));
#76045=CARTESIAN_POINT('Ctrl Pts',(200.448988707905,11.8325395843746,28.2951059507136));
#76046=CARTESIAN_POINT('Ctrl Pts',(200.451990019972,11.8775451644612,28.3274765300474));
#76047=CARTESIAN_POINT('Ctrl Pts',(200.454991332039,11.920579908153,28.3622984210677));
#76048=CARTESIAN_POINT('Ctrl Pts',(200.457992064127,11.9636063357389,28.3971135830475));
#76049=CARTESIAN_POINT('Ctrl Pts',(200.460992796215,12.0046622734666,28.4343787841528));
#76050=CARTESIAN_POINT('Ctrl Pts',(200.463993528303,12.0434656634074,28.4738364363857));
#76051=CARTESIAN_POINT('Ctrl Pts',(200.466997008005,12.0823045835926,28.5133302179367));
#76052=CARTESIAN_POINT('Ctrl Pts',(200.470000487708,12.1188864648877,28.5550200841132));
#76053=CARTESIAN_POINT('Ctrl Pts',(200.47300396741,12.1529665957103,28.598612026275));
#76054=CARTESIAN_POINT('Ctrl Pts',(200.476008826767,12.1870623813069,28.6422239924796));
#76055=CARTESIAN_POINT('Ctrl Pts',(200.479013686123,12.2186538243424,28.6877393421784));
#76056=CARTESIAN_POINT('Ctrl Pts',(200.48201854548,12.2475389542448,28.7348341306346));
#76057=CARTESIAN_POINT('Ctrl Pts',(200.485029003524,12.2764779032441,28.7820166666269));
#76058=CARTESIAN_POINT('Ctrl Pts',(200.488039461568,12.3027002162781,28.8307840540367));
#76059=CARTESIAN_POINT('Ctrl Pts',(200.491049919612,12.3260499641419,28.8807878048688));
#76060=CARTESIAN_POINT('Ctrl Pts',(200.493257519686,12.3431725761745,28.917456073437));
#76061=CARTESIAN_POINT('Ctrl Pts',(200.495465119761,12.3587514636632,28.9547886817217));
#76062=CARTESIAN_POINT('Ctrl Pts',(200.497672719836,12.3727421130063,28.9926427873983));
#76063=CARTESIAN_POINT('Ctrl Pts',(200.500684057657,12.3918264444484,29.0442787251921));
#76064=CARTESIAN_POINT('Ctrl Pts',(200.503695395479,12.4080329824707,29.0971003555017));
#76065=CARTESIAN_POINT('Ctrl Pts',(200.506706733301,12.4212180488663,29.1507558052357));
#76066=CARTESIAN_POINT('Ctrl Pts',(200.509712758574,12.4343798544049,29.2043165969898));
#76067=CARTESIAN_POINT('Ctrl Pts',(200.512718783848,12.4445306420242,29.2587077805627));
#76068=CARTESIAN_POINT('Ctrl Pts',(200.515724809122,12.4515758947125,29.3135605409531));
#76069=CARTESIAN_POINT('Ctrl Pts',(200.518727884712,12.4586142341981,29.3683594766954));
#76070=CARTESIAN_POINT('Ctrl Pts',(200.521730960303,12.4625530087727,29.4236185712117));
#76071=CARTESIAN_POINT('Ctrl Pts',(200.524734035894,12.4633487344701,29.4789588183609));
#76072=CARTESIAN_POINT('Ctrl Pts',(200.527735347967,12.4641439928879,29.5342665676727));
#76073=CARTESIAN_POINT('Ctrl Pts',(200.530736660041,12.4617998533954,29.5896548486423));
#76074=CARTESIAN_POINT('Ctrl Pts',(200.533737972115,12.4563248426624,29.6447418482831));
#76075=CARTESIAN_POINT('Ctrl Pts',(200.53673870421,12.4508508899294,29.6998182028213));
#76076=CARTESIAN_POINT('Ctrl Pts',(200.539739436305,12.4422473198108,29.7545928669506));
#76077=CARTESIAN_POINT('Ctrl Pts',(200.5427401684,12.4305745540886,29.8086886703365));
#76078=CARTESIAN_POINT('Ctrl Pts',(200.54574364811,12.4188911002223,29.8628340064348));
#76079=CARTESIAN_POINT('Ctrl Pts',(200.548747127819,12.4041329480555,29.916298723198));
#76080=CARTESIAN_POINT('Ctrl Pts',(200.551750607529,12.386411464481,29.9687168667283));
#76081=CARTESIAN_POINT('Ctrl Pts',(200.554755466893,12.3686818405086,30.021159088635));
#76082=CARTESIAN_POINT('Ctrl Pts',(200.557760326256,12.3479863691258,30.0725532887803));
#76083=CARTESIAN_POINT('Ctrl Pts',(200.56076518562,12.3244849046397,30.1225527988705));
#76084=CARTESIAN_POINT('Ctrl Pts',(200.563775643671,12.3009396519625,30.1726454686063));
#76085=CARTESIAN_POINT('Ctrl Pts',(200.566786101723,12.2745782145316,30.221337792492));
#76086=CARTESIAN_POINT('Ctrl Pts',(200.569796559774,12.2456062389068,30.2683081072046));
#76087=CARTESIAN_POINT('Ctrl Pts',(200.572004159792,12.2243607896,30.3027519246743));
#76088=CARTESIAN_POINT('Ctrl Pts',(200.57421175981,12.2017125012651,30.3362702827466));
#76089=CARTESIAN_POINT('Ctrl Pts',(200.576419359829,12.1777563186957,30.3687475489303));
#76090=CARTESIAN_POINT('Ctrl Pts',(200.579430697647,12.1450782257582,30.4130490614784));
#76091=CARTESIAN_POINT('Ctrl Pts',(200.582442035466,12.1098290739686,30.45559637391));
#76092=CARTESIAN_POINT('Ctrl Pts',(200.585453373285,12.0722240656048,30.4960762034794));
#76093=CARTESIAN_POINT('Ctrl Pts',(200.588459398556,12.0346853993213,30.5364846192605));
#76094=CARTESIAN_POINT('Ctrl Pts',(200.591465423827,11.9947994808948,30.574832407268));
#76095=CARTESIAN_POINT('Ctrl Pts',(200.594471449097,11.9528226647358,30.6108380708122));
#76096=CARTESIAN_POINT('Ctrl Pts',(200.597474524685,11.9108870386168,30.6468084035511));
#76097=CARTESIAN_POINT('Ctrl Pts',(200.600477600273,11.8668649778316,30.6804408228867));
#76098=CARTESIAN_POINT('Ctrl Pts',(200.60348067586,11.8210493744918,30.7114908892132));
#76099=CARTESIAN_POINT('Ctrl Pts',(200.606481987931,11.7752606757671,30.7425227217936));
#76100=CARTESIAN_POINT('Ctrl Pts',(200.609483300002,11.727680958082,30.7709749118339));
#76101=CARTESIAN_POINT('Ctrl Pts',(200.612484612073,11.6786340163266,30.796644948274));
#76102=CARTESIAN_POINT('Ctrl Pts',(200.615485344165,11.6295965524833,30.8223100241938));
#76103=CARTESIAN_POINT('Ctrl Pts',(200.618486076257,11.5790928949116,30.8451937698566));
#76104=CARTESIAN_POINT('Ctrl Pts',(200.62148680835,11.5274714516784,30.8651395964019));
#76105=CARTESIAN_POINT('Ctrl Pts',(200.624490288056,11.4758027413758,30.8851036863027));
#76106=CARTESIAN_POINT('Ctrl Pts',(200.627493767763,11.4230146939145,30.9021242924499));
#76107=CARTESIAN_POINT('Ctrl Pts',(200.630497247469,11.3694743146674,30.9160935635759));
#76108=CARTESIAN_POINT('Ctrl Pts',(200.63350210683,11.315909341543,30.9300692515137));
#76109=CARTESIAN_POINT('Ctrl Pts',(200.636506966191,11.2615918658583,30.9409907062689));
#76110=CARTESIAN_POINT('Ctrl Pts',(200.639511825551,11.2068993967915,30.9488011905045));
#76111=CARTESIAN_POINT('Ctrl Pts',(200.6425222836,11.1521050241049,30.9566262273217));
#76112=CARTESIAN_POINT('Ctrl Pts',(200.645532741648,11.096934789252,30.9613286702391));
#76113=CARTESIAN_POINT('Ctrl Pts',(200.648543199696,11.0417704452592,30.9629037835425));
#76114=CARTESIAN_POINT('Ctrl Pts',(200.650750799738,11.001317860917,30.9640588304286));
#76115=CARTESIAN_POINT('Ctrl Pts',(200.65295839978,10.9608685207544,30.9635332756275));
#76116=CARTESIAN_POINT('Ctrl Pts',(200.655165999822,10.9205711987917,30.961342983539));
#76117=CARTESIAN_POINT('Ctrl Pts',(200.65817733764,10.8656025236147,30.9583552551121));
#76118=CARTESIAN_POINT('Ctrl Pts',(200.661188675459,10.8106883204334,30.9522555185764));
#76119=CARTESIAN_POINT('Ctrl Pts',(200.664200013278,10.7562085845656,30.9430516261591));
#76120=CARTESIAN_POINT('Ctrl Pts',(200.667206038549,10.7018249608698,30.9338639710836));
#76121=CARTESIAN_POINT('Ctrl Pts',(200.670212063819,10.6478747994457,30.9215831154162));
#76122=CARTESIAN_POINT('Ctrl Pts',(200.67321808909,10.5947341242407,30.9062687580776));
#76123=CARTESIAN_POINT('Ctrl Pts',(200.676221164678,10.5416455936893,30.8909694280575));
#76124=CARTESIAN_POINT('Ctrl Pts',(200.679224240265,10.4893654803024,30.8726426386432));
#76125=CARTESIAN_POINT('Ctrl Pts',(200.682227315853,10.4382588976238,30.85139897288));
#76126=CARTESIAN_POINT('Ctrl Pts',(200.685228627924,10.3871823266191,30.8301677821824));
#76127=CARTESIAN_POINT('Ctrl Pts',(200.688229939994,10.3372784065553,30.806023312521));
#76128=CARTESIAN_POINT('Ctrl Pts',(200.691231252065,10.2888941751825,30.7791249962027));
#76129=CARTESIAN_POINT('Ctrl Pts',(200.694231984157,10.2405192936589,30.7522318777597));
#76130=CARTESIAN_POINT('Ctrl Pts',(200.697232716249,10.1936639784066,30.7225862258666));
#76131=CARTESIAN_POINT('Ctrl Pts',(200.700233448342,10.1486504001919,30.6903932580902));
#76132=CARTESIAN_POINT('Ctrl Pts',(200.703236928048,10.1035956053859,30.6581708128883));
#76133=CARTESIAN_POINT('Ctrl Pts',(200.706240407754,10.0603863465903,30.6233966997778));
#76134=CARTESIAN_POINT('Ctrl Pts',(200.709243887461,10.0193142714637,30.5863184394298));
#76135=CARTESIAN_POINT('Ctrl Pts',(200.712248746821,9.97822332979961,30.5492231471109));
#76136=CARTESIAN_POINT('Ctrl Pts',(200.715253606182,9.93927190027695,30.5098219735649));
#76137=CARTESIAN_POINT('Ctrl Pts',(200.718258465543,9.90271467753942,30.4683992828955));
#76138=CARTESIAN_POINT('Ctrl Pts',(200.721268923591,9.86608934097599,30.4268994130061));
#76139=CARTESIAN_POINT('Ctrl Pts',(200.724279381639,9.83186744882186,30.383370917966));
#76140=CARTESIAN_POINT('Ctrl Pts',(200.727289839687,9.80026256370662,30.3381302607329));
#76141=CARTESIAN_POINT('Ctrl Pts',(200.72949743973,9.77708637436698,30.3049548185802));
#76142=CARTESIAN_POINT('Ctrl Pts',(200.731705039772,9.75531658657298,30.2708593398782));
#76143=CARTESIAN_POINT('Ctrl Pts',(200.733912639815,9.73502162669244,30.2359768780771));
#76144=CARTESIAN_POINT('Ctrl Pts',(200.737034469505,9.70632194962605,30.1866486017531));
#76145=CARTESIAN_POINT('Ctrl Pts',(200.740156299194,9.68046138456981,30.1355535224928));
#76146=CARTESIAN_POINT('Ctrl Pts',(200.743278128884,9.65765161603659,30.0830377912887));
#76147=CARTESIAN_POINT('Ctrl Pts',(200.746391806722,9.63490140932597,30.0306591913607));
#76148=CARTESIAN_POINT('Ctrl Pts',(200.749505484559,9.61518634070828,29.9768677493751));
#76149=CARTESIAN_POINT('Ctrl Pts',(200.752619162397,9.59867218006485,29.9220338743227));
#76150=CARTESIAN_POINT('Ctrl Pts',(200.755727965602,9.58218387324064,29.8672858446924));
#76151=CARTESIAN_POINT('Ctrl Pts',(200.758836768807,9.56888666071386,29.8114990725187));
#76152=CARTESIAN_POINT('Ctrl Pts',(200.761945572012,9.55889793952383,29.755062935942));
#76153=CARTESIAN_POINT('Ctrl Pts',(200.765049230185,9.548925749549,29.6987202005025));
#76154=CARTESIAN_POINT('Ctrl Pts',(200.768152888357,9.54225124455546,29.6417307019684));
#76155=CARTESIAN_POINT('Ctrl Pts',(200.77125654653,9.53894124389919,29.5844959242873));
#76156=CARTESIAN_POINT('Ctrl Pts',(200.772786015739,9.53731009001419,29.5562908755073));
#76157=CARTESIAN_POINT('Ctrl Pts',(200.774315484948,9.53649521774352,29.5280264340767));
#76158=CARTESIAN_POINT('Ctrl Pts',(200.775844954157,9.5365000211178,29.4997513802026));
#76159=CARTESIAN_POINT('',(201.275844954123,9.5365002812049,29.4990927587658));
#76160=CARTESIAN_POINT('Ctrl Pts',(200.775844954206,9.53650002111796,29.4997513792903));
#76161=CARTESIAN_POINT('Ctrl Pts',(200.779035926708,9.53651004256292,29.4407603784615));
#76162=CARTESIAN_POINT('Ctrl Pts',(200.782226899209,9.54009107565949,29.381855563932));
#76163=CARTESIAN_POINT('Ctrl Pts',(200.78541787171,9.54718642921113,29.3234639455191));
#76164=CARTESIAN_POINT('Ctrl Pts',(200.788615175693,9.55429586126113,29.2649564672976));
#76165=CARTESIAN_POINT('Ctrl Pts',(200.791812479676,9.56493344073772,29.20696463018));
#76166=CARTESIAN_POINT('Ctrl Pts',(200.795009783659,9.57899146312995,29.1499043157329));
#76167=CARTESIAN_POINT('Ctrl Pts',(200.798218635059,9.59310025762155,29.0926379216628));
#76168=CARTESIAN_POINT('Ctrl Pts',(200.801427486458,9.61065407727911,29.0363101839334));
#76169=CARTESIAN_POINT('Ctrl Pts',(200.804636337857,9.63149530938396,28.9813217165121));
#76170=CARTESIAN_POINT('Ctrl Pts',(200.807310651841,9.64886476390697,28.9354933470876));
#76171=CARTESIAN_POINT('Ctrl Pts',(200.809984965824,9.66851667080154,28.8905949606548));
#76172=CARTESIAN_POINT('Ctrl Pts',(200.812659279808,9.69033553689697,28.8468451607122));
#76173=CARTESIAN_POINT('Ctrl Pts',(200.815670617627,9.71490407187492,28.7975818999421));
#76174=CARTESIAN_POINT('Ctrl Pts',(200.818681955446,9.74230714183326,28.7496043191936));
#76175=CARTESIAN_POINT('Ctrl Pts',(200.821693293265,9.77238665520209,28.7032580557834));
#76176=CARTESIAN_POINT('Ctrl Pts',(200.824699318536,9.80241310283357,28.6569935556189));
#76177=CARTESIAN_POINT('Ctrl Pts',(200.827705343807,9.83510633831289,28.6123551003561));
#76178=CARTESIAN_POINT('Ctrl Pts',(200.830711369078,9.8702622627025,28.5696640956483));
#76179=CARTESIAN_POINT('Ctrl Pts',(200.833714444666,9.90538369009925,28.5270149817828));
#76180=CARTESIAN_POINT('Ctrl Pts',(200.836717520254,9.94296268536604,28.4863099380973));
#76181=CARTESIAN_POINT('Ctrl Pts',(200.839720595842,9.98275278091625,28.4478401522267));
#76182=CARTESIAN_POINT('Ctrl Pts',(200.842721907913,10.0225195102521,28.4093929572358));
#76183=CARTESIAN_POINT('Ctrl Pts',(200.845723219984,10.0644943875634,28.3731787842046));
#76184=CARTESIAN_POINT('Ctrl Pts',(200.848724532055,10.1083932893525,28.3394528344232));
#76185=CARTESIAN_POINT('Ctrl Pts',(200.851725264147,10.1522837080452,28.3057334019001));
#76186=CARTESIAN_POINT('Ctrl Pts',(200.85472599624,10.1980969945793,28.2745015588358));
#76187=CARTESIAN_POINT('Ctrl Pts',(200.857726728332,10.2455168782303,28.2459715039264));
#76188=CARTESIAN_POINT('Ctrl Pts',(200.860730208039,10.2929801818012,28.2174153255303));
#76189=CARTESIAN_POINT('Ctrl Pts',(200.863733687746,10.3420525682668,28.1915661500015));
#76190=CARTESIAN_POINT('Ctrl Pts',(200.866737167452,10.3923910614365,28.1685933649791));
#76191=CARTESIAN_POINT('Ctrl Pts',(200.869742026813,10.4427526776909,28.1456100273632));
#76192=CARTESIAN_POINT('Ctrl Pts',(200.872746886174,10.4943810675172,28.125505905814));
#76193=CARTESIAN_POINT('Ctrl Pts',(200.875751745535,10.5469141132065,28.1084018434948));
#76194=CARTESIAN_POINT('Ctrl Pts',(200.878762203584,10.5995450390537,28.0912659126956));
#76195=CARTESIAN_POINT('Ctrl Pts',(200.881772661632,10.6530834764401,28.0771413416956));
#76196=CARTESIAN_POINT('Ctrl Pts',(200.884783119681,10.707154180014,28.0660984776782));
#76197=CARTESIAN_POINT('Ctrl Pts',(200.88699071972,10.7468047864749,28.0580006312214));
#76198=CARTESIAN_POINT('Ctrl Pts',(200.88919831976,10.7867413511787,28.0515588827169));
#76199=CARTESIAN_POINT('Ctrl Pts',(200.891405919799,10.8268145891604,28.0467832014898));
#76200=CARTESIAN_POINT('Ctrl Pts',(200.894417257618,10.8814775964558,28.0402688015834));
#76201=CARTESIAN_POINT('Ctrl Pts',(200.897428595438,10.9366223771427,28.036829374209));
#76202=CARTESIAN_POINT('Ctrl Pts',(200.900439933257,10.9918732515618,28.0365225639048));
#76203=CARTESIAN_POINT('Ctrl Pts',(200.903445958528,11.0470266533804,28.0362162948698));
#76204=CARTESIAN_POINT('Ctrl Pts',(200.906451983799,11.1022852540853,28.0390316780644));
#76205=CARTESIAN_POINT('Ctrl Pts',(200.90945800907,11.1572683657401,28.0449746012054));
#76206=CARTESIAN_POINT('Ctrl Pts',(200.912461084658,11.2121975248379,28.0509116928121));
#76207=CARTESIAN_POINT('Ctrl Pts',(200.915464160246,11.2668512084008,28.0599701882586));
#76208=CARTESIAN_POINT('Ctrl Pts',(200.918467235834,11.3208507213836,28.072103972767));
#76209=CARTESIAN_POINT('Ctrl Pts',(200.921468547905,11.374818523857,28.0842306318689));
#76210=CARTESIAN_POINT('Ctrl Pts',(200.924469859976,11.4281324034541,28.099428884926));
#76211=CARTESIAN_POINT('Ctrl Pts',(200.927471172047,11.4804230666641,28.1176013863516));
#76212=CARTESIAN_POINT('Ctrl Pts',(200.93047190414,11.5327036251398,28.1357703760929));
#76213=CARTESIAN_POINT('Ctrl Pts',(200.933472636232,11.5839608618802,28.1569122995162));
#76214=CARTESIAN_POINT('Ctrl Pts',(200.936473368325,11.6338421019984,28.1808804300844));
#76215=CARTESIAN_POINT('Ctrl Pts',(200.939476848032,11.6837690157725,28.2048705070225));
#76216=CARTESIAN_POINT('Ctrl Pts',(200.942480327739,11.7323169393867,28.2316917318594));
#76217=CARTESIAN_POINT('Ctrl Pts',(200.945483807446,11.7791559874737,28.2611504541778));
#76218=CARTESIAN_POINT('Ctrl Pts',(200.948488666807,11.8260165511686,28.2906227084176));
#76219=CARTESIAN_POINT('Ctrl Pts',(200.951493526168,11.8711662439269,28.322734568893));
#76220=CARTESIAN_POINT('Ctrl Pts',(200.954498385529,11.9143052432807,28.3572497332709));
#76221=CARTESIAN_POINT('Ctrl Pts',(200.957508843577,11.9575246197001,28.3918292066887));
#76222=CARTESIAN_POINT('Ctrl Pts',(200.960519301626,11.9987254258101,28.4288205754071));
#76223=CARTESIAN_POINT('Ctrl Pts',(200.963529759675,12.0376428350449,28.467948839989));
#76224=CARTESIAN_POINT('Ctrl Pts',(200.965737359714,12.066181373956,28.4966420013082));
#76225=CARTESIAN_POINT('Ctrl Pts',(200.967944959753,12.0934927800915,28.5264834560106));
#76226=CARTESIAN_POINT('Ctrl Pts',(200.970152559793,12.1194867551266,28.5573539078232));
#76227=CARTESIAN_POINT('Ctrl Pts',(200.973163897612,12.1549445548629,28.5994636004217));
#76228=CARTESIAN_POINT('Ctrl Pts',(200.976175235431,12.1880968627921,28.643664290199));
#76229=CARTESIAN_POINT('Ctrl Pts',(200.979186573251,12.2186892305583,28.6896736402404));
#76230=CARTESIAN_POINT('Ctrl Pts',(200.982192598522,12.2492276278187,28.7356018214128));
#76231=CARTESIAN_POINT('Ctrl Pts',(200.985198623793,12.2772147578341,28.7833318946167));
#76232=CARTESIAN_POINT('Ctrl Pts',(200.988204649064,12.3024366799456,28.8325489195962));
#76233=CARTESIAN_POINT('Ctrl Pts',(200.991207724652,12.3276338528725,28.8817176500311));
#76234=CARTESIAN_POINT('Ctrl Pts',(200.99421080024,12.3500709537771,28.9323699744583));
#76235=CARTESIAN_POINT('Ctrl Pts',(200.997213875828,12.3695785990762,28.9841640658578));
#76236=CARTESIAN_POINT('Ctrl Pts',(201.000215187899,12.3890747887652,29.0359277418529));
#76237=CARTESIAN_POINT('Ctrl Pts',(201.00321649997,12.4056447471642,29.088831363019));
#76238=CARTESIAN_POINT('Ctrl Pts',(201.006217812042,12.4191670705782,29.1425128312982));
#76239=CARTESIAN_POINT('Ctrl Pts',(201.009218544134,12.4326867809161,29.1961839260818));
#76240=CARTESIAN_POINT('Ctrl Pts',(201.012219276227,12.443159897221,29.250632058091));
#76241=CARTESIAN_POINT('Ctrl Pts',(201.015220008319,12.4505154122051,29.3054819058402));
#76242=CARTESIAN_POINT('Ctrl Pts',(201.018223488026,12.4578776622515,29.3603819767408));
#76243=CARTESIAN_POINT('Ctrl Pts',(201.021226967733,12.462116537947,29.4156839741909));
#76244=CARTESIAN_POINT('Ctrl Pts',(201.02423044744,12.4632127630113,29.4710058598879));
#76245=CARTESIAN_POINT('Ctrl Pts',(201.027235306801,12.4643094916287,29.5263531578006));
#76246=CARTESIAN_POINT('Ctrl Pts',(201.030240166162,12.4622607115556,29.5817198340573));
#76247=CARTESIAN_POINT('Ctrl Pts',(201.033245025523,12.4570993005867,29.6367255580705));
#76248=CARTESIAN_POINT('Ctrl Pts',(201.036255483572,12.4519282728193,29.6918337693633));
#76249=CARTESIAN_POINT('Ctrl Pts',(201.039265941621,12.4436331087229,29.746579162197));
#76250=CARTESIAN_POINT('Ctrl Pts',(201.042276399669,12.4322982433033,29.8005894080472));
#76251=CARTESIAN_POINT('Ctrl Pts',(201.044483999708,12.4239862691997,29.8401956802187));
#76252=CARTESIAN_POINT('Ctrl Pts',(201.046691599747,12.4140408024542,29.8794068140229));
#76253=CARTESIAN_POINT('Ctrl Pts',(201.048899199786,12.4025119699772,29.918081838963));
#76254=CARTESIAN_POINT('Ctrl Pts',(201.051910537605,12.3867857475464,29.9708375751519));
#76255=CARTESIAN_POINT('Ctrl Pts',(201.054921875424,12.3680460537856,30.0228144967179));
#76256=CARTESIAN_POINT('Ctrl Pts',(201.057933213243,12.3463891544883,30.0736449203786));
#76257=CARTESIAN_POINT('Ctrl Pts',(201.060939238514,12.3247704619039,30.1243856699187));
#76258=CARTESIAN_POINT('Ctrl Pts',(201.063945263785,12.3002449825008,30.173983454088));
#76259=CARTESIAN_POINT('Ctrl Pts',(201.066951289056,12.2729584725088,30.2220865441676));
#76260=CARTESIAN_POINT('Ctrl Pts',(201.069954364644,12.2456987375927,30.270142432759));
#76261=CARTESIAN_POINT('Ctrl Pts',(201.072957440232,12.2156835983674,30.3167060761311));
#76262=CARTESIAN_POINT('Ctrl Pts',(201.07596051582,12.1831057470186,30.361448223268));
#76263=CARTESIAN_POINT('Ctrl Pts',(201.078961827892,12.1505470265878,30.4061640961629));
#76264=CARTESIAN_POINT('Ctrl Pts',(201.081963139963,12.1154288870029,30.4490601673796));
#76265=CARTESIAN_POINT('Ctrl Pts',(201.084964452034,12.0779873064085,30.4898361567563));
#76266=CARTESIAN_POINT('Ctrl Pts',(201.087965184126,12.0405529610871,30.5306042665134));
#76267=CARTESIAN_POINT('Ctrl Pts',(201.090965916219,12.0007964231907,30.5692527197662));
#76268=CARTESIAN_POINT('Ctrl Pts',(201.093966648312,11.9589923933519,30.6055160964423));
#76269=CARTESIAN_POINT('Ctrl Pts',(201.096970128018,11.9171500857384,30.6418126776055));
#76270=CARTESIAN_POINT('Ctrl Pts',(201.099973607725,11.8732569402624,30.6757194729314));
#76271=CARTESIAN_POINT('Ctrl Pts',(201.102977087432,11.8276216746949,30.7070106103822));
#76272=CARTESIAN_POINT('Ctrl Pts',(201.105981946793,11.7819654464794,30.7383161214779));
#76273=CARTESIAN_POINT('Ctrl Pts',(201.108986806154,11.7345659551008,30.7670033060115));
#76274=CARTESIAN_POINT('Ctrl Pts',(201.111991665515,11.6857591266666,30.7928908191311));
#76275=CARTESIAN_POINT('Ctrl Pts',(201.115002123564,11.6368613608043,30.8188265661544));
#76276=CARTESIAN_POINT('Ctrl Pts',(201.118012581613,11.5865515004884,30.8419520010438));
#76277=CARTESIAN_POINT('Ctrl Pts',(201.121023039661,11.5351870917338,30.8621332632461));
#76278=CARTESIAN_POINT('Ctrl Pts',(201.1232306397,11.4975210392768,30.8769323916541));
#76279=CARTESIAN_POINT('Ctrl Pts',(201.12543823974,11.4592883548363,30.8901493188304));
#76280=CARTESIAN_POINT('Ctrl Pts',(201.127645839779,11.42063438191,30.9017485390594));
#76281=CARTESIAN_POINT('Ctrl Pts',(201.130657177598,11.3679073623102,30.9175707758453));
#76282=CARTESIAN_POINT('Ctrl Pts',(201.133668515417,11.3141766927841,30.930446786486));
#76283=CARTESIAN_POINT('Ctrl Pts',(201.136679853236,11.2598025327165,30.9402551489212));
#76284=CARTESIAN_POINT('Ctrl Pts',(201.139685878507,11.2055242985658,30.9500462076196));
#76285=CARTESIAN_POINT('Ctrl Pts',(201.142691903778,11.1506053419185,30.9567802654788));
#76286=CARTESIAN_POINT('Ctrl Pts',(201.145697929049,11.0954196607132,30.9603860237449));
#76287=CARTESIAN_POINT('Ctrl Pts',(201.148701004637,11.0402881308376,30.9639882438359));
#76288=CARTESIAN_POINT('Ctrl Pts',(201.151704080226,10.9848909188312,30.9644682112614));
#76289=CARTESIAN_POINT('Ctrl Pts',(201.154707155814,10.929609006691,30.9618061971619));
#76290=CARTESIAN_POINT('Ctrl Pts',(201.157708467885,10.8743595581323,30.9591457462955));
#76291=CARTESIAN_POINT('Ctrl Pts',(201.160709779956,10.8192258011874,30.9533469965259));
#76292=CARTESIAN_POINT('Ctrl Pts',(201.163711092027,10.7645882709785,30.9444423033957));
#76293=CARTESIAN_POINT('Ctrl Pts',(201.16671182412,10.7099612990164,30.9355393310232));
#76294=CARTESIAN_POINT('Ctrl Pts',(201.169712556212,10.6558308837645,30.9235316922459));
#76295=CARTESIAN_POINT('Ctrl Pts',(201.172713288305,10.6025696857297,30.9085032464638));
#76296=CARTESIAN_POINT('Ctrl Pts',(201.175716768012,10.5492597191874,30.8934610399159));
#76297=CARTESIAN_POINT('Ctrl Pts',(201.178720247718,10.4968210686832,30.8753926442385));
#76298=CARTESIAN_POINT('Ctrl Pts',(201.181723727425,10.4456120184879,30.8544320639866));
#76299=CARTESIAN_POINT('Ctrl Pts',(201.184728586786,10.3943794453159,30.8334618554514));
#76300=CARTESIAN_POINT('Ctrl Pts',(201.187733446147,10.3443780752864,30.8095970417164));
#76301=CARTESIAN_POINT('Ctrl Pts',(201.190738305508,10.2959439165109,30.7830188156461));
#76302=CARTESIAN_POINT('Ctrl Pts',(201.193748763557,10.2474195146695,30.7563910687281));
#76303=CARTESIAN_POINT('Ctrl Pts',(201.196759221606,10.2004686053393,30.7270400909435));
#76304=CARTESIAN_POINT('Ctrl Pts',(201.199769679654,10.1553993805914,30.6951912163727));
#76305=CARTESIAN_POINT('Ctrl Pts',(201.201977279693,10.1223496517097,30.6718361070795));
#76306=CARTESIAN_POINT('Ctrl Pts',(201.204184879732,10.0903111877009,30.6471386953245));
#76307=CARTESIAN_POINT('Ctrl Pts',(201.206392479772,10.0593934657064,30.6212009622026));
#76308=CARTESIAN_POINT('Ctrl Pts',(201.209362370245,10.0177997682988,30.5863068576791));
#76309=CARTESIAN_POINT('Ctrl Pts',(201.212332260719,9.9780525919316,30.5490127380806));
#76310=CARTESIAN_POINT('Ctrl Pts',(201.215302151193,9.94044673915803,30.5095440245176));
#76311=CARTESIAN_POINT('Ctrl Pts',(201.218267924276,9.90289302231497,30.4701300295144));
#76312=CARTESIAN_POINT('Ctrl Pts',(201.221233697358,9.86747512676013,30.4285477946313));
#76313=CARTESIAN_POINT('Ctrl Pts',(201.224199470441,9.83445434527412,30.3850624705351));
#76314=CARTESIAN_POINT('Ctrl Pts',(201.227162378013,9.80146546825652,30.3416191616815));
#76315=CARTESIAN_POINT('Ctrl Pts',(201.230125285585,9.77086944765679,30.296276833923));
#76316=CARTESIAN_POINT('Ctrl Pts',(201.233088193156,9.74288854327967,30.2493350621601));
#76317=CARTESIAN_POINT('Ctrl Pts',(201.236049482399,9.71492292196651,30.2024189298151));
#76318=CARTESIAN_POINT('Ctrl Pts',(201.239010771642,9.68956986442099,30.1539055502177));
#76319=CARTESIAN_POINT('Ctrl Pts',(201.241972060885,9.6670079355758,30.1041228403083));
#76320=CARTESIAN_POINT('Ctrl Pts',(201.244934752111,9.64443532507853,30.0543165614216));
#76321=CARTESIAN_POINT('Ctrl Pts',(201.247897443338,9.62465671848826,30.0032402423141));
#76322=CARTESIAN_POINT('Ctrl Pts',(201.250860134565,9.60780351635772,29.9512440591676));
#76323=CARTESIAN_POINT('Ctrl Pts',(201.253823411797,9.59094698074699,29.8992375914327));
#76324=CARTESIAN_POINT('Ctrl Pts',(201.256786689029,9.57701714999311,29.8463114209451));
#76325=CARTESIAN_POINT('Ctrl Pts',(201.259749966262,9.56609526273123,29.7928300777553));
#76326=CARTESIAN_POINT('Ctrl Pts',(201.262717941725,9.55515605898502,29.7392639407182));
#76327=CARTESIAN_POINT('Ctrl Pts',(201.265685917188,9.54723440875636,29.6851414109736));
#76328=CARTESIAN_POINT('Ctrl Pts',(201.268653892651,9.54235996429844,29.6308349201091));
#76329=CARTESIAN_POINT('Ctrl Pts',(201.271050913141,9.53842322580702,29.5869754701213));
#76330=CARTESIAN_POINT('Ctrl Pts',(201.273447933632,9.53647306489063,29.5429962617961));
#76331=CARTESIAN_POINT('Ctrl Pts',(201.275844954123,9.5365002812049,29.4990927587658));
#76332=CARTESIAN_POINT('',(201.775844954191,9.53650056016494,29.5012804696304));
#76333=CARTESIAN_POINT('Ctrl Pts',(201.275844954157,9.53650028120529,29.4990927581348));
#76334=CARTESIAN_POINT('Ctrl Pts',(201.278943009359,9.53653545725112,29.4423491981655));
#76335=CARTESIAN_POINT('Ctrl Pts',(201.282041064562,9.53987072460519,29.3857096621656));
#76336=CARTESIAN_POINT('Ctrl Pts',(201.285139119765,9.54647033012784,29.3294604186667));
#76337=CARTESIAN_POINT('Ctrl Pts',(201.288150457585,9.55288520668872,29.2747856426593));
#76338=CARTESIAN_POINT('Ctrl Pts',(201.291161795404,9.56240261438851,29.2203595877923));
#76339=CARTESIAN_POINT('Ctrl Pts',(201.294173133223,9.57499098432945,29.1665610171896));
#76340=CARTESIAN_POINT('Ctrl Pts',(201.297179158495,9.58755714609419,29.112857357059));
#76341=CARTESIAN_POINT('Ctrl Pts',(201.300185183766,9.60318339896488,29.0597794939176));
#76342=CARTESIAN_POINT('Ctrl Pts',(201.303191209037,9.62178667658693,29.0076989892691));
#76343=CARTESIAN_POINT('Ctrl Pts',(201.306194284625,9.64037169961471,28.9556695889743));
#76344=CARTESIAN_POINT('Ctrl Pts',(201.309197360213,9.6619277836783,28.9046361028439));
#76345=CARTESIAN_POINT('Ctrl Pts',(201.312200435801,9.68632175902193,28.8549560253899));
#76346=CARTESIAN_POINT('Ctrl Pts',(201.315201747872,9.71070140932188,28.8053051219131));
#76347=CARTESIAN_POINT('Ctrl Pts',(201.318203059943,9.73791541548378,28.7570065243937));
#76348=CARTESIAN_POINT('Ctrl Pts',(201.321204372014,9.76778298274491,28.7103966360337));
#76349=CARTESIAN_POINT('Ctrl Pts',(201.324205104106,9.79764477834792,28.6637957546456));
#76350=CARTESIAN_POINT('Ctrl Pts',(201.327205836199,9.83015883205242,28.6188833782219));
#76351=CARTESIAN_POINT('Ctrl Pts',(201.330206568291,9.86510020624162,28.575968232079));
#76352=CARTESIAN_POINT('Ctrl Pts',(201.333210047998,9.90007357442893,28.53301379077));
#76353=CARTESIAN_POINT('Ctrl Pts',(201.336213527704,9.93747836937182,28.4920606430972));
#76354=CARTESIAN_POINT('Ctrl Pts',(201.339217007411,9.97704933920155,28.4533844088817));
#76355=CARTESIAN_POINT('Ctrl Pts',(201.342221866771,10.0166384860332,28.4146904086627));
#76356=CARTESIAN_POINT('Ctrl Pts',(201.345226726132,10.0583953929353,28.3782757541214));
#76357=CARTESIAN_POINT('Ctrl Pts',(201.348231585493,10.1020203443707,28.3443768832029));
#76358=CARTESIAN_POINT('Ctrl Pts',(201.351242043541,10.1457265783032,28.3104148515292));
#76359=CARTESIAN_POINT('Ctrl Pts',(201.35425250159,10.1913073739994,28.2789782669899));
#76360=CARTESIAN_POINT('Ctrl Pts',(201.357262959638,10.2384335485633,28.250260511128));
#76361=CARTESIAN_POINT('Ctrl Pts',(201.359470559677,10.2729916600327,28.229201483583));
#76362=CARTESIAN_POINT('Ctrl Pts',(201.361678159716,10.308380177473,28.2096035715251));
#76363=CARTESIAN_POINT('Ctrl Pts',(201.363885759755,10.3444620337117,28.1915267581053));
#76364=CARTESIAN_POINT('Ctrl Pts',(201.366897097574,10.3936804864861,28.1668685813825));
#76365=CARTESIAN_POINT('Ctrl Pts',(201.369908435393,10.4443945319431,28.1449400134599));
#76366=CARTESIAN_POINT('Ctrl Pts',(201.372919773213,10.496270272697,28.1259226325162));
#76367=CARTESIAN_POINT('Ctrl Pts',(201.375925798484,10.5480544952006,28.1069388016944));
#76368=CARTESIAN_POINT('Ctrl Pts',(201.378931823755,10.6009958543138,28.0908561455167));
#76369=CARTESIAN_POINT('Ctrl Pts',(201.381937849026,10.6547381965548,28.0778092472942));
#76370=CARTESIAN_POINT('Ctrl Pts',(201.384940924614,10.7084278037525,28.0647751514305));
#76371=CARTESIAN_POINT('Ctrl Pts',(201.387944000202,10.7629163267984,28.0547710361226));
#76372=CARTESIAN_POINT('Ctrl Pts',(201.39094707579,10.8178318595013,28.0478818854559));
#76373=CARTESIAN_POINT('Ctrl Pts',(201.393948387861,10.8727151437743,28.040996780353));
#76374=CARTESIAN_POINT('Ctrl Pts',(201.396949699932,10.9280244181891,28.037223079588));
#76375=CARTESIAN_POINT('Ctrl Pts',(201.399951012004,10.9833792554417,28.0365943826641));
#76376=CARTESIAN_POINT('Ctrl Pts',(201.402951744096,11.0387233958339,28.0359658072306));
#76377=CARTESIAN_POINT('Ctrl Pts',(201.405952476189,11.0941125543052,28.0384810344984));
#76378=CARTESIAN_POINT('Ctrl Pts',(201.408953208282,11.1491651992981,28.0441215733042));
#76379=CARTESIAN_POINT('Ctrl Pts',(201.411956687989,11.2042682531333,28.0497672768578));
#76380=CARTESIAN_POINT('Ctrl Pts',(201.414960167696,11.2590336519833,28.0585439549238));
#76381=CARTESIAN_POINT('Ctrl Pts',(201.417963647403,11.3130853984731,28.0703812454843));
#76382=CARTESIAN_POINT('Ctrl Pts',(201.420968506764,11.3671619737377,28.0822239735272));
#76383=CARTESIAN_POINT('Ctrl Pts',(201.423973366125,11.4205237341886,28.0971299743663));
#76384=CARTESIAN_POINT('Ctrl Pts',(201.426978225487,11.4728085074863,28.1149785686681));
#76385=CARTESIAN_POINT('Ctrl Pts',(201.429988683535,11.5251906983579,28.1328604186703));
#76386=CARTESIAN_POINT('Ctrl Pts',(201.432999141584,11.5764914038044,28.1536956149628));
#76387=CARTESIAN_POINT('Ctrl Pts',(201.436009599633,11.6263682580533,28.1773152093929));
#76388=CARTESIAN_POINT('Ctrl Pts',(201.438217199672,11.6629434713964,28.1946357024026));
#76389=CARTESIAN_POINT('Ctrl Pts',(201.440424799711,11.6987534486628,28.2134524728893));
#76390=CARTESIAN_POINT('Ctrl Pts',(201.44263239975,11.7336727990414,28.2336838965145));
#76391=CARTESIAN_POINT('Ctrl Pts',(201.44564373757,11.7813055035869,28.2612811288119));
#76392=CARTESIAN_POINT('Ctrl Pts',(201.448655075389,11.8274780115704,28.291627067655));
#76393=CARTESIAN_POINT('Ctrl Pts',(201.451666413208,11.8718552337559,28.3245423438625));
#76394=CARTESIAN_POINT('Ctrl Pts',(201.454672438479,11.916154166443,28.3573995515308));
#76395=CARTESIAN_POINT('Ctrl Pts',(201.45767846375,11.9586636784989,28.3928167891312));
#76396=CARTESIAN_POINT('Ctrl Pts',(201.460684489021,11.9990757383647,28.4305702832766));
#76397=CARTESIAN_POINT('Ctrl Pts',(201.463687564609,12.0394481436184,28.4682867315459));
#76398=CARTESIAN_POINT('Ctrl Pts',(201.466690640197,12.0777267902844,28.5083345364326));
#76399=CARTESIAN_POINT('Ctrl Pts',(201.469693715785,12.1136364518988,28.550449525827));
#76400=CARTESIAN_POINT('Ctrl Pts',(201.472695027857,12.1495250260331,28.5925397837434));
#76401=CARTESIAN_POINT('Ctrl Pts',(201.475696339928,12.183047030988,28.6366944192596));
#76402=CARTESIAN_POINT('Ctrl Pts',(201.478697651999,12.2139655081345,28.6826139253329));
#76403=CARTESIAN_POINT('Ctrl Pts',(201.481698384091,12.2448780105433,28.7285245578448));
#76404=CARTESIAN_POINT('Ctrl Pts',(201.484699116184,12.2731876899333,28.7761989461178));
#76405=CARTESIAN_POINT('Ctrl Pts',(201.487699848276,12.2987005179312,28.8253080593891));
#76406=CARTESIAN_POINT('Ctrl Pts',(201.490703327983,12.324236706698,28.8744621393199));
#76407=CARTESIAN_POINT('Ctrl Pts',(201.49370680769,12.3469706842946,28.9250530994976));
#76408=CARTESIAN_POINT('Ctrl Pts',(201.496710287397,12.3667548137752,28.9767280544285));
#76409=CARTESIAN_POINT('Ctrl Pts',(201.499715146758,12.3865480311342,29.0284267463503));
#76410=CARTESIAN_POINT('Ctrl Pts',(201.502720006119,12.4033885386845,29.0812099221252));
#76411=CARTESIAN_POINT('Ctrl Pts',(201.50572486548,12.4171783446443,29.1347086238752));
#76412=CARTESIAN_POINT('Ctrl Pts',(201.508735323528,12.4309938439247,29.1883070050041));
#76413=CARTESIAN_POINT('Ctrl Pts',(201.511745781577,12.4417471847588,29.2426230564507));
#76414=CARTESIAN_POINT('Ctrl Pts',(201.514756239625,12.4493915926365,29.297277871966));
#76415=CARTESIAN_POINT('Ctrl Pts',(201.516963839664,12.454997316037,29.3373568137478));
#76416=CARTESIAN_POINT('Ctrl Pts',(201.519171439703,12.4589323153221,29.3776177266039));
#76417=CARTESIAN_POINT('Ctrl Pts',(201.521379039742,12.4611959639813,29.417910994373));
#76418=CARTESIAN_POINT('Ctrl Pts',(201.524390377561,12.464283756469,29.4728741393917));
#76419=CARTESIAN_POINT('Ctrl Pts',(201.527401715381,12.4642724907512,29.5281260748405));
#76420=CARTESIAN_POINT('Ctrl Pts',(201.5304130532,12.4611280972899,29.583288254334));
#76421=CARTESIAN_POINT('Ctrl Pts',(201.533419078471,12.4579892511111,29.638353117701));
#76422=CARTESIAN_POINT('Ctrl Pts',(201.536425103742,12.4517282765108,29.6933280168053));
#76423=CARTESIAN_POINT('Ctrl Pts',(201.539431129013,12.4423630725208,29.7478326391505));
#76424=CARTESIAN_POINT('Ctrl Pts',(201.542434204601,12.4330070582018,29.8022837784598));
#76425=CARTESIAN_POINT('Ctrl Pts',(201.545437280189,12.4205529377773,29.8562650377195));
#76426=CARTESIAN_POINT('Ctrl Pts',(201.548440355777,12.4050703867959,29.9094013411669));
#76427=CARTESIAN_POINT('Ctrl Pts',(201.551441667848,12.3895969277405,29.9625064410135));
#76428=CARTESIAN_POINT('Ctrl Pts',(201.554442979919,12.3710987105516,30.0147670630399));
#76429=CARTESIAN_POINT('Ctrl Pts',(201.557444291991,12.3496959544205,30.0658207142028));
#76430=CARTESIAN_POINT('Ctrl Pts',(201.560445024083,12.3282973341934,30.1168644996736));
#76431=CARTESIAN_POINT('Ctrl Pts',(201.563445756176,12.3039954937234,30.166701291245));
#76432=CARTESIAN_POINT('Ctrl Pts',(201.566446488269,12.276958898865,30.2149882660642));
#76433=CARTESIAN_POINT('Ctrl Pts',(201.569449967975,12.2498975480036,30.2633194547535));
#76434=CARTESIAN_POINT('Ctrl Pts',(201.572453447682,12.2200966986014,30.3100975304298));
#76435=CARTESIAN_POINT('Ctrl Pts',(201.575456927389,12.1877702255091,30.3550053458277));
#76436=CARTESIAN_POINT('Ctrl Pts',(201.57846178675,12.1554289031886,30.399933789718));
#76437=CARTESIAN_POINT('Ctrl Pts',(201.581466646111,12.1205599771605,30.4429898501169));
#76438=CARTESIAN_POINT('Ctrl Pts',(201.584471505473,12.0834180133996,30.4838890477291));
#76439=CARTESIAN_POINT('Ctrl Pts',(201.587481963521,12.0462068463168,30.5248644491834));
#76440=CARTESIAN_POINT('Ctrl Pts',(201.59049242157,12.006714558814,30.5636745897608));
#76441=CARTESIAN_POINT('Ctrl Pts',(201.593502879618,11.9652321528155,30.6000723345176));
#76442=CARTESIAN_POINT('Ctrl Pts',(201.595710479658,11.9348126752392,30.6267631773897));
#76443=CARTESIAN_POINT('Ctrl Pts',(201.597918079697,11.9033237844964,30.652157568172));
#76444=CARTESIAN_POINT('Ctrl Pts',(201.600125679736,11.8708901834167,30.6761728352706));
#76445=CARTESIAN_POINT('Ctrl Pts',(201.603137017555,11.8266482338728,30.7089315237877));
#76446=CARTESIAN_POINT('Ctrl Pts',(201.606148355374,11.780463354822,30.7392586312133));
#76447=CARTESIAN_POINT('Ctrl Pts',(201.609159693193,11.7326332231879,30.7669178388046));
#76448=CARTESIAN_POINT('Ctrl Pts',(201.612165718464,11.6848874726131,30.7945282505186));
#76449=CARTESIAN_POINT('Ctrl Pts',(201.615171743736,11.6355026828221,30.8194798410846));
#76450=CARTESIAN_POINT('Ctrl Pts',(201.618177769007,11.5848065405911,30.8415787565707));
#76451=CARTESIAN_POINT('Ctrl Pts',(201.621180844595,11.5341601442987,30.8636559873439));
#76452=CARTESIAN_POINT('Ctrl Pts',(201.624183920183,11.4822054260415,30.8828858785978));
#76453=CARTESIAN_POINT('Ctrl Pts',(201.627186995771,11.429294124133,30.8991207256648));
#76454=CARTESIAN_POINT('Ctrl Pts',(201.630188307842,11.376413893696,30.9153460390298));
#76455=CARTESIAN_POINT('Ctrl Pts',(201.633189619913,11.3225786964833,30.9285796400069));
#76456=CARTESIAN_POINT('Ctrl Pts',(201.636190931984,11.2681575057671,30.9387229761496));
#76457=CARTESIAN_POINT('Ctrl Pts',(201.639191664077,11.2137468314919,30.9488643521772));
#76458=CARTESIAN_POINT('Ctrl Pts',(201.642192396169,11.1587509070089,30.9559165528706));
#76459=CARTESIAN_POINT('Ctrl Pts',(201.645193128262,11.1035487557779,30.9598321496586));
#76460=CARTESIAN_POINT('Ctrl Pts',(201.648196607969,11.0482960588096,30.9637513317548));
#76461=CARTESIAN_POINT('Ctrl Pts',(201.651200087676,10.9928372852408,30.9645281350195));
#76462=CARTESIAN_POINT('Ctrl Pts',(201.654203567382,10.9375549314591,30.9621671803918));
#76463=CARTESIAN_POINT('Ctrl Pts',(201.657208426743,10.8822471836207,30.959805141255));
#76464=CARTESIAN_POINT('Ctrl Pts',(201.660213286104,10.8271165429726,30.9543025235911));
#76465=CARTESIAN_POINT('Ctrl Pts',(201.663218145466,10.7725405443215,30.945715893951));
#76466=CARTESIAN_POINT('Ctrl Pts',(201.666228603514,10.7178628590599,30.9371132656065));
#76467=CARTESIAN_POINT('Ctrl Pts',(201.669239061563,10.6637423969213,30.9254152588641));
#76468=CARTESIAN_POINT('Ctrl Pts',(201.672249519611,10.6105454863477,30.9107293970836));
#76469=CARTESIAN_POINT('Ctrl Pts',(201.67445711965,10.5715356413456,30.8999601026715));
#76470=CARTESIAN_POINT('Ctrl Pts',(201.67666471969,10.5330221805194,30.8875851821225));
#76471=CARTESIAN_POINT('Ctrl Pts',(201.678872319729,10.4951426685791,30.8736634685797));
#76472=CARTESIAN_POINT('Ctrl Pts',(201.681883657548,10.4434720738802,30.8546731706288));
#76473=CARTESIAN_POINT('Ctrl Pts',(201.684894995367,10.3927669749891,30.8327239236214));
#76474=CARTESIAN_POINT('Ctrl Pts',(201.687906333186,10.3433883253009,30.8079347684991));
#76475=CARTESIAN_POINT('Ctrl Pts',(201.690912358457,10.2940967885397,30.7831893459591));
#76476=CARTESIAN_POINT('Ctrl Pts',(201.693918383728,10.2461275246584,30.7556141930645));
#76477=CARTESIAN_POINT('Ctrl Pts',(201.696924408999,10.1998224727877,30.7253767481654));
#76478=CARTESIAN_POINT('Ctrl Pts',(201.699927484587,10.153562858068,30.6951689739673));
#76479=CARTESIAN_POINT('Ctrl Pts',(201.702930560175,10.1089646598888,30.6623043701208));
#76480=CARTESIAN_POINT('Ctrl Pts',(201.705933635763,10.0663444522473,30.6269958154983));
#76481=CARTESIAN_POINT('Ctrl Pts',(201.708934947835,10.0237492727665,30.5917079953636));
#76482=CARTESIAN_POINT('Ctrl Pts',(201.711936259906,9.98313018691714,30.5539794051631));
#76483=CARTESIAN_POINT('Ctrl Pts',(201.714937571977,9.94477215104161,30.5140643159005));
#76484=CARTESIAN_POINT('Ctrl Pts',(201.717938304069,9.9064215275364,30.4741569398957));
#76485=CARTESIAN_POINT('Ctrl Pts',(201.720939036162,9.87033145153059,30.4320642842625));
#76486=CARTESIAN_POINT('Ctrl Pts',(201.723939768255,9.83674966897721,30.3880770897706));
#76487=CARTESIAN_POINT('Ctrl Pts',(201.726943247961,9.80313713733304,30.3440496184936));
#76488=CARTESIAN_POINT('Ctrl Pts',(201.729946727668,9.77203780817293,30.2981245630788));
#76489=CARTESIAN_POINT('Ctrl Pts',(201.732950207375,9.74365783213183,30.2506241451194));
#76490=CARTESIAN_POINT('Ctrl Pts',(201.735955066736,9.71526481969356,30.2031019077508));
#76491=CARTESIAN_POINT('Ctrl Pts',(201.738959926097,9.68959389524046,30.154003333666));
#76492=CARTESIAN_POINT('Ctrl Pts',(201.741964785458,9.66680506989105,30.1036750188071));
#76493=CARTESIAN_POINT('Ctrl Pts',(201.744975243507,9.6439737841476,30.0532529316696));
#76494=CARTESIAN_POINT('Ctrl Pts',(201.747985701555,9.62403551457131,30.0015970201963));
#76495=CARTESIAN_POINT('Ctrl Pts',(201.750996159604,9.60710153044035,29.9490724924758));
#76496=CARTESIAN_POINT('Ctrl Pts',(201.753203759643,9.59468366464524,29.9105557127776));
#76497=CARTESIAN_POINT('Ctrl Pts',(201.755411359682,9.5838802995295,29.8715722210717));
#76498=CARTESIAN_POINT('Ctrl Pts',(201.757618959721,9.57471779430217,29.8322692945807));
#76499=CARTESIAN_POINT('Ctrl Pts',(201.761619230085,9.55811492355215,29.7610506275853));
#76500=CARTESIAN_POINT('Ctrl Pts',(201.765619500448,9.54684447122907,29.6885456861229));
#76501=CARTESIAN_POINT('Ctrl Pts',(201.769619770812,9.54105985342675,29.6154378565152));
#76502=CARTESIAN_POINT('Ctrl Pts',(201.771694831927,9.53805919737696,29.577514616174));
#76503=CARTESIAN_POINT('Ctrl Pts',(201.773769893042,9.53653393815549,29.5394294781608));
#76504=CARTESIAN_POINT('Ctrl Pts',(201.775844954157,9.53650056016549,29.5012804702496));
#76505=CARTESIAN_POINT('',(202.275844954211,9.5365001227665,29.4994005523254));
#76506=CARTESIAN_POINT('Ctrl Pts',(201.775844954191,9.53650056016494,29.5012804696304));
#76507=CARTESIAN_POINT('Ctrl Pts',(201.778811262791,9.53645284621078,29.4467463022148));
#76508=CARTESIAN_POINT('Ctrl Pts',(201.781777571391,9.53945754436547,29.3921280057072));
#76509=CARTESIAN_POINT('Ctrl Pts',(201.78474387999,9.5455162473522,29.3377986951854));
#76510=CARTESIAN_POINT('Ctrl Pts',(201.787707949009,9.55157037598047,29.2835104036311));
#76511=CARTESIAN_POINT('Ctrl Pts',(201.790672018027,9.56067388448575,29.2295112035404));
#76512=CARTESIAN_POINT('Ctrl Pts',(201.793636087046,9.5727763727872,29.1761713911256));
#76513=CARTESIAN_POINT('Ctrl Pts',(201.796599159415,9.5848747917047,29.1228495138801));
#76514=CARTESIAN_POINT('Ctrl Pts',(201.799562231785,9.59997007127091,29.0701871133066));
#76515=CARTESIAN_POINT('Ctrl Pts',(201.802525304154,9.61796076786666,29.0185440717529));
#76516=CARTESIAN_POINT('Ctrl Pts',(201.805490722761,9.63596570996164,28.9668601379022));
#76517=CARTESIAN_POINT('Ctrl Pts',(201.808456141367,9.65687047392248,28.9161976901676));
#76518=CARTESIAN_POINT('Ctrl Pts',(201.811421559974,9.68052431889611,28.866899552223));
#76519=CARTESIAN_POINT('Ctrl Pts',(201.814388093819,9.70418705963906,28.8175828741694));
#76520=CARTESIAN_POINT('Ctrl Pts',(201.817354627664,9.7306006801876,28.7696320047885));
#76521=CARTESIAN_POINT('Ctrl Pts',(201.82032116151,9.75956859734311,28.7233648312736));
#76522=CARTESIAN_POINT('Ctrl Pts',(201.823293215422,9.78859041741771,28.6770115647304));
#76523=CARTESIAN_POINT('Ctrl Pts',(201.826265269334,9.82017571292884,28.632348695266));
#76524=CARTESIAN_POINT('Ctrl Pts',(201.829237323245,9.85408550628692,28.5896636758328));
#76525=CARTESIAN_POINT('Ctrl Pts',(201.831613415402,9.88119564506759,28.5555379355645));
#76526=CARTESIAN_POINT('Ctrl Pts',(201.833989507558,9.90979064007753,28.5226758097128));
#76527=CARTESIAN_POINT('Ctrl Pts',(201.836365599714,9.93973182930301,28.4912068318001));
#76528=CARTESIAN_POINT('Ctrl Pts',(201.839376937533,9.97767776302064,28.4513246567453));
#76529=CARTESIAN_POINT('Ctrl Pts',(201.842388275352,10.0179560153532,28.4135035133625));
#76530=CARTESIAN_POINT('Ctrl Pts',(201.845399613171,10.060314008029,28.3780274127709));
#76531=CARTESIAN_POINT('Ctrl Pts',(201.848405638443,10.1025972734949,28.3426138984789));
#76532=CARTESIAN_POINT('Ctrl Pts',(201.851411663714,10.1469525965704,28.3095375527112));
#76533=CARTESIAN_POINT('Ctrl Pts',(201.854417688985,10.1930905304169,28.2790457183428));
#76534=CARTESIAN_POINT('Ctrl Pts',(201.857420764573,10.2391831910981,28.2485838042968));
#76535=CARTESIAN_POINT('Ctrl Pts',(201.860423840161,10.2870545592629,28.2207016670607));
#76536=CARTESIAN_POINT('Ctrl Pts',(201.863426915749,10.3363835550428,28.1956053266046));
#76537=CARTESIAN_POINT('Ctrl Pts',(201.86642822782,10.3856835830137,28.1705237236468));
#76538=CARTESIAN_POINT('Ctrl Pts',(201.869429539891,10.4364390725868,28.1482249135451));
#76539=CARTESIAN_POINT('Ctrl Pts',(201.872430851962,10.4883035091198,28.1288694623702));
#76540=CARTESIAN_POINT('Ctrl Pts',(201.875431584055,10.5401579232833,28.1095177514748));
#76541=CARTESIAN_POINT('Ctrl Pts',(201.878432316147,10.5931203647429,28.0931084541402));
#76542=CARTESIAN_POINT('Ctrl Pts',(201.88143304824,10.6468256224804,28.0797535041185));
#76543=CARTESIAN_POINT('Ctrl Pts',(201.884436527947,10.7005800553277,28.0663863256641));
#76544=CARTESIAN_POINT('Ctrl Pts',(201.887440007654,10.7550781501432,28.0560792091638));
#76545=CARTESIAN_POINT('Ctrl Pts',(201.89044348736,10.8099423194507,28.0488934125764));
#76546=CARTESIAN_POINT('Ctrl Pts',(201.893448346721,10.8648316907211,28.0417043151793));
#76547=CARTESIAN_POINT('Ctrl Pts',(201.896453206083,10.9200869446324,28.0376394345377));
#76548=CARTESIAN_POINT('Ctrl Pts',(201.899458065444,10.9753264438558,28.0367080039762));
#76549=CARTESIAN_POINT('Ctrl Pts',(201.902468523492,11.0306688659314,28.0357748379629));
#76550=CARTESIAN_POINT('Ctrl Pts',(201.905478981541,11.0859949463211,28.0379867630428));
#76551=CARTESIAN_POINT('Ctrl Pts',(201.908489439589,11.1409253196295,28.0433008875244));
#76552=CARTESIAN_POINT('Ctrl Pts',(201.910697039628,11.1812063307928,28.0471977899969));
#76553=CARTESIAN_POINT('Ctrl Pts',(201.912904639668,11.2212746142991,28.0527617795955));
#76554=CARTESIAN_POINT('Ctrl Pts',(201.915112239707,11.2609845343961,28.0599585690661));
#76555=CARTESIAN_POINT('Ctrl Pts',(201.918123577526,11.3151519479069,28.0697755485578));
#76556=CARTESIAN_POINT('Ctrl Pts',(201.921134915345,11.3688773621993,28.0826734691986));
#76557=CARTESIAN_POINT('Ctrl Pts',(201.924146253164,11.421784725125,28.098597168673));
#76558=CARTESIAN_POINT('Ctrl Pts',(201.927152278435,11.4745987498313,28.1144927758429));
#76559=CARTESIAN_POINT('Ctrl Pts',(201.930158303706,11.5265970860914,28.1334034173089));
#76560=CARTESIAN_POINT('Ctrl Pts',(201.933164328977,11.57741408551,28.1552229835937));
#76561=CARTESIAN_POINT('Ctrl Pts',(201.936167404565,11.6281812203981,28.1770211392788));
#76562=CARTESIAN_POINT('Ctrl Pts',(201.939170480153,11.677768832408,28.2017223579122));
#76563=CARTESIAN_POINT('Ctrl Pts',(201.942173555742,11.7258284418033,28.2291714029542));
#76564=CARTESIAN_POINT('Ctrl Pts',(201.945174867813,11.7738598288201,28.2566043289027));
#76565=CARTESIAN_POINT('Ctrl Pts',(201.948176179884,11.8203645345873,28.286781621612));
#76566=CARTESIAN_POINT('Ctrl Pts',(201.951177491955,11.8650181038493,28.3195018297291));
#76567=CARTESIAN_POINT('Ctrl Pts',(201.954178224047,11.9096630441817,28.3522157149391));
#76568=CARTESIAN_POINT('Ctrl Pts',(201.95717895614,11.952457133182,28.3874712278554));
#76569=CARTESIAN_POINT('Ctrl Pts',(201.960179688233,11.9931062963205,28.4250245890214));
#76570=CARTESIAN_POINT('Ctrl Pts',(201.96318316794,12.0337926797825,28.4626123358461));
#76571=CARTESIAN_POINT('Ctrl Pts',(201.966186647646,12.072329825509,28.5025017754049));
#76572=CARTESIAN_POINT('Ctrl Pts',(201.969190127353,12.1084592176021,28.5444109602381));
#76573=CARTESIAN_POINT('Ctrl Pts',(201.972194986714,12.1446052058017,28.5863393961369));
#76574=CARTESIAN_POINT('Ctrl Pts',(201.975199846075,12.1783409138953,28.6302890074987));
#76575=CARTESIAN_POINT('Ctrl Pts',(201.978204705437,12.2094490837466,28.6759458975137));
#76576=CARTESIAN_POINT('Ctrl Pts',(201.981215163485,12.2406152146876,28.7216878559564));
#76577=CARTESIAN_POINT('Ctrl Pts',(201.984225621534,12.2691437557156,28.7691429940413));
#76578=CARTESIAN_POINT('Ctrl Pts',(201.987236079582,12.2948622613818,28.8179706941419));
#76579=CARTESIAN_POINT('Ctrl Pts',(201.989443679622,12.3137219077204,28.8537765518919));
#76580=CARTESIAN_POINT('Ctrl Pts',(201.991651279661,12.3310714291689,28.8903199429348));
#76581=CARTESIAN_POINT('Ctrl Pts',(201.9938588797,12.3468595199812,28.9274603215182));
#76582=CARTESIAN_POINT('Ctrl Pts',(201.996870217519,12.3683957014059,28.9781226809425));
#76583=CARTESIAN_POINT('Ctrl Pts',(201.999881555338,12.3871141977066,29.0301072401307));
#76584=CARTESIAN_POINT('Ctrl Pts',(202.002892893157,12.4028546381928,29.0830694133301));
#76585=CARTESIAN_POINT('Ctrl Pts',(202.005898918428,12.4185673096767,29.1359381516147));
#76586=CARTESIAN_POINT('Ctrl Pts',(202.008904943699,12.4313122028411,29.1897805794268));
#76587=CARTESIAN_POINT('Ctrl Pts',(202.01191096897,12.4409772400928,29.2442328333534));
#76588=CARTESIAN_POINT('Ctrl Pts',(202.014914044558,12.4506327934602,29.298631655631));
#76589=CARTESIAN_POINT('Ctrl Pts',(202.017917120147,12.4572143861445,29.3536386015974));
#76590=CARTESIAN_POINT('Ctrl Pts',(202.020920195735,12.4606604267649,29.4088771835215));
#76591=CARTESIAN_POINT('Ctrl Pts',(202.023921507806,12.4641044437429,29.4640833273092));
#76592=CARTESIAN_POINT('Ctrl Pts',(202.026922819877,12.4644165256822,29.5195203118828));
#76593=CARTESIAN_POINT('Ctrl Pts',(202.029924131948,12.4615868976476,29.5748063541742));
#76594=CARTESIAN_POINT('Ctrl Pts',(202.032924864041,12.458757816415,29.6300817128994));
#76595=CARTESIAN_POINT('Ctrl Pts',(202.035925596133,12.4527882580257,29.6852056606625));
#76596=CARTESIAN_POINT('Ctrl Pts',(202.038926328226,12.4437205054879,29.7397985655371));
#76597=CARTESIAN_POINT('Ctrl Pts',(202.041929807933,12.4346444500811,29.7944414582938));
#76598=CARTESIAN_POINT('Ctrl Pts',(202.044933287639,12.4224646198972,29.8485518152115));
#76599=CARTESIAN_POINT('Ctrl Pts',(202.047936767346,12.4072747219128,29.9017587672537));
#76600=CARTESIAN_POINT('Ctrl Pts',(202.050941626707,12.3920778464193,29.9549901600128));
#76601=CARTESIAN_POINT('Ctrl Pts',(202.053946486068,12.373868320616,30.0073168215674));
#76602=CARTESIAN_POINT('Ctrl Pts',(202.056951345429,12.3527892071491,30.0583848234157));
#76603=CARTESIAN_POINT('Ctrl Pts',(202.059961803478,12.3316708188424,30.1095479757358));
#76604=CARTESIAN_POINT('Ctrl Pts',(202.062972261527,12.3076723919677,30.1594473073083));
#76605=CARTESIAN_POINT('Ctrl Pts',(202.065982719575,12.2809839267766,30.2077516720857));
#76606=CARTESIAN_POINT('Ctrl Pts',(202.068190319614,12.2614129990811,30.2431737626279));
#76607=CARTESIAN_POINT('Ctrl Pts',(202.070397919654,12.2403965064129,30.2777386633128));
#76608=CARTESIAN_POINT('Ctrl Pts',(202.072605519693,12.2180237448525,30.3113263258243));
#76609=CARTESIAN_POINT('Ctrl Pts',(202.075616857512,12.1875055613897,30.3571425047454));
#76610=CARTESIAN_POINT('Ctrl Pts',(202.078628195331,12.1543352314198,30.4013296715185));
#76611=CARTESIAN_POINT('Ctrl Pts',(202.08163953315,12.1187127014353,30.4435645932565));
#76612=CARTESIAN_POINT('Ctrl Pts',(202.084645558421,12.0831530160784,30.4857250049041));
#76613=CARTESIAN_POINT('Ctrl Pts',(202.087651583692,12.0451500536704,30.5259396065147));
#76614=CARTESIAN_POINT('Ctrl Pts',(202.090657608963,12.0049463883838,30.5639149432518));
#76615=CARTESIAN_POINT('Ctrl Pts',(202.093660684551,11.9647821732205,30.6018530164282));
#76616=CARTESIAN_POINT('Ctrl Pts',(202.096663760139,11.9224219148628,30.6375558171404));
#76617=CARTESIAN_POINT('Ctrl Pts',(202.099666835728,11.8781464585529,30.6707651546451));
#76618=CARTESIAN_POINT('Ctrl Pts',(202.102668147799,11.8338970024269,30.7039549903997));
#76619=CARTESIAN_POINT('Ctrl Pts',(202.10566945987,11.7877349988977,30.7346539494039));
#76620=CARTESIAN_POINT('Ctrl Pts',(202.108670771941,11.7399741692062,30.7626442408325));
#76621=CARTESIAN_POINT('Ctrl Pts',(202.111671504034,11.6922225688966,30.7906291233709));
#76622=CARTESIAN_POINT('Ctrl Pts',(202.114672236126,11.642873211028,30.8159061113701));
#76623=CARTESIAN_POINT('Ctrl Pts',(202.117672968219,11.5922666017872,30.8383021043126));
#76624=CARTESIAN_POINT('Ctrl Pts',(202.120676447926,11.5416136547077,30.8607186041003));
#76625=CARTESIAN_POINT('Ctrl Pts',(202.123679927632,11.4897016399509,30.8802486249136));
#76626=CARTESIAN_POINT('Ctrl Pts',(202.126683407339,11.4368919745653,30.8967668569093));
#76627=CARTESIAN_POINT('Ctrl Pts',(202.1296882667,11.3840580509573,30.9132926765871));
#76628=CARTESIAN_POINT('Ctrl Pts',(202.132693126061,11.3303261672975,30.9268038207952));
#76629=CARTESIAN_POINT('Ctrl Pts',(202.135697985423,11.2760706811343,30.9372255317166));
#76630=CARTESIAN_POINT('Ctrl Pts',(202.138708443471,11.2217141055429,30.9476666604862));
#76631=CARTESIAN_POINT('Ctrl Pts',(202.14171890152,11.1668325028109,30.9550067875569));
#76632=CARTESIAN_POINT('Ctrl Pts',(202.144729359568,11.1118069607444,30.9592228937106));
#76633=CARTESIAN_POINT('Ctrl Pts',(202.146936959608,11.0714561613462,30.9623146079811));
#76634=CARTESIAN_POINT('Ctrl Pts',(202.149144559647,11.0310280885006,30.9637274948763));
#76635=CARTESIAN_POINT('Ctrl Pts',(202.151352159686,10.990672105428,30.9634702731463));
#76636=CARTESIAN_POINT('Ctrl Pts',(202.154363497505,10.9356234118671,30.9631194027396));
#76637=CARTESIAN_POINT('Ctrl Pts',(202.157374835324,10.8804800383442,30.9596574879137));
#76638=CARTESIAN_POINT('Ctrl Pts',(202.160386173143,10.8256219200354,30.9530741671463));
#76639=CARTESIAN_POINT('Ctrl Pts',(202.163392198414,10.7708605814337,30.9465024605551));
#76640=CARTESIAN_POINT('Ctrl Pts',(202.166398223685,10.7163840190019,30.9368203388821));
#76641=CARTESIAN_POINT('Ctrl Pts',(202.169404248956,10.6625706849657,30.9240694180255));
#76642=CARTESIAN_POINT('Ctrl Pts',(202.172407324544,10.6088101556342,30.9113310090978));
#76643=CARTESIAN_POINT('Ctrl Pts',(202.175410400133,10.5557120763433,30.8955298875416));
#76644=CARTESIAN_POINT('Ctrl Pts',(202.178413475721,10.5036464391887,30.8767590176461));
#76645=CARTESIAN_POINT('Ctrl Pts',(202.181414787792,10.4516113769001,30.8579991706991));
#76646=CARTESIAN_POINT('Ctrl Pts',(202.184416099863,10.4006080503334,30.8362732108151));
#76647=CARTESIAN_POINT('Ctrl Pts',(202.187417411934,10.3509907368055,30.8117237614253));
#76648=CARTESIAN_POINT('Ctrl Pts',(202.190418144027,10.3013830114092,30.7871790560117));
#76649=CARTESIAN_POINT('Ctrl Pts',(202.193418876119,10.2531612396853,30.7598121786561));
#76650=CARTESIAN_POINT('Ctrl Pts',(202.196419608212,10.2066570539907,30.7298126767997));
#76651=CARTESIAN_POINT('Ctrl Pts',(202.199423087919,10.1601102868333,30.6997857059606));
#76652=CARTESIAN_POINT('Ctrl Pts',(202.202426567625,10.1152846918199,30.6671215815921));
#76653=CARTESIAN_POINT('Ctrl Pts',(202.205430047332,10.0724834398953,30.6320535679602));
#76654=CARTESIAN_POINT('Ctrl Pts',(202.208434906693,10.0296625271324,30.5969694457681));
#76655=CARTESIAN_POINT('Ctrl Pts',(202.211439766054,9.98886820018554,30.559479590762));
#76656=CARTESIAN_POINT('Ctrl Pts',(202.214444625415,9.95036848450246,30.5198558386725));
#76657=CARTESIAN_POINT('Ctrl Pts',(202.217455083464,9.91179703571885,30.4801582591652));
#76658=CARTESIAN_POINT('Ctrl Pts',(202.220465541513,9.87552908468643,30.4383192401548));
#76659=CARTESIAN_POINT('Ctrl Pts',(202.223475999561,9.84179310985319,30.3946446499122));
#76660=CARTESIAN_POINT('Ctrl Pts',(202.2256835996,9.81705417041017,30.3626176209453));
#76661=CARTESIAN_POINT('Ctrl Pts',(202.227891199639,9.79367594071422,30.3296042342714));
#76662=CARTESIAN_POINT('Ctrl Pts',(202.230098799678,9.77173314285901,30.2957341124075));
#76663=CARTESIAN_POINT('Ctrl Pts',(202.233170214418,9.74120431899568,30.248610906359));
#76664=CARTESIAN_POINT('Ctrl Pts',(202.236241629157,9.71333265900746,30.199638446855));
#76665=CARTESIAN_POINT('Ctrl Pts',(202.239313043896,9.68834143141664,30.1491410089201));
#76666=CARTESIAN_POINT('Ctrl Pts',(202.242377749617,9.6634047931973,30.0987538746264));
#76667=CARTESIAN_POINT('Ctrl Pts',(202.245442455338,9.64133630392324,30.0468488253206));
#76668=CARTESIAN_POINT('Ctrl Pts',(202.248507161059,9.62231482382211,29.993777080614));
#76669=CARTESIAN_POINT('Ctrl Pts',(202.251567901762,9.60331795310428,29.9407739984353));
#76670=CARTESIAN_POINT('Ctrl Pts',(202.254628642465,9.58736043913028,29.886607682295));
#76671=CARTESIAN_POINT('Ctrl Pts',(202.257689383168,9.57457370771792,29.8316506222985));
#76672=CARTESIAN_POINT('Ctrl Pts',(202.260747068025,9.5617997425851,29.7767484314603));
#76673=CARTESIAN_POINT('Ctrl Pts',(202.263804752883,9.5521903894846,29.7210575485588));
#76674=CARTESIAN_POINT('Ctrl Pts',(202.26686243774,9.5458271156249,29.6649650640232));
#76675=CARTESIAN_POINT('Ctrl Pts',(202.269856609879,9.53959601654511,29.6100377048558));
#76676=CARTESIAN_POINT('Ctrl Pts',(202.272850782018,9.53647746167809,29.5547257397934));
#76677=CARTESIAN_POINT('Ctrl Pts',(202.275844954157,9.53650012276609,29.4994005533173));
#76678=CARTESIAN_POINT('',(202.775844954126,9.53650011397254,29.4994224209001));
#76679=CARTESIAN_POINT('Ctrl Pts',(202.275844954211,9.53650012276649,29.4994005523254));
#76680=CARTESIAN_POINT('Ctrl Pts',(202.279119309422,9.53652490443265,29.4388982484398));
#76681=CARTESIAN_POINT('Ctrl Pts',(202.282393664633,9.540305713722,29.3785134960796));
#76682=CARTESIAN_POINT('Ctrl Pts',(202.285668019843,9.5477739722089,29.3186941418319));
#76683=CARTESIAN_POINT('Ctrl Pts',(202.288952785623,9.5552659754678,29.2586845963996));
#76684=CARTESIAN_POINT('Ctrl Pts',(202.292237551403,9.566468768621,29.1992443913266));
#76685=CARTESIAN_POINT('Ctrl Pts',(202.295522317182,9.58126302198713,29.1408097478788));
#76686=CARTESIAN_POINT('Ctrl Pts',(202.298821265787,9.59612115336547,29.0821227977566));
#76687=CARTESIAN_POINT('Ctrl Pts',(202.302120214392,9.61460166204428,29.0244504401604));
#76688=CARTESIAN_POINT('Ctrl Pts',(202.305419162996,9.63653552964663,28.9682134938869));
#76689=CARTESIAN_POINT('Ctrl Pts',(202.306561255221,9.64412900946451,28.9487443275598));
#76690=CARTESIAN_POINT('Ctrl Pts',(202.307703347446,9.65213597693153,28.9294469932177));
#76691=CARTESIAN_POINT('Ctrl Pts',(202.308845439671,9.66054814145892,28.9103382591258));
#76692=CARTESIAN_POINT('Ctrl Pts',(202.31185677749,9.6827283722935,28.8599545401987));
#76693=CARTESIAN_POINT('Ctrl Pts',(202.314868115309,9.70780147747075,28.8107192287392));
#76694=CARTESIAN_POINT('Ctrl Pts',(202.317879453128,9.73562610566513,28.762985139007));
#76695=CARTESIAN_POINT('Ctrl Pts',(202.3208854784,9.76340164615013,28.7153352608988));
#76696=CARTESIAN_POINT('Ctrl Pts',(202.323891503671,9.79391881258575,28.669181800712));
#76697=CARTESIAN_POINT('Ctrl Pts',(202.326897528942,9.82698913822091,28.6248555729776));
#76698=CARTESIAN_POINT('Ctrl Pts',(202.32990060453,9.86002701337135,28.5805728406595));
#76699=CARTESIAN_POINT('Ctrl Pts',(202.332903680118,9.89561277061498,28.5381142096381));
#76700=CARTESIAN_POINT('Ctrl Pts',(202.335906755706,9.9335141755226,28.4977823409115));
#76701=CARTESIAN_POINT('Ctrl Pts',(202.338908067777,9.97139332332479,28.4574741565486));
#76702=CARTESIAN_POINT('Ctrl Pts',(202.341909379848,10.0115850627582,28.4192906426313));
#76703=CARTESIAN_POINT('Ctrl Pts',(202.344910691919,10.0538178226943,28.3835003191451));
#76704=CARTESIAN_POINT('Ctrl Pts',(202.347911424012,10.0960424215021,28.3477169118402));
#76705=CARTESIAN_POINT('Ctrl Pts',(202.350912156104,10.1403068551407,28.3143261173153));
#76706=CARTESIAN_POINT('Ctrl Pts',(202.353912888197,10.1863054778245,28.2835570401447));
#76707=CARTESIAN_POINT('Ctrl Pts',(202.356916367904,10.2323462190534,28.2527597893313));
#76708=CARTESIAN_POINT('Ctrl Pts',(202.359919847611,10.2801238820762,28.2245893455089));
#76709=CARTESIAN_POINT('Ctrl Pts',(202.362923327317,10.3293039995066,28.1992313330488));
#76710=CARTESIAN_POINT('Ctrl Pts',(202.365928186678,10.3785067079196,28.1738616723362));
#76711=CARTESIAN_POINT('Ctrl Pts',(202.368933046039,10.4291126722085,28.1513072333536));
#76712=CARTESIAN_POINT('Ctrl Pts',(202.371937905401,10.4807659797898,28.1317060687643));
#76713=CARTESIAN_POINT('Ctrl Pts',(202.374948363449,10.5325155283909,28.1120683830662));
#76714=CARTESIAN_POINT('Ctrl Pts',(202.377958821498,10.5853158140669,28.0953951225459));
#76715=CARTESIAN_POINT('Ctrl Pts',(202.380969279546,10.638795392514,28.0817745307847));
#76716=CARTESIAN_POINT('Ctrl Pts',(202.383176879585,10.6780125207929,28.0717864099011));
#76717=CARTESIAN_POINT('Ctrl Pts',(202.385384479625,10.7175946189491,28.0634387857504));
#76718=CARTESIAN_POINT('Ctrl Pts',(202.387592079664,10.7573930510406,28.0567487681223));
#76719=CARTESIAN_POINT('Ctrl Pts',(202.390603417483,10.8116812017825,28.0476230647622));
#76720=CARTESIAN_POINT('Ctrl Pts',(202.393614755302,10.8665978878447,28.0415457224413));
#76721=CARTESIAN_POINT('Ctrl Pts',(202.396626093121,10.9217706225594,28.0385923174879));
#76722=CARTESIAN_POINT('Ctrl Pts',(202.399632118392,10.9768460225262,28.0356441228786));
#76723=CARTESIAN_POINT('Ctrl Pts',(202.402638143663,11.0321760520258,28.0358089562565));
#76724=CARTESIAN_POINT('Ctrl Pts',(202.405644168934,11.0873807423092,28.0391109364933));
#76725=CARTESIAN_POINT('Ctrl Pts',(202.408647244522,11.1425312626101,28.0424096766393));
#76726=CARTESIAN_POINT('Ctrl Pts',(202.41165032011,11.1975561632272,28.0488394339358));
#76727=CARTESIAN_POINT('Ctrl Pts',(202.414653395699,11.2520749746903,28.0583722889959));
#76728=CARTESIAN_POINT('Ctrl Pts',(202.41765470777,11.3065617706927,28.0678995460113));
#76729=CARTESIAN_POINT('Ctrl Pts',(202.420656019841,11.3605425479361,28.0805261980597));
#76730=CARTESIAN_POINT('Ctrl Pts',(202.423657331912,11.4136437733348,28.0961727033636));
#76731=CARTESIAN_POINT('Ctrl Pts',(202.426658064004,11.4667347373648,28.111816185111));
#76732=CARTESIAN_POINT('Ctrl Pts',(202.429658796097,11.5189459813392,28.130478211984));
#76733=CARTESIAN_POINT('Ctrl Pts',(202.43265952819,11.5699182059822,28.1520291217945));
#76734=CARTESIAN_POINT('Ctrl Pts',(202.435663007897,11.6209371032389,28.1735997646518));
#76735=CARTESIAN_POINT('Ctrl Pts',(202.438666487603,11.6707142277645,28.1980643689411));
#76736=CARTESIAN_POINT('Ctrl Pts',(202.44166996731,11.7189107956159,28.2252453106786));
#76737=CARTESIAN_POINT('Ctrl Pts',(202.444674826671,11.7671295026545,28.2524387380345));
#76738=CARTESIAN_POINT('Ctrl Pts',(202.447679686032,11.8137657609265,28.2823507047672));
#76739=CARTESIAN_POINT('Ctrl Pts',(202.450684545394,11.8585087715102,28.3147595437043));
#76740=CARTESIAN_POINT('Ctrl Pts',(202.453695003442,11.9033351477711,28.3472287671522));
#76741=CARTESIAN_POINT('Ctrl Pts',(202.456705461491,11.9462608200782,28.3822038217028));
#76742=CARTESIAN_POINT('Ctrl Pts',(202.459715919539,11.9870080913358,28.4194227109375));
#76743=CARTESIAN_POINT('Ctrl Pts',(202.461923519578,12.0168884869997,28.4467157075525));
#76744=CARTESIAN_POINT('Ctrl Pts',(202.464131119618,12.0455981711185,28.4752144682489));
#76745=CARTESIAN_POINT('Ctrl Pts',(202.466338719657,12.0730412338316,28.5048041597267));
#76746=CARTESIAN_POINT('Ctrl Pts',(202.469350057476,12.1104757016507,28.545166795814));
#76747=CARTESIAN_POINT('Ctrl Pts',(202.472361395295,12.1457074999546,28.5877284791222));
#76748=CARTESIAN_POINT('Ctrl Pts',(202.475372733114,12.1784689464185,28.6322193869835));
#76749=CARTESIAN_POINT('Ctrl Pts',(202.478378758385,12.2111725957268,28.676631804784));
#76750=CARTESIAN_POINT('Ctrl Pts',(202.481384783656,12.2414142319036,28.7229662711761));
#76751=CARTESIAN_POINT('Ctrl Pts',(202.484390808927,12.2689650718549,28.7709184569527));
#76752=CARTESIAN_POINT('Ctrl Pts',(202.487393884516,12.2964888773549,28.8188235893169));
#76753=CARTESIAN_POINT('Ctrl Pts',(202.490396960104,12.3213268557498,28.8683428410891));
#76754=CARTESIAN_POINT('Ctrl Pts',(202.493400035692,12.343293441774,28.9191428925398));
#76755=CARTESIAN_POINT('Ctrl Pts',(202.496401347763,12.3652471282072,28.9699131123232));
#76756=CARTESIAN_POINT('Ctrl Pts',(202.499402659834,12.3843325556044,29.0219621576059));
#76757=CARTESIAN_POINT('Ctrl Pts',(202.502403971905,12.4004111123555,29.0749341622865));
#76758=CARTESIAN_POINT('Ctrl Pts',(202.505404703998,12.4164865620598,29.1278959305692));
#76759=CARTESIAN_POINT('Ctrl Pts',(202.50840543609,12.4295561420746,29.1817797994226));
#76760=CARTESIAN_POINT('Ctrl Pts',(202.511406168183,12.439530945825,29.2362142801208));
#76761=CARTESIAN_POINT('Ctrl Pts',(202.51440964789,12.4495148829841,29.2906986036403));
#76762=CARTESIAN_POINT('Ctrl Pts',(202.517413127597,12.4563982875769,29.3457340261452));
#76763=CARTESIAN_POINT('Ctrl Pts',(202.520416607303,12.4601436028484,29.4009398714872));
#76764=CARTESIAN_POINT('Ctrl Pts',(202.523421466664,12.4638906385377,29.4561710757416));
#76765=CARTESIAN_POINT('Ctrl Pts',(202.526426326026,12.4644967056998,29.5115723304389));
#76766=CARTESIAN_POINT('Ctrl Pts',(202.529431185387,12.4619764235825,29.5667621665992));
#76767=CARTESIAN_POINT('Ctrl Pts',(202.532441643435,12.4594514456473,29.622054833079));
#76768=CARTESIAN_POINT('Ctrl Pts',(202.535452101484,12.4537885368043,29.6771347681487));
#76769=CARTESIAN_POINT('Ctrl Pts',(202.538462559532,12.4450541976733,29.7316260257114));
#76770=CARTESIAN_POINT('Ctrl Pts',(202.540670159572,12.4386492164061,29.7715850287537));
#76771=CARTESIAN_POINT('Ctrl Pts',(202.542877759611,12.4305936879302,29.8112276041533));
#76772=CARTESIAN_POINT('Ctrl Pts',(202.54508535965,12.4209309280141,29.8504105418118));
#76773=CARTESIAN_POINT('Ctrl Pts',(202.548096697469,12.4077501734128,29.9038591103702));
#76774=CARTESIAN_POINT('Ctrl Pts',(202.551108035288,12.3915220963785,29.956674127302));
#76775=CARTESIAN_POINT('Ctrl Pts',(202.554119373107,12.3723252372777,30.0084837196318));
#76776=CARTESIAN_POINT('Ctrl Pts',(202.557125398378,12.3531622449311,30.0602019104091));
#76777=CARTESIAN_POINT('Ctrl Pts',(202.560131423649,12.3310410465083,30.1109177059251));
#76778=CARTESIAN_POINT('Ctrl Pts',(202.56313744892,12.3060903803334,30.1602727984708));
#76779=CARTESIAN_POINT('Ctrl Pts',(202.566140524508,12.2811641971715,30.2095794609921));
#76780=CARTESIAN_POINT('Ctrl Pts',(202.569143600096,12.2534142833967,30.2575275970591));
#76781=CARTESIAN_POINT('Ctrl Pts',(202.572146675685,12.2230173362518,30.3037791022586));
#76782=CARTESIAN_POINT('Ctrl Pts',(202.575147987756,12.1926382393175,30.3500034468651));
#76783=CARTESIAN_POINT('Ctrl Pts',(202.578149299827,12.1596154793837,30.3945326954565));
#76784=CARTESIAN_POINT('Ctrl Pts',(202.581150611898,12.1241703778796,30.4370556074738));
#76785=CARTESIAN_POINT('Ctrl Pts',(202.584151343991,12.0887321258455,30.4795703022931));
#76786=CARTESIAN_POINT('Ctrl Pts',(202.587152076083,12.0508727996188,30.520079025576));
#76787=CARTESIAN_POINT('Ctrl Pts',(202.590152808176,12.0108540687231,30.5583035017167));
#76788=CARTESIAN_POINT('Ctrl Pts',(202.593156287883,11.9707986947581,30.5965629780211));
#76789=CARTESIAN_POINT('Ctrl Pts',(202.596159767589,11.9285803484357,30.6325336636257));
#76790=CARTESIAN_POINT('Ctrl Pts',(202.599163247296,11.884496572017,30.6659751558632));
#76791=CARTESIAN_POINT('Ctrl Pts',(202.602168106657,11.84039254563,30.6994320095151));
#76792=CARTESIAN_POINT('Ctrl Pts',(202.605172966018,11.7944218195366,30.7303570589392));
#76793=CARTESIAN_POINT('Ctrl Pts',(202.608177825379,11.7469112462918,30.7585530740349));
#76794=CARTESIAN_POINT('Ctrl Pts',(202.611188283428,11.699312150816,30.7868016242611));
#76795=CARTESIAN_POINT('Ctrl Pts',(202.614198741477,11.6501679464801,30.8123107395737));
#76796=CARTESIAN_POINT('Ctrl Pts',(202.617209199525,11.5998293557888,30.834929583886));
#76797=CARTESIAN_POINT('Ctrl Pts',(202.619416799564,11.5629155463338,30.8515162164787));
#76798=CARTESIAN_POINT('Ctrl Pts',(202.621624399604,11.5253599557688,30.8665496106646));
#76799=CARTESIAN_POINT('Ctrl Pts',(202.623831999643,11.4873060597025,30.8799873384119));
#76800=CARTESIAN_POINT('Ctrl Pts',(202.626843337462,11.4353975915199,30.8983174421681));
#76801=CARTESIAN_POINT('Ctrl Pts',(202.629854675281,11.3823454786743,30.9137527853886));
#76802=CARTESIAN_POINT('Ctrl Pts',(202.6328660131,11.3285036499403,30.9261548309969));
#76803=CARTESIAN_POINT('Ctrl Pts',(202.635872038371,11.2747568079937,30.9385349971391));
#76804=CARTESIAN_POINT('Ctrl Pts',(202.638878063642,11.220223525117,30.9478923681986));
#76805=CARTESIAN_POINT('Ctrl Pts',(202.641884088913,11.1652739540451,30.9541378098771));
#76806=CARTESIAN_POINT('Ctrl Pts',(202.644887164501,11.1103783026181,30.960377123173));
#76807=CARTESIAN_POINT('Ctrl Pts',(202.647890240089,11.0550676939211,30.9635104971319));
#76808=CARTESIAN_POINT('Ctrl Pts',(202.650893315678,10.9997217273275,30.9634999735444));
#76809=CARTESIAN_POINT('Ctrl Pts',(202.653894627749,10.9444082619306,30.9634894561367));
#76810=CARTESIAN_POINT('Ctrl Pts',(202.65689593982,10.889060006361,30.9603387008083));
#76811=CARTESIAN_POINT('Ctrl Pts',(202.659897251891,10.8340586088789,30.9540617953556));
#76812=CARTESIAN_POINT('Ctrl Pts',(202.662897983983,10.7790678399578,30.9477861028625));
#76813=CARTESIAN_POINT('Ctrl Pts',(202.665898716076,10.7244243198954,30.9383855199263));
#76814=CARTESIAN_POINT('Ctrl Pts',(202.668899448169,10.6705042988143,30.9259259563176));
#76815=CARTESIAN_POINT('Ctrl Pts',(202.671902927875,10.6165349059757,30.9134549841348));
#76816=CARTESIAN_POINT('Ctrl Pts',(202.674906407582,10.5632908506835,30.8979195547848));
#76817=CARTESIAN_POINT('Ctrl Pts',(202.677909887289,10.5111364256746,30.8794363543483));
#76818=CARTESIAN_POINT('Ctrl Pts',(202.68091474665,10.4589580434292,30.8609446636178));
#76819=CARTESIAN_POINT('Ctrl Pts',(202.683919606011,10.4078707764935,30.8395027071667));
#76820=CARTESIAN_POINT('Ctrl Pts',(202.686924465372,10.3582189277104,30.8152753724034));
#76821=CARTESIAN_POINT('Ctrl Pts',(202.689934923421,10.3084745670478,30.7910028969992));
#76822=CARTESIAN_POINT('Ctrl Pts',(202.692945381469,10.2601714281986,30.7639349351043));
#76823=CARTESIAN_POINT('Ctrl Pts',(202.695955839518,10.2136281446128,30.734281797263));
#76824=CARTESIAN_POINT('Ctrl Pts',(202.698163439557,10.1794974731306,30.7125368444342));
#76825=CARTESIAN_POINT('Ctrl Pts',(202.700371039596,10.1463125986136,30.6894026829662));
#76826=CARTESIAN_POINT('Ctrl Pts',(202.702578639635,10.1141877581856,30.6649759320483));
#76827=CARTESIAN_POINT('Ctrl Pts',(202.705631402739,10.0697641643131,30.631197583333));
#76828=CARTESIAN_POINT('Ctrl Pts',(202.708684165843,10.0271717147639,30.5947955506121));
#76829=CARTESIAN_POINT('Ctrl Pts',(202.711736928947,9.98673924406939,30.5559994746641));
#76830=CARTESIAN_POINT('Ctrl Pts',(202.714713719638,9.94731299372029,30.5181688950183));
#76831=CARTESIAN_POINT('Ctrl Pts',(202.717690510329,9.90994088495104,30.4780624372868));
#76832=CARTESIAN_POINT('Ctrl Pts',(202.72066730102,9.87489692336547,30.4359355303372));
#76833=CARTESIAN_POINT('Ctrl Pts',(202.723641242856,9.83988649963546,30.3938489397803));
#76834=CARTESIAN_POINT('Ctrl Pts',(202.726615184692,9.80720015500378,30.3497461406315));
#76835=CARTESIAN_POINT('Ctrl Pts',(202.729589126528,9.77707437246157,30.3039186274181));
#76836=CARTESIAN_POINT('Ctrl Pts',(202.732561452323,9.74696496027342,30.2581160168811));
#76837=CARTESIAN_POINT('Ctrl Pts',(202.735533778119,9.7194136488174,30.2105909989348));
#76838=CARTESIAN_POINT('Ctrl Pts',(202.738506103914,9.69461451188773,30.1616653061978));
#76839=CARTESIAN_POINT('Ctrl Pts',(202.741617674765,9.66865360554443,30.1104475831567));
#76840=CARTESIAN_POINT('Ctrl Pts',(202.744729245616,9.64570947287336,30.0576952307279));
#76841=CARTESIAN_POINT('Ctrl Pts',(202.747840816467,9.62595032668182,30.0038052652109));
#76842=CARTESIAN_POINT('Ctrl Pts',(202.75081544914,9.60706076746592,29.9522869614892));
#76843=CARTESIAN_POINT('Ctrl Pts',(202.753790081812,9.59108180910761,29.8997296520723));
#76844=CARTESIAN_POINT('Ctrl Pts',(202.756764714485,9.57810963351725,29.8464968047523));
#76845=CARTESIAN_POINT('Ctrl Pts',(202.759741049455,9.5651300343211,29.7932334937933));
#76846=CARTESIAN_POINT('Ctrl Pts',(202.762717384425,9.55516073709183,29.7392944060208));
#76847=CARTESIAN_POINT('Ctrl Pts',(202.765693719395,9.54824655854444,29.6850518717061));
#76848=CARTESIAN_POINT('Ctrl Pts',(202.768674770717,9.54132142366917,29.6307233837258));
#76849=CARTESIAN_POINT('Ctrl Pts',(202.77165582204,9.53746109245465,29.5760910270364));
#76850=CARTESIAN_POINT('Ctrl Pts',(202.774636873362,9.5366583622647,29.5215290796404));
#76851=CARTESIAN_POINT('Ctrl Pts',(202.77503956695,9.53654992592277,29.5141586106361));
#76852=CARTESIAN_POINT('Ctrl Pts',(202.775442260538,9.53649720654187,29.5067894195638));
#76853=CARTESIAN_POINT('Ctrl Pts',(202.775844954126,9.53650011397254,29.4994224209001));
#76854=CARTESIAN_POINT('',(203.275844954122,9.53650053107307,29.5012467760758));
#76855=CARTESIAN_POINT('Ctrl Pts',(202.775844954157,9.53650011397276,29.499422420335));
#76856=CARTESIAN_POINT('Ctrl Pts',(202.777671729314,9.53651330322503,29.4660028414331));
#76857=CARTESIAN_POINT('Ctrl Pts',(202.779498504471,9.537671130685,29.4326074630415));
#76858=CARTESIAN_POINT('Ctrl Pts',(202.781325279628,9.53996915343813,29.3992916235468));
#76859=CARTESIAN_POINT('Ctrl Pts',(202.784336617447,9.54375731685769,29.3443723046266));
#76860=CARTESIAN_POINT('Ctrl Pts',(202.787347955266,9.55065636465342,29.2895527858654));
#76861=CARTESIAN_POINT('Ctrl Pts',(202.790359293085,9.56065290987794,29.2352129078728));
#76862=CARTESIAN_POINT('Ctrl Pts',(202.793365318356,9.57063181937689,29.1809688953172));
#76863=CARTESIAN_POINT('Ctrl Pts',(202.796371343627,9.58369728681845,29.1272033590048));
#76864=CARTESIAN_POINT('Ctrl Pts',(202.799377368898,9.59978414191605,29.0742914133234));
#76865=CARTESIAN_POINT('Ctrl Pts',(202.802380444486,9.61585521167632,29.0214313878529));
#76866=CARTESIAN_POINT('Ctrl Pts',(202.805383520074,9.63494164303026,28.9694237960519));
#76867=CARTESIAN_POINT('Ctrl Pts',(202.808386595662,9.6569275459023,28.9186321018116));
#76868=CARTESIAN_POINT('Ctrl Pts',(202.811387907734,9.6789005378398,28.8678702343309));
#76869=CARTESIAN_POINT('Ctrl Pts',(202.814389219805,9.70376941710798,28.8183233323324));
#76870=CARTESIAN_POINT('Ctrl Pts',(202.817390531876,9.73136971287122,28.7703360742235));
#76871=CARTESIAN_POINT('Ctrl Pts',(202.820391263969,9.75896467510764,28.7223580892518));
#76872=CARTESIAN_POINT('Ctrl Pts',(202.823391996061,9.789289742555,28.675939606633));
#76873=CARTESIAN_POINT('Ctrl Pts',(202.826392728154,9.8221350262239,28.6313997734565));
#76874=CARTESIAN_POINT('Ctrl Pts',(202.829396207861,9.85501038460989,28.5868191574724));
#76875=CARTESIAN_POINT('Ctrl Pts',(202.832399687568,9.89041025543968,28.544121052898));
#76876=CARTESIAN_POINT('Ctrl Pts',(202.835403167275,9.92808289575131,28.5035934707063));
#76877=CARTESIAN_POINT('Ctrl Pts',(202.838408026636,9.96577284106353,28.463047272091));
#76878=CARTESIAN_POINT('Ctrl Pts',(202.841412885997,10.0057372557433,28.4246739493435));
#76879=CARTESIAN_POINT('Ctrl Pts',(202.844417745358,10.047688095616,28.3887240276292));
#76880=CARTESIAN_POINT('Ctrl Pts',(202.847428203407,10.0897170987624,28.3527071236191));
#76881=CARTESIAN_POINT('Ctrl Pts',(202.850438661455,10.1337394998062,28.3191229608318));
#76882=CARTESIAN_POINT('Ctrl Pts',(202.853449119504,10.1794357583125,28.2881804691854));
#76883=CARTESIAN_POINT('Ctrl Pts',(202.855656719543,10.2129452975408,28.2654900198677));
#76884=CARTESIAN_POINT('Ctrl Pts',(202.857864319583,10.2473542880417,28.2442192254203));
#76885=CARTESIAN_POINT('Ctrl Pts',(202.860071919622,10.2825286936883,28.2244345667041));
#76886=CARTESIAN_POINT('Ctrl Pts',(202.863083257441,10.3305093134119,28.1974467564263));
#76887=CARTESIAN_POINT('Ctrl Pts',(202.86609459526,10.380114578031,28.1731137701796));
#76888=CARTESIAN_POINT('Ctrl Pts',(202.869105933079,10.4310196725613,28.1516329739319));
#76889=CARTESIAN_POINT('Ctrl Pts',(202.87211195835,10.481834961238,28.1301900737191));
#76890=CARTESIAN_POINT('Ctrl Pts',(202.875117983621,10.5339450467044,28.1115895810636));
#76891=CARTESIAN_POINT('Ctrl Pts',(202.878124008892,10.5870006320155,28.0959829872668));
#76892=CARTESIAN_POINT('Ctrl Pts',(202.88112708448,10.6400041561682,28.0803917075476));
#76893=CARTESIAN_POINT('Ctrl Pts',(202.884130160068,10.6939508384774,28.0677886549604));
#76894=CARTESIAN_POINT('Ctrl Pts',(202.887133235656,10.7484732711875,28.05827653321));
#76895=CARTESIAN_POINT('Ctrl Pts',(202.890134547727,10.8029636863104,28.048769997329));
#76896=CARTESIAN_POINT('Ctrl Pts',(202.893135859798,10.8580286629236,28.0423508849124));
#76897=CARTESIAN_POINT('Ctrl Pts',(202.896137171869,10.9132898202213,28.039070982312));
#76898=CARTESIAN_POINT('Ctrl Pts',(202.899137903961,10.9685402987615,28.0357917135255));
#76899=CARTESIAN_POINT('Ctrl Pts',(202.902138636054,11.0239863563091,28.0356504808928));
#76900=CARTESIAN_POINT('Ctrl Pts',(202.905139368146,11.0792460135248,28.0386470928142));
#76901=CARTESIAN_POINT('Ctrl Pts',(202.908142847853,11.1345562691331,28.0416464485772));
#76902=CARTESIAN_POINT('Ctrl Pts',(202.91114632756,11.1896792555139,28.0477893600535));
#76903=CARTESIAN_POINT('Ctrl Pts',(202.914149807266,11.244236036138,28.0570235592181));
#76904=CARTESIAN_POINT('Ctrl Pts',(202.917154666627,11.2988178775253,28.0662620001301));
#76905=CARTESIAN_POINT('Ctrl Pts',(202.920159525988,11.3528324794864,28.0785944416681));
#76906=CARTESIAN_POINT('Ctrl Pts',(202.923164385349,11.4059123040621,28.0939176939414));
#76907=CARTESIAN_POINT('Ctrl Pts',(202.926174843398,11.45909102756,28.1092694966696));
#76908=CARTESIAN_POINT('Ctrl Pts',(202.929185301446,11.5113309957098,28.1276230661159));
#76909=CARTESIAN_POINT('Ctrl Pts',(202.932195759495,11.5622821419246,28.1488260501058));
#76910=CARTESIAN_POINT('Ctrl Pts',(202.934403359534,11.5996451446931,28.1643744176769));
#76911=CARTESIAN_POINT('Ctrl Pts',(202.936610959574,11.6363154733947,28.181454005409));
#76912=CARTESIAN_POINT('Ctrl Pts',(202.938818559613,11.6721639707555,28.1999892898833));
#76913=CARTESIAN_POINT('Ctrl Pts',(202.941829897433,11.721064103903,28.2252728567117));
#76914=CARTESIAN_POINT('Ctrl Pts',(202.944841235252,11.7686374015785,28.2533719287005));
#76915=CARTESIAN_POINT('Ctrl Pts',(202.947852573072,11.814540566128,28.2841233960094));
#76916=CARTESIAN_POINT('Ctrl Pts',(202.950858598343,11.860362749139,28.3148206121318));
#76917=CARTESIAN_POINT('Ctrl Pts',(202.953864623614,11.9045202115577,28.3481606458421));
#76918=CARTESIAN_POINT('Ctrl Pts',(202.956870648886,11.9466945550314,28.383934737807));
#76919=CARTESIAN_POINT('Ctrl Pts',(202.959873724474,11.9888275146402,28.4196737261979));
#76920=CARTESIAN_POINT('Ctrl Pts',(202.962876800063,12.0289808099204,28.4578417015899));
#76921=CARTESIAN_POINT('Ctrl Pts',(202.965879875651,12.0668668745335,28.4981879806954));
#76922=CARTESIAN_POINT('Ctrl Pts',(202.968881187722,12.1047306910494,28.5385105669749));
#76923=CARTESIAN_POINT('Ctrl Pts',(202.971882499794,12.1403295555235,28.5810085375439));
#76924=CARTESIAN_POINT('Ctrl Pts',(202.974883811865,12.1734124326928,28.6253940814275));
#76925=CARTESIAN_POINT('Ctrl Pts',(202.977884543958,12.2064889168721,28.6697710481751));
#76926=CARTESIAN_POINT('Ctrl Pts',(202.980885276051,12.2370500643195,28.7160344409564));
#76927=CARTESIAN_POINT('Ctrl Pts',(202.983886008144,12.2648863063175,28.7638649022832));
#76928=CARTESIAN_POINT('Ctrl Pts',(202.986889487851,12.2927480365137,28.8117391594744));
#76929=CARTESIAN_POINT('Ctrl Pts',(202.989892967559,12.3178796108901,28.8611828947601));
#76930=CARTESIAN_POINT('Ctrl Pts',(202.992896447266,12.3401166560611,28.9118507008015));
#76931=CARTESIAN_POINT('Ctrl Pts',(202.995901306627,12.3623639158619,28.962541781198));
#76932=CARTESIAN_POINT('Ctrl Pts',(202.998906165989,12.3817138114823,29.014457557986));
#76933=CARTESIAN_POINT('Ctrl Pts',(203.00191102535,12.3980507877041,29.0672341915076));
#76934=CARTESIAN_POINT('Ctrl Pts',(203.004921483399,12.4144182031624,29.1201091590424));
#76935=CARTESIAN_POINT('Ctrl Pts',(203.007931941448,12.4277613582521,29.1738476740637));
#76936=CARTESIAN_POINT('Ctrl Pts',(203.010942399497,12.4380153796125,29.2280735062598));
#76937=CARTESIAN_POINT('Ctrl Pts',(203.013149999534,12.4455347595751,29.2678378700871));
#76938=CARTESIAN_POINT('Ctrl Pts',(203.01535759957,12.4513940516442,29.3078640367316));
#76939=CARTESIAN_POINT('Ctrl Pts',(203.017565199607,12.4555854622499,29.3480025918423));
#76940=CARTESIAN_POINT('Ctrl Pts',(203.020576537426,12.4613028716816,29.4027546968372));
#76941=CARTESIAN_POINT('Ctrl Pts',(203.023587875244,12.4639386166715,29.4579437296724));
#76942=CARTESIAN_POINT('Ctrl Pts',(203.026599213063,12.4634405314833,29.5131932108198));
#76943=CARTESIAN_POINT('Ctrl Pts',(203.029605238334,12.4629433250081,29.5683452218249));
#76944=CARTESIAN_POINT('Ctrl Pts',(203.032611263604,12.4593232650675,29.6235569461207));
#76945=CARTESIAN_POINT('Ctrl Pts',(203.035617288875,12.4525800102121,29.6784476503969));
#76946=CARTESIAN_POINT('Ctrl Pts',(203.038620364463,12.4458433722219,29.7332844927918));
#76947=CARTESIAN_POINT('Ctrl Pts',(203.04162344005,12.4359896745757,29.7878004180681));
#76948=CARTESIAN_POINT('Ctrl Pts',(203.044626515638,12.4230705437693,29.841617443138));
#76949=CARTESIAN_POINT('Ctrl Pts',(203.047627827709,12.4101589995539,29.8954028648623));
#76950=CARTESIAN_POINT('Ctrl Pts',(203.050629139779,12.3941857132844,29.9484896878859));
#76951=CARTESIAN_POINT('Ctrl Pts',(203.05363045185,12.3752533998737,30.0005100759584));
#76952=CARTESIAN_POINT('Ctrl Pts',(203.056631183942,12.3563247449745,30.052520411525));
#76953=CARTESIAN_POINT('Ctrl Pts',(203.059631916034,12.3344383790158,30.1034642259552));
#76954=CARTESIAN_POINT('Ctrl Pts',(203.062632648126,12.3097461505299,30.1529910192124));
#76955=CARTESIAN_POINT('Ctrl Pts',(203.065636127833,12.2850313126553,30.2025631615771));
#76956=CARTESIAN_POINT('Ctrl Pts',(203.068639607539,12.2575057156321,30.2507152175747));
#76957=CARTESIAN_POINT('Ctrl Pts',(203.071643087246,12.2273677949094,30.2971201578302));
#76958=CARTESIAN_POINT('Ctrl Pts',(203.074647946606,12.1972160302742,30.3435464142852));
#76959=CARTESIAN_POINT('Ctrl Pts',(203.077652805967,12.164449862477,30.3882235290813));
#76960=CARTESIAN_POINT('Ctrl Pts',(203.080657665328,12.1293099364181,30.4308551538812));
#76961=CARTESIAN_POINT('Ctrl Pts',(203.083668123376,12.0941045372562,30.473566210401));
#76962=CARTESIAN_POINT('Ctrl Pts',(203.086678581424,12.0565169040922,30.5142237757011));
#76963=CARTESIAN_POINT('Ctrl Pts',(203.089689039472,12.0168258650238,30.5525670573501));
#76964=CARTESIAN_POINT('Ctrl Pts',(203.091896639515,11.9877200153056,30.5806845826045));
#76965=CARTESIAN_POINT('Ctrl Pts',(203.094104239557,11.957483870211,30.6075583776143));
#76966=CARTESIAN_POINT('Ctrl Pts',(203.0963118396,11.926238028769,30.6330998914757));
#76967=CARTESIAN_POINT('Ctrl Pts',(203.099323177418,11.8836162756414,30.6679404989954));
#76968=CARTESIAN_POINT('Ctrl Pts',(203.102334515237,11.8389373322898,30.7004453989026));
#76969=CARTESIAN_POINT('Ctrl Pts',(203.105345853056,11.7924872123271,30.7303642827626));
#76970=CARTESIAN_POINT('Ctrl Pts',(203.108351878327,11.7461190388321,30.7602303842649));
#76971=CARTESIAN_POINT('Ctrl Pts',(203.111357903598,11.6979863298982,30.7875192403134));
#76972=CARTESIAN_POINT('Ctrl Pts',(203.114363928868,11.6484071089273,30.8120215208191));
#76973=CARTESIAN_POINT('Ctrl Pts',(203.117367004456,11.5988765379085,30.8364997582933));
#76974=CARTESIAN_POINT('Ctrl Pts',(203.120370080044,11.547902737463,30.8581966044755));
#76975=CARTESIAN_POINT('Ctrl Pts',(203.123373155632,11.4958299658219,30.8769476732952));
#76976=CARTESIAN_POINT('Ctrl Pts',(203.126374467702,11.4437877732366,30.8956877307943));
#76977=CARTESIAN_POINT('Ctrl Pts',(203.129375779773,11.3906483840938,30.9114852614432));
#76978=CARTESIAN_POINT('Ctrl Pts',(203.132377091844,11.3367756265677,30.9242241492651));
#76979=CARTESIAN_POINT('Ctrl Pts',(203.135377823936,11.2829132795026,30.9369605754033));
#76980=CARTESIAN_POINT('Ctrl Pts',(203.138378556028,11.2283183586918,30.9466394113539));
#76981=CARTESIAN_POINT('Ctrl Pts',(203.141379288121,11.1733671801888,30.9531951248313));
#76982=CARTESIAN_POINT('Ctrl Pts',(203.144382767827,11.1183656857512,30.9597568410343));
#76983=CARTESIAN_POINT('Ctrl Pts',(203.147386247534,11.0630078069323,30.9631896592757));
#76984=CARTESIAN_POINT('Ctrl Pts',(203.15038972724,11.0076758223022,30.9634798706344));
#76985=CARTESIAN_POINT('Ctrl Pts',(203.153394586601,10.9523184208174,30.9637702153022));
#76986=CARTESIAN_POINT('Ctrl Pts',(203.156399445962,10.8969874650048,30.9609151027594));
#76987=CARTESIAN_POINT('Ctrl Pts',(203.159404305322,10.8420627661499,30.9549529477491));
#76988=CARTESIAN_POINT('Ctrl Pts',(203.162414763371,10.7870357309823,30.9489796839849));
#76989=CARTESIAN_POINT('Ctrl Pts',(203.165425221419,10.7324169863944,30.939887900727));
#76990=CARTESIAN_POINT('Ctrl Pts',(203.168435679467,10.6785775914021,30.9277674478889));
#76991=CARTESIAN_POINT('Ctrl Pts',(203.170643279509,10.6390966058739,30.9188793943889));
#76992=CARTESIAN_POINT('Ctrl Pts',(203.172850879551,10.6000345125662,30.9083637777217));
#76993=CARTESIAN_POINT('Ctrl Pts',(203.175058479593,10.561531536798,30.8962727730559));
#76994=CARTESIAN_POINT('Ctrl Pts',(203.178069817415,10.5090104890604,30.8797797041287));
#76995=CARTESIAN_POINT('Ctrl Pts',(203.181081155236,10.4573120718238,30.8602848289508));
#76996=CARTESIAN_POINT('Ctrl Pts',(203.184092493058,10.4068025270114,30.8378897593001));
#76997=CARTESIAN_POINT('Ctrl Pts',(203.187098518332,10.3563820902308,30.815534198629));
#76998=CARTESIAN_POINT('Ctrl Pts',(203.190104543606,10.3071468419408,30.7902888096372));
#76999=CARTESIAN_POINT('Ctrl Pts',(203.193110568879,10.2594463502455,30.7623044568706));
#77000=CARTESIAN_POINT('Ctrl Pts',(203.19611364447,10.2117926649861,30.7343475639427));
#77001=CARTESIAN_POINT('Ctrl Pts',(203.199116720061,10.1656712057506,30.7036572972487));
#77002=CARTESIAN_POINT('Ctrl Pts',(203.202119795651,10.1214083815894,30.6704311248675));
#77003=CARTESIAN_POINT('Ctrl Pts',(203.205121107725,10.077171550194,30.6372244641224));
#77004=CARTESIAN_POINT('Ctrl Pts',(203.208122419799,10.0347916115257,30.6014851656245));
#77005=CARTESIAN_POINT('Ctrl Pts',(203.211123731873,9.99456537628992,30.563453556788));
#77006=CARTESIAN_POINT('Ctrl Pts',(203.214124463968,9.95434691443848,30.5254292972425));
#77007=CARTESIAN_POINT('Ctrl Pts',(203.217125196063,9.91628171254241,30.4851139694643));
#77008=CARTESIAN_POINT('Ctrl Pts',(203.220125928158,9.88063116082989,30.4427861114245));
#77009=CARTESIAN_POINT('Ctrl Pts',(203.223129407868,9.84494796576275,30.4004194959683));
#77010=CARTESIAN_POINT('Ctrl Pts',(203.226132887577,9.81168417838141,30.3560370732873));
#77011=CARTESIAN_POINT('Ctrl Pts',(203.229136367287,9.78106114953375,30.3099508187687));
#77012=CARTESIAN_POINT('Ctrl Pts',(203.23214122665,9.75042405393841,30.2638433944396));
#77013=CARTESIAN_POINT('Ctrl Pts',(203.235146086014,9.72243040193221,30.2160310341985));
#77014=CARTESIAN_POINT('Ctrl Pts',(203.238150945377,9.69725662554668,30.1668522702353));
#77015=CARTESIAN_POINT('Ctrl Pts',(203.241161403428,9.6720359451002,30.1175818758506));
#77016=CARTESIAN_POINT('Ctrl Pts',(203.24417186148,9.64964584916801,30.0669404758587));
#77017=CARTESIAN_POINT('Ctrl Pts',(203.247182319531,9.63021497557521,30.0152875283389));
#77018=CARTESIAN_POINT('Ctrl Pts',(203.249389919549,9.61596611504658,29.9774098878104));
#77019=CARTESIAN_POINT('Ctrl Pts',(203.251597519567,9.60330754219997,29.9389887240316));
#77020=CARTESIAN_POINT('Ctrl Pts',(203.253805119585,9.5922726417023,29.9001698823002));
#77021=CARTESIAN_POINT('Ctrl Pts',(203.257521581763,9.57369554893588,29.8348189329119));
#77022=CARTESIAN_POINT('Ctrl Pts',(203.26123804394,9.5596592711323,29.7681244782473));
#77023=CARTESIAN_POINT('Ctrl Pts',(203.264954506117,9.55032021996541,29.7006509042065));
#77024=CARTESIAN_POINT('Ctrl Pts',(203.268584655452,9.54119806325685,29.6347443677619));
#77025=CARTESIAN_POINT('Ctrl Pts',(203.272214804787,9.53655747952402,29.5680944076123));
#77026=CARTESIAN_POINT('Ctrl Pts',(203.275844954122,9.53650053107307,29.5012467760758));
#77027=CARTESIAN_POINT('',(203.77584495419,9.53650027734347,29.4990990092893));
#77028=CARTESIAN_POINT('Ctrl Pts',(203.275844954157,9.53650053107252,29.501246775435));
#77029=CARTESIAN_POINT('Ctrl Pts',(203.278822538506,9.53645381984567,29.4464158461698));
#77030=CARTESIAN_POINT('Ctrl Pts',(203.281800122854,9.53949281226948,29.3915218506111));
#77031=CARTESIAN_POINT('Ctrl Pts',(203.284777707203,9.54561214053705,29.3369411019086));
#77032=CARTESIAN_POINT('Ctrl Pts',(203.287753798455,9.55172840029411,29.2823877224849));
#77033=CARTESIAN_POINT('Ctrl Pts',(203.290729889707,9.56092187543824,29.228147811872));
#77034=CARTESIAN_POINT('Ctrl Pts',(203.293705980959,9.57313526104874,29.1745936897699));
#77035=CARTESIAN_POINT('Ctrl Pts',(203.296681802693,9.58534754060459,29.121044417575));
#77036=CARTESIAN_POINT('Ctrl Pts',(203.299657624428,9.60057906605375,29.0681813337964));
#77037=CARTESIAN_POINT('Ctrl Pts',(203.302633446162,9.61872171788103,29.0163652645369));
#77038=CARTESIAN_POINT('Ctrl Pts',(203.305612215513,9.63688234040339,28.9644978703228));
#77039=CARTESIAN_POINT('Ctrl Pts',(203.308590984865,9.65795966395401,28.9136800675947));
#77040=CARTESIAN_POINT('Ctrl Pts',(203.311569754216,9.68179665286988,28.8642546220263));
#77041=CARTESIAN_POINT('Ctrl Pts',(203.314550255797,9.70564750359939,28.8148004343077));
#77042=CARTESIAN_POINT('Ctrl Pts',(203.317530757378,9.73226095077253,28.7667406839756));
#77043=CARTESIAN_POINT('Ctrl Pts',(203.32051125896,9.76143463323604,28.7203923536465));
#77044=CARTESIAN_POINT('Ctrl Pts',(203.323496997708,9.7906595780319,28.6739625826725));
#77045=CARTESIAN_POINT('Ctrl Pts',(203.326482736457,9.82245341829168,28.629250665693));
#77046=CARTESIAN_POINT('Ctrl Pts',(203.329468475206,9.85657221526708,28.5865422007007));
#77047=CARTESIAN_POINT('Ctrl Pts',(203.330496236663,9.86831670714956,28.5718409431863));
#77048=CARTESIAN_POINT('Ctrl Pts',(203.33152399812,9.88033635510133,28.5573767590068));
#77049=CARTESIAN_POINT('Ctrl Pts',(203.332551759578,9.89262022370826,28.5431602636491));
#77050=CARTESIAN_POINT('Ctrl Pts',(203.335563097396,9.92861191986607,28.5015059772253));
#77051=CARTESIAN_POINT('Ctrl Pts',(203.338574435214,9.96703199604216,28.4617986197016));
#77052=CARTESIAN_POINT('Ctrl Pts',(203.341585773032,10.0076417703286,28.4243339765506));
#77053=CARTESIAN_POINT('Ctrl Pts',(203.344591798303,10.0481799015793,28.3869354278513));
#77054=CARTESIAN_POINT('Ctrl Pts',(203.347597823573,10.0908996797894,28.3517720963619));
#77055=CARTESIAN_POINT('Ctrl Pts',(203.350603848843,10.1355238401233,28.3191049077056));
#77056=CARTESIAN_POINT('Ctrl Pts',(203.35360692443,10.1801042126919,28.2864697739538));
#77057=CARTESIAN_POINT('Ctrl Pts',(203.356610000017,10.2265848417551,28.25632624088));
#77058=CARTESIAN_POINT('Ctrl Pts',(203.359613075604,10.2746548860809,28.2288954741196));
#77059=CARTESIAN_POINT('Ctrl Pts',(203.362614387674,10.3226967018997,28.2014808157194));
#77060=CARTESIAN_POINT('Ctrl Pts',(203.365615699744,10.3723256255439,28.1767760269267));
#77061=CARTESIAN_POINT('Ctrl Pts',(203.368617011814,10.4232032326172,28.1549580901932));
#77062=CARTESIAN_POINT('Ctrl Pts',(203.371617743906,10.4740710080167,28.1331443695943));
#77063=CARTESIAN_POINT('Ctrl Pts',(203.374618475998,10.5261865029468,28.114216600833));
#77064=CARTESIAN_POINT('Ctrl Pts',(203.377619208089,10.5791902882369,28.0983040855857));
#77065=CARTESIAN_POINT('Ctrl Pts',(203.380622687795,10.632242606334,28.0823770000764));
#77066=CARTESIAN_POINT('Ctrl Pts',(203.383626167501,10.6861843332858,28.0694708356454));
#77067=CARTESIAN_POINT('Ctrl Pts',(203.386629647206,10.7406412499097,28.059664869292));
#77068=CARTESIAN_POINT('Ctrl Pts',(203.389634506566,10.7951231814234,28.049854398549));
#77069=CARTESIAN_POINT('Ctrl Pts',(203.392639365926,10.8501202497595,28.043147028591));
#77070=CARTESIAN_POINT('Ctrl Pts',(203.395644225286,10.9052516981477,28.0395702655396));
#77071=CARTESIAN_POINT('Ctrl Pts',(203.398654683333,10.9604858680659,28.0359868382233));
#77072=CARTESIAN_POINT('Ctrl Pts',(203.401665141381,11.0158543894073,28.0355456735817));
#77073=CARTESIAN_POINT('Ctrl Pts',(203.404675599428,11.0709762775324,28.0382221037286));
#77074=CARTESIAN_POINT('Ctrl Pts',(203.406883199476,11.1113977286625,28.0401847576591));
#77075=CARTESIAN_POINT('Ctrl Pts',(203.409090799523,11.1516865628465,28.043822775828));
#77076=CARTESIAN_POINT('Ctrl Pts',(203.411298399571,11.1916956689283,28.0491088874371));
#77077=CARTESIAN_POINT('Ctrl Pts',(203.414309737412,11.2462711955327,28.0563195540329));
#77078=CARTESIAN_POINT('Ctrl Pts',(203.417321075253,11.3005528314848,28.0666287993735));
#77079=CARTESIAN_POINT('Ctrl Pts',(203.420332413093,11.3541623137251,28.079999540304));
#77080=CARTESIAN_POINT('Ctrl Pts',(203.423338438386,11.4076772190814,28.0933466928139));
#77081=CARTESIAN_POINT('Ctrl Pts',(203.426344463679,11.4605218161861,28.1097444955115));
#77082=CARTESIAN_POINT('Ctrl Pts',(203.429350488972,11.5123257930212,28.1291044781585));
#77083=CARTESIAN_POINT('Ctrl Pts',(203.432353564582,11.5640789368482,28.1484454636895));
#77084=CARTESIAN_POINT('Ctrl Pts',(203.435356640191,11.6147929914568,28.1707426871275));
#77085=CARTESIAN_POINT('Ctrl Pts',(203.438359715801,11.6641124402058,28.1958577850695));
#77086=CARTESIAN_POINT('Ctrl Pts',(203.441361027894,11.713402926752,28.2209581344979));
#77087=CARTESIAN_POINT('Ctrl Pts',(203.444362339987,11.7612999615425,28.2488728394512));
#77088=CARTESIAN_POINT('Ctrl Pts',(203.44736365208,11.807469810782,28.2794162238192));
#77089=CARTESIAN_POINT('Ctrl Pts',(203.450364384194,11.8536307380826,28.3099537059326));
#77090=CARTESIAN_POINT('Ctrl Pts',(203.453365116308,11.8980647029871,28.3431185675757));
#77091=CARTESIAN_POINT('Ctrl Pts',(203.456365848423,11.9404662896964,28.378681397664));
#77092=CARTESIAN_POINT('Ctrl Pts',(203.459369328151,11.9829067013283,28.414276790782));
#77093=CARTESIAN_POINT('Ctrl Pts',(203.462372807879,12.0233106120234,28.4522741989873));
#77094=CARTESIAN_POINT('Ctrl Pts',(203.465376287608,12.0614062952404,28.4924043834831));
#77095=CARTESIAN_POINT('Ctrl Pts',(203.46838114699,12.099519477782,28.5325530018556));
#77096=CARTESIAN_POINT('Ctrl Pts',(203.471386006372,12.1353219777912,28.5748359461026));
#77097=CARTESIAN_POINT('Ctrl Pts',(203.474390865755,12.1685817484918,28.6189500881948));
#77098=CARTESIAN_POINT('Ctrl Pts',(203.477401323824,12.2019034891633,28.6631464242423));
#77099=CARTESIAN_POINT('Ctrl Pts',(203.480411781894,12.2326727431014,28.7091803339009));
#77100=CARTESIAN_POINT('Ctrl Pts',(203.483422239963,12.2607009446265,28.7567198521298));
#77101=CARTESIAN_POINT('Ctrl Pts',(203.48562983983,12.2812543130927,28.7915810698213));
#77102=CARTESIAN_POINT('Ctrl Pts',(203.487837439697,12.3003346244636,28.8272513205496));
#77103=CARTESIAN_POINT('Ctrl Pts',(203.490045039564,12.3178838986814,28.8635926779207));
#77104=CARTESIAN_POINT('Ctrl Pts',(203.493056377337,12.3418224724883,28.9131651135022));
#77105=CARTESIAN_POINT('Ctrl Pts',(203.49606771511,12.3630099402896,28.9641932196739));
#77106=CARTESIAN_POINT('Ctrl Pts',(203.499079052884,12.3812696071989,29.0163404893641));
#77107=CARTESIAN_POINT('Ctrl Pts',(203.502085078109,12.3994970607327,29.0683957617803));
#77108=CARTESIAN_POINT('Ctrl Pts',(203.505091103335,12.4148067910545,29.1215657853658));
#77109=CARTESIAN_POINT('Ctrl Pts',(203.50809712856,12.4270694173725,29.1754924839081));
#77110=CARTESIAN_POINT('Ctrl Pts',(203.511100204103,12.4393200109045,29.2293662665085));
#77111=CARTESIAN_POINT('Ctrl Pts',(203.514103279646,12.4485293073333,29.2839947411676));
#77112=CARTESIAN_POINT('Ctrl Pts',(203.517106355189,12.4546177493063,29.3390048031673));
#77113=CARTESIAN_POINT('Ctrl Pts',(203.520107667215,12.4607026159215,29.3939825612302));
#77114=CARTESIAN_POINT('Ctrl Pts',(203.523108979241,12.4636702028574,29.4493409390914));
#77115=CARTESIAN_POINT('Ctrl Pts',(203.526110291267,12.4634924560214,29.504699060365));
#77116=CARTESIAN_POINT('Ctrl Pts',(203.529111023315,12.4633147435335,29.5600464841496));
#77117=CARTESIAN_POINT('Ctrl Pts',(203.532111755363,12.4599929062211,29.6153931241434));
#77118=CARTESIAN_POINT('Ctrl Pts',(203.53511248741,12.4535509912168,29.6703577586512));
#77119=CARTESIAN_POINT('Ctrl Pts',(203.538115967073,12.4471031776842,29.7253727214313));
#77120=CARTESIAN_POINT('Ctrl Pts',(203.541119446736,12.4375296407133,29.7800044548445));
#77121=CARTESIAN_POINT('Ctrl Pts',(203.544122926399,12.4249062121686,29.8338780264157));
#77122=CARTESIAN_POINT('Ctrl Pts',(203.547127785717,12.4122769850257,29.8877763449247));
#77123=CARTESIAN_POINT('Ctrl Pts',(203.550132645035,12.3965952232226,29.9409153005076));
#77124=CARTESIAN_POINT('Ctrl Pts',(203.553137504352,12.3779868692051,29.992934517252));
#77125=CARTESIAN_POINT('Ctrl Pts',(203.556147962359,12.3593438438863,30.0450506568047));
#77126=CARTESIAN_POINT('Ctrl Pts',(203.559158420365,12.3377635401926,30.0960424030824));
#77127=CARTESIAN_POINT('Ctrl Pts',(203.562168878371,12.3134198757357,30.1455698877909));
#77128=CARTESIAN_POINT('Ctrl Pts',(203.564376478767,12.2955684115537,30.1818889112013));
#77129=CARTESIAN_POINT('Ctrl Pts',(203.566584079162,12.2762319757039,30.2174209825774));
#77130=CARTESIAN_POINT('Ctrl Pts',(203.568791679557,12.2554940105294,30.2520419134096));
#77131=CARTESIAN_POINT('Ctrl Pts',(203.571803017387,12.2272058206967,30.2992675430859));
#77132=CARTESIAN_POINT('Ctrl Pts',(203.574814355217,12.1961904872769,30.3449930895672));
#77133=CARTESIAN_POINT('Ctrl Pts',(203.577825693047,12.162632241804,30.3888861121189));
#77134=CARTESIAN_POINT('Ctrl Pts',(203.580831718329,12.1291331991939,30.432701699377));
#77135=CARTESIAN_POINT('Ctrl Pts',(203.58383774361,12.0931004655364,30.4746907628363));
#77136=CARTESIAN_POINT('Ctrl Pts',(203.586843768891,12.0547622776991,30.5145485634226));
#77137=CARTESIAN_POINT('Ctrl Pts',(203.589846844489,12.0164617094789,30.5543672532612));
#77138=CARTESIAN_POINT('Ctrl Pts',(203.592849920087,11.975860532681,30.5920584448174));
#77139=CARTESIAN_POINT('Ctrl Pts',(203.595852995684,11.9332269007235,30.6273507891362));
#77140=CARTESIAN_POINT('Ctrl Pts',(203.598854307765,11.8906183048172,30.6626224084804));
#77141=CARTESIAN_POINT('Ctrl Pts',(203.601855619845,11.8459800251689,30.6954976370934));
#77142=CARTESIAN_POINT('Ctrl Pts',(203.604856931925,11.7996149889168,30.7257439045329));
#77143=CARTESIAN_POINT('Ctrl Pts',(203.607857664027,11.753258912329,30.7559843271284));
#77144=CARTESIAN_POINT('Ctrl Pts',(203.610858396128,11.7051771835488,30.7835965095059));
#77145=CARTESIAN_POINT('Ctrl Pts',(203.613859128229,11.6557016249187,30.8083912370079));
#77146=CARTESIAN_POINT('Ctrl Pts',(203.616862607944,11.6061807641086,30.8332086677443));
#77147=CARTESIAN_POINT('Ctrl Pts',(203.619866087658,11.5552639965075,30.8552032530011));
#77148=CARTESIAN_POINT('Ctrl Pts',(203.622869567373,11.5033063208547,30.8742325121273));
#77149=CARTESIAN_POINT('Ctrl Pts',(203.625874426741,11.4513247783509,30.8932705123777));
#77150=CARTESIAN_POINT('Ctrl Pts',(203.62887928611,11.3983018804351,30.9093403179845));
#77151=CARTESIAN_POINT('Ctrl Pts',(203.631884145478,11.3446079733236,30.9223493223262));
#77152=CARTESIAN_POINT('Ctrl Pts',(203.634894603533,11.2908140231397,30.9353825651864));
#77153=CARTESIAN_POINT('Ctrl Pts',(203.637905061588,11.2363470865423,30.9453435199054));
#77154=CARTESIAN_POINT('Ctrl Pts',(203.640915519643,11.1815867109599,30.9521909366205));
#77155=CARTESIAN_POINT('Ctrl Pts',(203.643123119612,11.1414303622548,30.9572122179835));
#77156=CARTESIAN_POINT('Ctrl Pts',(203.645330719581,11.1011163999379,30.9605603017668));
#77157=CARTESIAN_POINT('Ctrl Pts',(203.64753831955,11.0607944334066,30.9622367410467));
#77158=CARTESIAN_POINT('Ctrl Pts',(203.65054965754,11.0057921361647,30.9645235345617));
#77159=CARTESIAN_POINT('Ctrl Pts',(203.653560995531,10.9505462244997,30.9637073914156));
#77160=CARTESIAN_POINT('Ctrl Pts',(203.656572333521,10.8954357009739,30.9597597601555));
#77161=CARTESIAN_POINT('Ctrl Pts',(203.659578358965,10.8404224024234,30.9558190932341));
#77162=CARTESIAN_POINT('Ctrl Pts',(203.662584384408,10.7855445400654,30.948757939387));
#77163=CARTESIAN_POINT('Ctrl Pts',(203.665590409851,10.7311821253338,30.9385997359446));
#77164=CARTESIAN_POINT('Ctrl Pts',(203.668593485612,10.6768730540861,30.9284515003075));
#77165=CARTESIAN_POINT('Ctrl Pts',(203.671596561373,10.6230789445967,30.91521233193));
#77166=CARTESIAN_POINT('Ctrl Pts',(203.674599637133,10.5701738178678,30.8989573628791));
#77167=CARTESIAN_POINT('Ctrl Pts',(203.677600949377,10.5172997589814,30.8827119393458));
#77168=CARTESIAN_POINT('Ctrl Pts',(203.680602261621,10.4653141514163,30.8634543802098));
#77169=CARTESIAN_POINT('Ctrl Pts',(203.683603573865,10.4145776984974,30.8413101725192));
#77170=CARTESIAN_POINT('Ctrl Pts',(203.68660430613,10.3638510499784,30.8191702440135));
#77171=CARTESIAN_POINT('Ctrl Pts',(203.689605038395,10.3143735599288,30.7941449858488));
#77172=CARTESIAN_POINT('Ctrl Pts',(203.69260577066,10.2664855607394,30.7664078400721));
#77173=CARTESIAN_POINT('Ctrl Pts',(203.695609250537,10.2185537130319,30.7386452968523));
#77174=CARTESIAN_POINT('Ctrl Pts',(203.698612730415,10.1722147212041,30.7081661703928));
#77175=CARTESIAN_POINT('Ctrl Pts',(203.701616210292,10.127782583291,30.675188932891));
#77176=CARTESIAN_POINT('Ctrl Pts',(203.704621069823,10.083330035401,30.64219654724));
#77177=CARTESIAN_POINT('Ctrl Pts',(203.707625929354,10.0407864932563,30.60670410167));
#77178=CARTESIAN_POINT('Ctrl Pts',(203.710630788885,10.0004326976241,30.5689702792973));
#77179=CARTESIAN_POINT('Ctrl Pts',(203.7136412471,9.96000371439727,30.5311661508903));
#77180=CARTESIAN_POINT('Ctrl Pts',(203.716651705316,9.92177299262161,30.491112686194));
#77181=CARTESIAN_POINT('Ctrl Pts',(203.719662163531,9.88598340189775,30.449104456397));
#77182=CARTESIAN_POINT('Ctrl Pts',(203.721869762201,9.85973854239347,30.4182994075896));
#77183=CARTESIAN_POINT('Ctrl Pts',(203.724077360872,9.83480557440133,30.3864439463869));
#77184=CARTESIAN_POINT('Ctrl Pts',(203.726284959543,9.81126534399656,30.3536639664507));
#77185=CARTESIAN_POINT('Ctrl Pts',(203.729317528431,9.77892822977764,30.3086342476645));
#77186=CARTESIAN_POINT('Ctrl Pts',(203.73235009732,9.74908658968655,30.2616718031847));
#77187=CARTESIAN_POINT('Ctrl Pts',(203.735382666209,9.72197530517356,30.2130814325263));
#77188=CARTESIAN_POINT('Ctrl Pts',(203.738410312439,9.69490802942409,30.1645699368519));
#77189=CARTESIAN_POINT('Ctrl Pts',(203.741437958668,9.67056257157521,30.1144362026879));
#77190=CARTESIAN_POINT('Ctrl Pts',(203.744465604898,9.64913114704461,30.0630147352557));
#77191=CARTESIAN_POINT('Ctrl Pts',(203.747489133158,9.62772887187511,30.0116632073143));
#77192=CARTESIAN_POINT('Ctrl Pts',(203.750512661419,9.6092329601498,29.9590278983659));
#77193=CARTESIAN_POINT('Ctrl Pts',(203.753536189679,9.59378911509744,29.9054666412685));
#77194=CARTESIAN_POINT('Ctrl Pts',(203.756557313621,9.57835755103658,29.851947976242));
#77195=CARTESIAN_POINT('Ctrl Pts',(203.759578437562,9.56597338189694,29.7975053197424));
#77196=CARTESIAN_POINT('Ctrl Pts',(203.762599561504,9.55673302857216,29.7425132969252));
#77197=CARTESIAN_POINT('Ctrl Pts',(203.765619853801,9.54749521889826,29.6875364121122));
#77198=CARTESIAN_POINT('Ctrl Pts',(203.768640146099,9.54139959904263,29.6320109701614));
#77199=CARTESIAN_POINT('Ctrl Pts',(203.771660438397,9.53849143670484,29.5763214872425));
#77200=CARTESIAN_POINT('Ctrl Pts',(203.773055276983,9.5371483822433,29.5506028375224));
#77201=CARTESIAN_POINT('Ctrl Pts',(203.77445011557,9.53648442441668,29.5248492967995));
#77202=CARTESIAN_POINT('Ctrl Pts',(203.775844954157,9.53650027734309,29.4990990099061));
#77203=CARTESIAN_POINT('',(204.275844954108,9.53650001147645,29.4998167199766));
#77204=CARTESIAN_POINT('Ctrl Pts',(203.77584495419,9.53650027734347,29.4990990092893));
#77205=CARTESIAN_POINT('Ctrl Pts',(203.779226360791,9.53653870847609,29.4366744456907));
#77206=CARTESIAN_POINT('Ctrl Pts',(203.782607767392,9.54057525081011,29.3743982782863));
#77207=CARTESIAN_POINT('Ctrl Pts',(203.785989173993,9.5485288292999,29.3127469876704));
#77208=CARTESIAN_POINT('Ctrl Pts',(203.789397074907,9.55654472641247,29.2506126410907));
#77209=CARTESIAN_POINT('Ctrl Pts',(203.792804975822,9.56853915786416,29.189113258323));
#77210=CARTESIAN_POINT('Ctrl Pts',(203.796212876736,9.58437923470691,29.128718302537));
#77211=CARTESIAN_POINT('Ctrl Pts',(203.799152451003,9.59804250821099,29.0766230502625));
#77212=CARTESIAN_POINT('Ctrl Pts',(203.802092025269,9.61456622497412,29.0253493198056));
#77213=CARTESIAN_POINT('Ctrl Pts',(203.805031599536,9.63383676531657,28.9751854935319));
#77214=CARTESIAN_POINT('Ctrl Pts',(203.808042937614,9.65357775726336,28.9237970180201));
#77215=CARTESIAN_POINT('Ctrl Pts',(203.811054275693,9.67626331988589,28.8734170402998));
#77216=CARTESIAN_POINT('Ctrl Pts',(203.814065613771,9.70176916669647,28.8244047413873));
#77217=CARTESIAN_POINT('Ctrl Pts',(203.817071639294,9.72723001649326,28.7754789092016));
#77218=CARTESIAN_POINT('Ctrl Pts',(203.820077664817,9.75550103462224,28.7279164316734));
#77219=CARTESIAN_POINT('Ctrl Pts',(203.82308369034,9.78640981931206,28.682056772546));
#77220=CARTESIAN_POINT('Ctrl Pts',(203.826086766176,9.81728827449957,28.636242113591));
#77221=CARTESIAN_POINT('Ctrl Pts',(203.829089842011,9.85079907518602,28.5921273982855));
#77222=CARTESIAN_POINT('Ctrl Pts',(203.832092917846,9.88672475340363,28.5500260659809));
#77223=CARTESIAN_POINT('Ctrl Pts',(203.83509423016,9.92262933467787,28.5079494572018));
#77224=CARTESIAN_POINT('Ctrl Pts',(203.838095542473,9.96094564073565,28.4678842883773));
#77225=CARTESIAN_POINT('Ctrl Pts',(203.841096854787,10.001415276456,28.4301117815844));
#77226=CARTESIAN_POINT('Ctrl Pts',(203.844097587117,10.0418770916852,28.3923465740802));
#77227=CARTESIAN_POINT('Ctrl Pts',(203.847098319446,10.084491024585,28.3568735084142));
#77228=CARTESIAN_POINT('Ctrl Pts',(203.850099051776,10.1289627561949,28.3239360689552));
#77229=CARTESIAN_POINT('Ctrl Pts',(203.85310253171,10.1734752081031,28.2909684705096));
#77230=CARTESIAN_POINT('Ctrl Pts',(203.856106011644,10.2198484321534,28.2605414511267));
#77231=CARTESIAN_POINT('Ctrl Pts',(203.859109491577,10.267757237836,28.2328564456785));
#77232=CARTESIAN_POINT('Ctrl Pts',(203.86211435116,10.3156880504362,28.2051587231187));
#77233=CARTESIAN_POINT('Ctrl Pts',(203.865119210743,10.3651553788918,28.1802057632513));
#77234=CARTESIAN_POINT('Ctrl Pts',(203.868124070326,10.415810333059,28.1581525112594));
#77235=CARTESIAN_POINT('Ctrl Pts',(203.871134528585,10.4665596679073,28.1360581694872));
#77236=CARTESIAN_POINT('Ctrl Pts',(203.874144986844,10.5185005525536,28.1168745109617));
#77237=CARTESIAN_POINT('Ctrl Pts',(203.877155445103,10.5712661967198,28.100707473069));
#77238=CARTESIAN_POINT('Ctrl Pts',(203.879363043245,10.6099597536398,28.0888520279055));
#77239=CARTESIAN_POINT('Ctrl Pts',(203.881570641387,10.6490964531806,28.078617708136));
#77240=CARTESIAN_POINT('Ctrl Pts',(203.883778239528,10.6885286501563,28.0700287246848));
#77241=CARTESIAN_POINT('Ctrl Pts',(203.886789578636,10.7423172970144,28.0583126694518));
#77242=CARTESIAN_POINT('Ctrl Pts',(203.889800917743,10.7968797976543,28.049611366135));
#77243=CARTESIAN_POINT('Ctrl Pts',(203.892812256851,10.8518477134735,28.0440181491526));
#77244=CARTESIAN_POINT('Ctrl Pts',(203.89581828342,10.9067186560981,28.0384347996013));
#77245=CARTESIAN_POINT('Ctrl Pts',(203.898824309989,10.9619930737726,28.0359487075318));
#77246=CARTESIAN_POINT('Ctrl Pts',(203.901830336558,11.017292589224,28.0366021674343));
#77247=CARTESIAN_POINT('Ctrl Pts',(203.904833413448,11.0725378417567,28.0372549861261));
#77248=CARTESIAN_POINT('Ctrl Pts',(203.907836490339,11.1278076182619,28.0410412475636));
#77249=CARTESIAN_POINT('Ctrl Pts',(203.91083956723,11.1827205483093,28.0479512917173));
#77250=CARTESIAN_POINT('Ctrl Pts',(203.913840880606,11.2376012315127,28.0548572780449));
#77251=CARTESIAN_POINT('Ctrl Pts',(203.916842193982,11.2921249611837,28.0648833452408));
#77252=CARTESIAN_POINT('Ctrl Pts',(203.919843507358,11.345914822217,28.0779679378542));
#77253=CARTESIAN_POINT('Ctrl Pts',(203.922844240756,11.3996942888129,28.0910500019804));
#77254=CARTESIAN_POINT('Ctrl Pts',(203.925844974153,11.4527396560845,28.1071892929545));
#77255=CARTESIAN_POINT('Ctrl Pts',(203.928845707551,11.5046858252472,28.126273510558));
#77256=CARTESIAN_POINT('Ctrl Pts',(203.931849188552,11.5566795586116,28.1453752025123));
#77257=CARTESIAN_POINT('Ctrl Pts',(203.934852669554,11.6075715869345,28.1674270256495));
#77258=CARTESIAN_POINT('Ctrl Pts',(203.937856150555,11.6570150054717,28.192267790186));
#77259=CARTESIAN_POINT('Ctrl Pts',(203.940861011207,11.7064811358652,28.2171199653387));
#77260=CARTESIAN_POINT('Ctrl Pts',(203.943865871859,11.7544968720457,28.2447633719305));
#77261=CARTESIAN_POINT('Ctrl Pts',(203.94687073251,11.8007411521433,28.2749914868605));
#77262=CARTESIAN_POINT('Ctrl Pts',(203.949881191827,11.8470715947194,28.305275922903));
#77263=CARTESIAN_POINT('Ctrl Pts',(203.952891651144,11.8916235627321,28.3381543730727));
#77264=CARTESIAN_POINT('Ctrl Pts',(203.955902110461,11.934107126041,28.3733784454931));
#77265=CARTESIAN_POINT('Ctrl Pts',(203.958109700148,11.965260603412,28.3992084902822));
#77266=CARTESIAN_POINT('Ctrl Pts',(203.960317289834,11.9953024892084,28.4262989888429));
#77267=CARTESIAN_POINT('Ctrl Pts',(203.962524879521,12.0241314837119,28.4545398362108));
#77268=CARTESIAN_POINT('Ctrl Pts',(203.965536213295,12.0634566016757,28.4930626731418));
#77269=CARTESIAN_POINT('Ctrl Pts',(203.96854754707,12.1006869375865,28.5338875525938));
#77270=CARTESIAN_POINT('Ctrl Pts',(203.971558880845,12.1355421901611,28.5767577867297));
#77271=CARTESIAN_POINT('Ctrl Pts',(203.97456490208,12.170335951748,28.6195523899968));
#77272=CARTESIAN_POINT('Ctrl Pts',(203.977570923316,12.202762615318,28.6643847807526));
#77273=CARTESIAN_POINT('Ctrl Pts',(203.980576944552,12.2325790809666,28.7109619406116));
#77274=CARTESIAN_POINT('Ctrl Pts',(203.983580016113,12.2623662890507,28.757493396386));
#77275=CARTESIAN_POINT('Ctrl Pts',(203.986583087674,12.2895480901372,28.8057657873714));
#77276=CARTESIAN_POINT('Ctrl Pts',(203.989586159236,12.3139231636225,28.8554550674342));
#77277=CARTESIAN_POINT('Ctrl Pts',(203.992587467296,12.3382839232737,28.9051151683395));
#77278=CARTESIAN_POINT('Ctrl Pts',(203.995588775357,12.359840990447,28.9561900363124));
#77279=CARTESIAN_POINT('Ctrl Pts',(203.998590083417,12.3784388641185,29.0083308552618));
#77280=CARTESIAN_POINT('Ctrl Pts',(204.001590811522,12.3970331440441,29.0604615988198));
#77281=CARTESIAN_POINT('Ctrl Pts',(204.004591539627,12.4126691890835,29.1136573875744));
#77282=CARTESIAN_POINT('Ctrl Pts',(204.007592267732,12.4252403977259,29.1675514194794));
#77283=CARTESIAN_POINT('Ctrl Pts',(204.010595743518,12.4378231174659,29.2214948006141));
#77284=CARTESIAN_POINT('Ctrl Pts',(204.013599219304,12.447335274324,29.2761371872828));
#77285=CARTESIAN_POINT('Ctrl Pts',(204.01660269509,12.4537211174992,29.3311001405069));
#77286=CARTESIAN_POINT('Ctrl Pts',(204.019607550562,12.4601098940947,29.3860883416793));
#77287=CARTESIAN_POINT('Ctrl Pts',(204.022612406034,12.4633694632053,29.4413968753827));
#77288=CARTESIAN_POINT('Ctrl Pts',(204.025617261506,12.4634961521434,29.4966440111136));
#77289=CARTESIAN_POINT('Ctrl Pts',(204.028627715764,12.4636230771343,29.5519940858772));
#77290=CARTESIAN_POINT('Ctrl Pts',(204.031638170022,12.4606054905345,29.6072820061521));
#77291=CARTESIAN_POINT('Ctrl Pts',(204.034648624281,12.4544918060457,29.662129072488));
#77292=CARTESIAN_POINT('Ctrl Pts',(204.036856256025,12.4500085079138,29.7023496220594));
#77293=CARTESIAN_POINT('Ctrl Pts',(204.039063887769,12.4438613506776,29.7423331751537));
#77294=CARTESIAN_POINT('Ctrl Pts',(204.041271519514,12.436086741375,29.7819346045576));
#77295=CARTESIAN_POINT('Ctrl Pts',(204.044282861004,12.4254817101582,29.8359533183871));
#77296=CARTESIAN_POINT('Ctrl Pts',(204.047294202494,12.4118024972489,29.8894851965204));
#77297=CARTESIAN_POINT('Ctrl Pts',(204.050305543985,12.3951097375372,29.942155029632));
#77298=CARTESIAN_POINT('Ctrl Pts',(204.053311572865,12.3784464271983,29.9947319426047));
#77299=CARTESIAN_POINT('Ctrl Pts',(204.056317601746,12.3587802791638,30.0464493297879));
#77300=CARTESIAN_POINT('Ctrl Pts',(204.059323630626,12.3362227185147,30.096943126709));
#77301=CARTESIAN_POINT('Ctrl Pts',(204.062326709783,12.3136872929046,30.1473873756238));
#77302=CARTESIAN_POINT('Ctrl Pts',(204.06532978894,12.2882662895848,30.1966099334772));
#77303=CARTESIAN_POINT('Ctrl Pts',(204.068332868098,12.260120005378,30.2442646182952));
#77304=CARTESIAN_POINT('Ctrl Pts',(204.071334183691,12.2319902501247,30.2918913178182));
#77305=CARTESIAN_POINT('Ctrl Pts',(204.074335499285,12.2011386541017,30.3379515159806));
#77306=CARTESIAN_POINT('Ctrl Pts',(204.077336814879,12.1677713740695,30.3821237259613));
#77307=CARTESIAN_POINT('Ctrl Pts',(204.080337550442,12.1344105425606,30.42628739927));
#77308=CARTESIAN_POINT('Ctrl Pts',(204.083338286004,12.0985353105404,30.4685633883658));
#77309=CARTESIAN_POINT('Ctrl Pts',(204.086339021567,12.0603937158286,30.5086612005184));
#77310=CARTESIAN_POINT('Ctrl Pts',(204.089342504637,12.0222171982498,30.5487957266724));
#77311=CARTESIAN_POINT('Ctrl Pts',(204.092345987706,11.9817705368738,30.586747708615));
#77312=CARTESIAN_POINT('Ctrl Pts',(204.095349470776,11.9393394154937,30.6222627644629));
#77313=CARTESIAN_POINT('Ctrl Pts',(204.098354333445,11.896888804092,30.6577941335541));
#77314=CARTESIAN_POINT('Ctrl Pts',(204.101359196114,11.8524523395228,30.6908860295983));
#77315=CARTESIAN_POINT('Ctrl Pts',(204.104364058783,11.806347050573,30.7213257894732));
#77316=CARTESIAN_POINT('Ctrl Pts',(204.10737452001,11.7601558598094,30.7518222636783));
#77317=CARTESIAN_POINT('Ctrl Pts',(204.110384981238,11.7122900908655,30.7796564653641));
#77318=CARTESIAN_POINT('Ctrl Pts',(204.113395442465,11.6630928377565,30.8046609285619));
#77319=CARTESIAN_POINT('Ctrl Pts',(204.115603014812,11.6270164735986,30.8229967108036));
#77320=CARTESIAN_POINT('Ctrl Pts',(204.117810587159,11.5902246710188,30.839811822276));
#77321=CARTESIAN_POINT('Ctrl Pts',(204.120018159507,11.5528587026747,30.8550570116703));
#77322=CARTESIAN_POINT('Ctrl Pts',(204.12302950634,11.5018878293625,30.8758529565279));
#77323=CARTESIAN_POINT('Ctrl Pts',(204.126040853173,11.4496359401254,30.8938122338179));
#77324=CARTESIAN_POINT('Ctrl Pts',(204.129052200006,11.3964499229062,30.9087795102952));
#77325=CARTESIAN_POINT('Ctrl Pts',(204.132058234392,11.3433577334367,30.9237203823538));
#77326=CARTESIAN_POINT('Ctrl Pts',(204.135064268778,11.2893351902625,30.9356795870154));
#77327=CARTESIAN_POINT('Ctrl Pts',(204.138070303164,11.2347477532021,30.9445503599275));
#77328=CARTESIAN_POINT('Ctrl Pts',(204.141073387922,11.1802138792876,30.9534124285198));
#77329=CARTESIAN_POINT('Ctrl Pts',(204.144076472679,11.1251167278233,30.9591919846774));
#77330=CARTESIAN_POINT('Ctrl Pts',(204.147079557437,11.0698336459468,30.9618329288581));
#77331=CARTESIAN_POINT('Ctrl Pts',(204.150080878715,11.0145830275516,30.9644723222164));
#77332=CARTESIAN_POINT('Ctrl Pts',(204.153082199993,10.9591472211274,30.9639767317573));
#77333=CARTESIAN_POINT('Ctrl Pts',(204.156083521271,10.9039081135936,30.960341946041));
#77334=CARTESIAN_POINT('Ctrl Pts',(204.159084262591,10.8486796801503,30.95670786269));
#77335=CARTESIAN_POINT('Ctrl Pts',(204.162085003911,10.7936483962654,30.9499358235573));
#77336=CARTESIAN_POINT('Ctrl Pts',(204.16508574523,10.7391932394833,30.9400736382799));
#77337=CARTESIAN_POINT('Ctrl Pts',(204.168089234121,10.6846882218852,30.9302024228825));
#77338=CARTESIAN_POINT('Ctrl Pts',(204.171092723012,10.6307609054681,30.9172355031283));
#77339=CARTESIAN_POINT('Ctrl Pts',(204.174096211903,10.5777807566252,30.9012719794972));
#77340=CARTESIAN_POINT('Ctrl Pts',(204.177101080438,10.5247762715057,30.8853011230681));
#77341=CARTESIAN_POINT('Ctrl Pts',(204.180105948972,10.4727203177654,30.8663310998614));
#77342=CARTESIAN_POINT('Ctrl Pts',(204.183110817507,10.4219647040667,30.8445101140026));
#77343=CARTESIAN_POINT('Ctrl Pts',(204.186121284598,10.3711145244418,30.8226484721141));
#77344=CARTESIAN_POINT('Ctrl Pts',(204.18913175169,10.3215699975059,30.797925493185));
#77345=CARTESIAN_POINT('Ctrl Pts',(204.192142218781,10.2736594681296,30.7705359820809));
#77346=CARTESIAN_POINT('Ctrl Pts',(204.194349745687,10.2385274505778,30.750451695863));
#77347=CARTESIAN_POINT('Ctrl Pts',(204.196557272593,10.2042735336006,30.7289345812719));
#77348=CARTESIAN_POINT('Ctrl Pts',(204.1987647995,10.1710164400011,30.7060756639828));
#77349=CARTESIAN_POINT('Ctrl Pts',(204.201765499031,10.1258099490225,30.675003452723));
#77350=CARTESIAN_POINT('Ctrl Pts',(204.204766198562,10.0822554830452,30.6413190711555));
#77351=CARTESIAN_POINT('Ctrl Pts',(204.207766898093,10.0406720412411,30.6052249171746));
#77352=CARTESIAN_POINT('Ctrl Pts',(204.210762304788,9.99916194711496,30.5691944284956));
#77353=CARTESIAN_POINT('Ctrl Pts',(204.213757711483,9.95961637746621,30.5307629467643));
#77354=CARTESIAN_POINT('Ctrl Pts',(204.216753118178,9.92232407296167,30.4901751593946));
#77355=CARTESIAN_POINT('Ctrl Pts',(204.219745603105,9.88506814397559,30.4496269620107));
#77356=CARTESIAN_POINT('Ctrl Pts',(204.222738088032,9.85006148522582,30.406927014425));
#77357=CARTESIAN_POINT('Ctrl Pts',(204.225730572958,9.81755709691058,30.3623578323025));
#77358=CARTESIAN_POINT('Ctrl Pts',(204.228721341017,9.785071357228,30.317814220706));
#77359=CARTESIAN_POINT('Ctrl Pts',(204.231712109076,9.75508535565408,30.2714039288233));
#77360=CARTESIAN_POINT('Ctrl Pts',(204.234702877134,9.72781124896586,30.2234417956838));
#77361=CARTESIAN_POINT('Ctrl Pts',(204.237693130609,9.70054183498594,30.1754879147779));
#77362=CARTESIAN_POINT('Ctrl Pts',(204.240683384084,9.67598365154099,30.1259831852319));
#77363=CARTESIAN_POINT('Ctrl Pts',(204.24367363756,9.65430377762247,30.0752685695211));
#77364=CARTESIAN_POINT('Ctrl Pts',(204.246666640412,9.63260397022328,30.0245073244426));
#77365=CARTESIAN_POINT('Ctrl Pts',(204.249659643265,9.61378796625327,29.9725344618907));
#77366=CARTESIAN_POINT('Ctrl Pts',(204.252652646118,9.59797472410803,29.9197110622322));
#77367=CARTESIAN_POINT('Ctrl Pts',(204.255647123817,9.58215368975522,29.8668616330667));
#77368=CARTESIAN_POINT('Ctrl Pts',(204.258641601516,9.56933848774583,29.8131613499567));
#77369=CARTESIAN_POINT('Ctrl Pts',(204.261636079215,9.55959732571954,29.758983369979));
#77370=CARTESIAN_POINT('Ctrl Pts',(204.264635948165,9.54983862572631,29.704707848084));
#77371=CARTESIAN_POINT('Ctrl Pts',(204.267635817115,9.54316507874804,29.6499534407802));
#77372=CARTESIAN_POINT('Ctrl Pts',(204.270635686065,9.53959305818328,29.5950989710434));
#77373=CARTESIAN_POINT('Ctrl Pts',(204.272372108746,9.53752545535506,29.5633474022292));
#77374=CARTESIAN_POINT('Ctrl Pts',(204.274108531427,9.53649603584491,29.5315623331089));
#77375=CARTESIAN_POINT('Ctrl Pts',(204.275844954108,9.53650001147645,29.4998167199766));
#77376=CARTESIAN_POINT('',(204.775844954127,9.53650044545502,29.5011418610453));
#77377=CARTESIAN_POINT('Ctrl Pts',(204.275844954157,9.53650001147656,29.4998167190727));
#77378=CARTESIAN_POINT('Ctrl Pts',(204.276400449269,9.53650128331826,29.4896610506928));
#77379=CARTESIAN_POINT('Ctrl Pts',(204.276955944381,9.53660826359327,29.4795061482609));
#77380=CARTESIAN_POINT('Ctrl Pts',(204.277511439493,9.53682091319707,29.4693534676914));
#77381=CARTESIAN_POINT('Ctrl Pts',(204.280522821154,9.53797370302999,29.4143150066341));
#77382=CARTESIAN_POINT('Ctrl Pts',(204.283534202815,9.54223866752445,29.3592272091366));
#77383=CARTESIAN_POINT('Ctrl Pts',(204.286545584476,9.54962062900635,29.3044701296577));
#77384=CARTESIAN_POINT('Ctrl Pts',(204.289551653075,9.55698956629596,29.2498096595603));
#77385=CARTESIAN_POINT('Ctrl Pts',(204.292557721675,9.56746451667963,29.1954792681896));
#77386=CARTESIAN_POINT('Ctrl Pts',(204.295563790275,9.58099835221424,29.1418567694605));
#77387=CARTESIAN_POINT('Ctrl Pts',(204.298566908844,9.594518906207,29.0882868936155));
#77388=CARTESIAN_POINT('Ctrl Pts',(204.301570027414,9.61109227001882,29.0354240432555));
#77389=CARTESIAN_POINT('Ctrl Pts',(204.304573145983,9.63062009606983,28.9836368247907));
#77390=CARTESIAN_POINT('Ctrl Pts',(204.307574500615,9.65013645208959,28.9318800245104));
#77391=CARTESIAN_POINT('Ctrl Pts',(204.310575855247,9.67260364477141,28.8811980964853));
#77392=CARTESIAN_POINT('Ctrl Pts',(204.313577209879,9.6978739016151,28.831943210569));
#77393=CARTESIAN_POINT('Ctrl Pts',(204.316577984038,9.72313927110199,28.7826978507213));
#77394=CARTESIAN_POINT('Ctrl Pts',(204.319578758197,9.75120638727083,28.7348794539368));
#77395=CARTESIAN_POINT('Ctrl Pts',(204.322579532357,9.78188088839983,28.6888168641087));
#77396=CARTESIAN_POINT('Ctrl Pts',(204.325583053042,9.81258346505192,28.6427121144652));
#77397=CARTESIAN_POINT('Ctrl Pts',(204.328586573727,9.84589790113683,28.5983668222543));
#77398=CARTESIAN_POINT('Ctrl Pts',(204.331590094412,9.88158653725754,28.5560807363146));
#77399=CARTESIAN_POINT('Ctrl Pts',(204.334594994206,9.91729156032239,28.513775234118));
#77400=CARTESIAN_POINT('Ctrl Pts',(204.337599894,9.95537259328542,28.473531206814));
#77401=CARTESIAN_POINT('Ctrl Pts',(204.340604793794,9.99555392092646,28.4356127000787));
#77402=CARTESIAN_POINT('Ctrl Pts',(204.343615290898,10.0358100954369,28.397623561493));
#77403=CARTESIAN_POINT('Ctrl Pts',(204.346625788002,10.0781739749656,28.3619689368908));
#77404=CARTESIAN_POINT('Ctrl Pts',(204.349636285106,10.1223363910121,28.3288728337801));
#77405=CARTESIAN_POINT('Ctrl Pts',(204.351843549899,10.1547158096761,28.3046071192947));
#77406=CARTESIAN_POINT('Ctrl Pts',(204.354050814692,10.1880613644728,28.2817159252824));
#77407=CARTESIAN_POINT('Ctrl Pts',(204.356258079485,10.2222424211719,28.2602720465459));
#77408=CARTESIAN_POINT('Ctrl Pts',(204.359269473318,10.2688759848679,28.2310159444379));
#77409=CARTESIAN_POINT('Ctrl Pts',(204.36228086715,10.3172595531988,28.2043339143422));
#77410=CARTESIAN_POINT('Ctrl Pts',(204.365292260982,10.3670781215844,28.1804386540131));
#77411=CARTESIAN_POINT('Ctrl Pts',(204.368298343285,10.416808819438,28.1565855404037));
#77412=CARTESIAN_POINT('Ctrl Pts',(204.371304425588,10.4679690223464,28.1355096680641));
#77413=CARTESIAN_POINT('Ctrl Pts',(204.374310507892,10.5202170756615,28.1173790846681));
#77414=CARTESIAN_POINT('Ctrl Pts',(204.377313641088,10.5724138712135,28.0992662882151));
#77415=CARTESIAN_POINT('Ctrl Pts',(204.380316774285,10.6256959069131,28.0840932286431));
#77416=CARTESIAN_POINT('Ctrl Pts',(204.383319907482,10.6797011022628,28.0719800890365));
#77417=CARTESIAN_POINT('Ctrl Pts',(204.386321277629,10.7336745927592,28.0598740606959));
#77418=CARTESIAN_POINT('Ctrl Pts',(204.389322647775,10.7883698875996,28.0508245067879));
#77419=CARTESIAN_POINT('Ctrl Pts',(204.392324017921,10.8434115077447,28.0449012768567));
#77420=CARTESIAN_POINT('Ctrl Pts',(204.395324808445,10.898442498297,28.0389791908148));
#77421=CARTESIAN_POINT('Ctrl Pts',(204.398325598969,10.9538191570559,28.0361822859652));
#77422=CARTESIAN_POINT('Ctrl Pts',(204.401326389493,11.0091599213979,28.0365286658633));
#77423=CARTESIAN_POINT('Ctrl Pts',(204.404329927704,11.0645513587528,28.0368753629255));
#77424=CARTESIAN_POINT('Ctrl Pts',(204.407333465916,11.1199063073609,28.0403710912032));
#77425=CARTESIAN_POINT('Ctrl Pts',(204.410337004127,11.1748437497578,28.0469817918654));
#77426=CARTESIAN_POINT('Ctrl Pts',(204.413341922119,11.229806429616,28.0535955293873));
#77427=CARTESIAN_POINT('Ctrl Pts',(204.416346840112,11.2843507007041,28.063326998946));
#77428=CARTESIAN_POINT('Ctrl Pts',(204.419351758105,11.3381044918167,28.07609073231));
#77429=CARTESIAN_POINT('Ctrl Pts',(204.422362274259,11.3919584262298,28.0888782445064));
#77430=CARTESIAN_POINT('Ctrl Pts',(204.425372790414,11.4450184322874,28.1047091535964));
#77431=CARTESIAN_POINT('Ctrl Pts',(204.428383306568,11.4969275350303,28.1234480485907));
#77432=CARTESIAN_POINT('Ctrl Pts',(204.430590444204,11.5349843095062,28.1371863307617));
#77433=CARTESIAN_POINT('Ctrl Pts',(204.432797581841,11.5724228080511,28.1524865970125));
#77434=CARTESIAN_POINT('Ctrl Pts',(204.435004719478,11.6091104890114,28.1692796453889));
#77435=CARTESIAN_POINT('Ctrl Pts',(204.438015741664,11.6591605717578,28.19218906454));
#77436=CARTESIAN_POINT('Ctrl Pts',(204.44102676385,11.7080206170168,28.2179737904179));
#77437=CARTESIAN_POINT('Ctrl Pts',(204.444037786037,11.7553399525135,28.2464874128526));
#77438=CARTESIAN_POINT('Ctrl Pts',(204.447043495562,11.8025757975657,28.274950725726));
#77439=CARTESIAN_POINT('Ctrl Pts',(204.450049205088,11.8482758793376,28.3061331095639));
#77440=CARTESIAN_POINT('Ctrl Pts',(204.453054914614,11.8921122033382,28.3398413614272));
#77441=CARTESIAN_POINT('Ctrl Pts',(204.456057674636,11.9359055107388,28.3735165353713));
#77442=CARTESIAN_POINT('Ctrl Pts',(204.459060434657,11.9778382671686,28.4097123469522));
#77443=CARTESIAN_POINT('Ctrl Pts',(204.462063194679,12.0176112622621,28.4481922376606));
#77444=CARTESIAN_POINT('Ctrl Pts',(204.465064191928,12.0573609085787,28.4866495387104));
#77445=CARTESIAN_POINT('Ctrl Pts',(204.468065189176,12.0949529281937,28.5273878948412));
#77446=CARTESIAN_POINT('Ctrl Pts',(204.471066186425,12.1301228188404,28.5701319102495));
#77447=CARTESIAN_POINT('Ctrl Pts',(204.474066605003,12.1652859278187,28.6128676835014));
#77448=CARTESIAN_POINT('Ctrl Pts',(204.477067023581,12.198027500383,28.6576079405851));
#77449=CARTESIAN_POINT('Ctrl Pts',(204.48006744216,12.2281229409497,28.7040437876911));
#77450=CARTESIAN_POINT('Ctrl Pts',(204.483070612855,12.2582459863915,28.7505222278192));
#77451=CARTESIAN_POINT('Ctrl Pts',(204.486073783551,12.2857177634556,28.7986989211841));
#77452=CARTESIAN_POINT('Ctrl Pts',(204.489076954246,12.3103575716893,28.8482367881534));
#77453=CARTESIAN_POINT('Ctrl Pts',(204.492081506642,12.335008716218,28.8977974465288));
#77454=CARTESIAN_POINT('Ctrl Pts',(204.495086059038,12.3568250865711,28.9487200409479));
#77455=CARTESIAN_POINT('Ctrl Pts',(204.498090611434,12.3756738622899,29.0006467436649));
#77456=CARTESIAN_POINT('Ctrl Pts',(204.501100769622,12.3945578054185,29.0526703294722));
#77457=CARTESIAN_POINT('Ctrl Pts',(204.50411092781,12.4104629420159,29.1057012591851));
#77458=CARTESIAN_POINT('Ctrl Pts',(204.507121085999,12.4233064824285,29.1593669025522));
#77459=CARTESIAN_POINT('Ctrl Pts',(204.509331177156,12.4327363506682,29.19876880652));
#77460=CARTESIAN_POINT('Ctrl Pts',(204.511541268313,12.4405168791148,29.2385125619717));
#77461=CARTESIAN_POINT('Ctrl Pts',(204.513751359471,12.4466330927872,29.2784487760064));
#77462=CARTESIAN_POINT('Ctrl Pts',(204.516763175375,12.45496800221,29.3328721079075));
#77463=CARTESIAN_POINT('Ctrl Pts',(204.51977499128,12.4602447953578,29.3878794931995));
#77464=CARTESIAN_POINT('Ctrl Pts',(204.522786807184,12.4623933569935,29.4430972810729));
#77465=CARTESIAN_POINT('Ctrl Pts',(204.525793306424,12.4645381258402,29.4982175947048));
#77466=CARTESIAN_POINT('Ctrl Pts',(204.528799805663,12.463565602104,29.5535470509709));
#77467=CARTESIAN_POINT('Ctrl Pts',(204.531806304903,12.4594572324276,29.6087052745489));
#77468=CARTESIAN_POINT('Ctrl Pts',(204.534809851571,12.4553528974288,29.6638093292804));
#77469=CARTESIAN_POINT('Ctrl Pts',(204.537813398239,12.4481188563938,29.7187419610406));
#77470=CARTESIAN_POINT('Ctrl Pts',(204.540816944907,12.4377885958395,29.773123055918));
#77471=CARTESIAN_POINT('Ctrl Pts',(204.543818724355,12.42746441338,29.8274721541724));
#77472=CARTESIAN_POINT('Ctrl Pts',(204.546820503804,12.4140477207097,29.8812698416567));
#77473=CARTESIAN_POINT('Ctrl Pts',(204.549822283252,12.397623519851,29.9341436936767));
#77474=CARTESIAN_POINT('Ctrl Pts',(204.552823478201,12.3812025170739,29.9870072502252));
#77475=CARTESIAN_POINT('Ctrl Pts',(204.55582467315,12.3617753256444,30.0389468252126));
#77476=CARTESIAN_POINT('Ctrl Pts',(204.558825868099,12.3394768554888,30.0896049555507));
#77477=CARTESIAN_POINT('Ctrl Pts',(204.561829800073,12.3171580496061,30.1403092850182));
#77478=CARTESIAN_POINT('Ctrl Pts',(204.564833732047,12.2919629467405,30.1897293514413));
#77479=CARTESIAN_POINT('Ctrl Pts',(204.567837664022,12.264074115055,30.2375289022459));
#77480=CARTESIAN_POINT('Ctrl Pts',(204.570842970426,12.2361725230138,30.2853503234277));
#77481=CARTESIAN_POINT('Ctrl Pts',(204.57384827683,12.205575036934,30.3315493104731));
#77482=CARTESIAN_POINT('Ctrl Pts',(204.576853583234,12.1725078589686,30.375818229233));
#77483=CARTESIAN_POINT('Ctrl Pts',(204.579864474381,12.1393792324633,30.420169412661));
#77484=CARTESIAN_POINT('Ctrl Pts',(204.582875365528,12.1037720863909,30.4625829584856));
#77485=CARTESIAN_POINT('Ctrl Pts',(204.585886256675,12.0659524691719,30.5027849138605));
#77486=CARTESIAN_POINT('Ctrl Pts',(204.588090170938,12.0382692386172,30.5322119700085));
#77487=CARTESIAN_POINT('Ctrl Pts',(204.590294085201,12.0094014093267,30.5604547891699));
#77488=CARTESIAN_POINT('Ctrl Pts',(204.592497999464,11.9794645777,30.5874196020999));
#77489=CARTESIAN_POINT('Ctrl Pts',(204.595509605638,11.9385564768285,30.6242664969574));
#77490=CARTESIAN_POINT('Ctrl Pts',(204.598521211813,11.8954813553504,30.6588782425937));
#77491=CARTESIAN_POINT('Ctrl Pts',(204.601532817987,11.8505130146541,30.6909911258712));
#77492=CARTESIAN_POINT('Ctrl Pts',(204.604539121475,11.8056238519877,30.7230474663723));
#77493=CARTESIAN_POINT('Ctrl Pts',(204.607545424962,11.758848511541,30.7526133723107));
#77494=CARTESIAN_POINT('Ctrl Pts',(204.610551728449,11.7104947221468,30.7794645363594));
#77495=CARTESIAN_POINT('Ctrl Pts',(204.613555088052,11.6621882825954,30.8062894067421));
#77496=CARTESIAN_POINT('Ctrl Pts',(204.616558447654,11.6123069151187,30.8304045468145));
#77497=CARTESIAN_POINT('Ctrl Pts',(204.619561807256,11.5611866969351,30.8516292913307));
#77498=CARTESIAN_POINT('Ctrl Pts',(204.622563408558,11.5100964068086,30.8728416099342));
#77499=CARTESIAN_POINT('Ctrl Pts',(204.625565009859,11.4577691898301,30.8911666853219));
#77500=CARTESIAN_POINT('Ctrl Pts',(204.628566611161,11.4045629743253,30.9064711336551));
#77501=CARTESIAN_POINT('Ctrl Pts',(204.631567637126,11.3513669572101,30.9217726484828));
#77502=CARTESIAN_POINT('Ctrl Pts',(204.63456866309,11.297292782866,30.934054540551));
#77503=CARTESIAN_POINT('Ctrl Pts',(204.637569689055,11.2427132686662,30.9432333557722));
#77504=CARTESIAN_POINT('Ctrl Pts',(204.640573467329,11.1880836983501,30.9524205890939));
#77505=CARTESIAN_POINT('Ctrl Pts',(204.643577245603,11.1329483835845,30.9584989726131));
#77506=CARTESIAN_POINT('Ctrl Pts',(204.646581023877,11.0776885739645,30.9614365314564));
#77507=CARTESIAN_POINT('Ctrl Pts',(204.649586184862,11.0224033269251,30.9643754425287));
#77508=CARTESIAN_POINT('Ctrl Pts',(204.652591345848,10.9669939991435,30.9641706488739));
#77509=CARTESIAN_POINT('Ctrl Pts',(204.655596506833,10.9118418677849,30.9608423575884));
#77510=CARTESIAN_POINT('Ctrl Pts',(204.658607267649,10.8565869656935,30.9575078643497));
#77511=CARTESIAN_POINT('Ctrl Pts',(204.661618028465,10.8015907424027,30.9510383089441));
#77512=CARTESIAN_POINT('Ctrl Pts',(204.664628789281,10.7472281931458,30.9415056932457));
#77513=CARTESIAN_POINT('Ctrl Pts',(204.666834072673,10.7074094116684,30.9345233654006));
#77514=CARTESIAN_POINT('Ctrl Pts',(204.669039356065,10.6679304544797,30.9258987751431));
#77515=CARTESIAN_POINT('Ctrl Pts',(204.671244639457,10.6289334192774,30.9156771675318));
#77516=CARTESIAN_POINT('Ctrl Pts',(204.674253319779,10.5757295485697,30.9017317717611));
#77517=CARTESIAN_POINT('Ctrl Pts',(204.677262000102,10.5232010291994,30.8847536203949));
#77518=CARTESIAN_POINT('Ctrl Pts',(204.680270680425,10.4717180778835,30.8648261650353));
#77519=CARTESIAN_POINT('Ctrl Pts',(204.683274043593,10.4203261109018,30.8449339268925));
#77520=CARTESIAN_POINT('Ctrl Pts',(204.686277406762,10.369976534148,30.8221029173947));
#77521=CARTESIAN_POINT('Ctrl Pts',(204.689280769931,10.3210253251765,30.79646659847));
#77522=CARTESIAN_POINT('Ctrl Pts',(204.692281182635,10.2721222052251,30.7708554643258));
#77523=CARTESIAN_POINT('Ctrl Pts',(204.69528159534,10.2246151978537,30.7424447239705));
#77524=CARTESIAN_POINT('Ctrl Pts',(204.698282008044,10.1788394205826,30.7114155161673));
#77525=CARTESIAN_POINT('Ctrl Pts',(204.701280661182,10.1330904881283,30.6804045051801));
#77526=CARTESIAN_POINT('Ctrl Pts',(204.70427931432,10.0890712102181,30.6467783663478));
#77527=CARTESIAN_POINT('Ctrl Pts',(204.707277967458,10.0470892181024,30.6107624821461));
#77528=CARTESIAN_POINT('Ctrl Pts',(204.710276049297,10.0051152243286,30.5747534596329));
#77529=CARTESIAN_POINT('Ctrl Pts',(204.713274131136,9.96517814644921,30.5363559400557));
#77530=CARTESIAN_POINT('Ctrl Pts',(204.716272212975,9.92755207795919,30.4958351793898));
#77531=CARTESIAN_POINT('Ctrl Pts',(204.719273076784,9.88989109562312,30.4552768188456));
#77532=CARTESIAN_POINT('Ctrl Pts',(204.722273940592,9.85454576702586,30.4125916696237));
#77533=CARTESIAN_POINT('Ctrl Pts',(204.725274804401,9.8217517992952,30.3680803116854));
#77534=CARTESIAN_POINT('Ctrl Pts',(204.728277063021,9.78894258882165,30.3235482647232));
#77535=CARTESIAN_POINT('Ctrl Pts',(204.731279321641,9.75868739212584,30.2771887607261));
#77536=CARTESIAN_POINT('Ctrl Pts',(204.73428158026,9.73117831254707,30.2293310465414));
#77537=CARTESIAN_POINT('Ctrl Pts',(204.737289494286,9.70361741364187,30.1813831819572));
#77538=CARTESIAN_POINT('Ctrl Pts',(204.740297408312,9.67881320209428,30.131931943521));
#77539=CARTESIAN_POINT('Ctrl Pts',(204.743305322338,9.65691103634704,30.0813297564323));
#77540=CARTESIAN_POINT('Ctrl Pts',(204.745533974709,9.64068307464761,30.0438371009817));
#77541=CARTESIAN_POINT('Ctrl Pts',(204.747762627079,9.62604727834639,30.0057130844164));
#77542=CARTESIAN_POINT('Ctrl Pts',(204.74999127945,9.61304502324796,29.9671061361862));
#77543=CARTESIAN_POINT('Ctrl Pts',(204.753547770861,9.59229597813274,29.9054970303406));
#77544=CARTESIAN_POINT('Ctrl Pts',(204.757104262271,9.57563762197559,29.8424493021325));
#77545=CARTESIAN_POINT('Ctrl Pts',(204.760660753682,9.56323692096333,29.7784674212849));
#77546=CARTESIAN_POINT('Ctrl Pts',(204.764179434315,9.55096805779392,29.7151657627202));
#77547=CARTESIAN_POINT('Ctrl Pts',(204.767698114948,9.54286688239446,29.6509498184118));
#77548=CARTESIAN_POINT('Ctrl Pts',(204.77121679558,9.53904836750614,29.5863283123519));
#77549=CARTESIAN_POINT('Ctrl Pts',(204.772759515096,9.5373741895816,29.5579958579657));
#77550=CARTESIAN_POINT('Ctrl Pts',(204.774302234611,9.53652263808773,29.5295856968488));
#77551=CARTESIAN_POINT('Ctrl Pts',(204.775844954127,9.53650044545502,29.5011418610453));
#77552=CARTESIAN_POINT('',(204.899999975772,10.9852095428848,28.0365747397361));
#77553=CARTESIAN_POINT('Ctrl Pts',(204.775844954157,9.53650044545459,29.5011418604867));
#77554=CARTESIAN_POINT('Ctrl Pts',(204.77884502705,9.53645728823607,29.4458281239961));
#77555=CARTESIAN_POINT('Ctrl Pts',(204.781845099943,9.53955436493385,29.3904748053103));
#77556=CARTESIAN_POINT('Ctrl Pts',(204.784845172835,9.54577854890722,29.3354636174531));
#77557=CARTESIAN_POINT('Ctrl Pts',(204.787844592698,9.55200137805301,29.2804644039648));
#77558=CARTESIAN_POINT('Ctrl Pts',(204.79084401256,9.56134990379099,29.2258076973229));
#77559=CARTESIAN_POINT('Ctrl Pts',(204.793843432423,9.5737591602953,29.1718699691305));
#77560=CARTESIAN_POINT('Ctrl Pts',(204.796845619017,9.58617986337696,29.1178824875642));
#77561=CARTESIAN_POINT('Ctrl Pts',(204.799847805612,9.60166682078197,29.0646158250656));
#77562=CARTESIAN_POINT('Ctrl Pts',(204.802849992207,9.62010423858225,29.0124346837384));
#77563=CARTESIAN_POINT('Ctrl Pts',(204.805853487826,9.63854969553359,28.960230790197));
#77564=CARTESIAN_POINT('Ctrl Pts',(204.808856983445,9.65994797423536,28.9091138493192));
#77565=CARTESIAN_POINT('Ctrl Pts',(204.811860479065,9.68413500609405,28.8594287176177));
#77566=CARTESIAN_POINT('Ctrl Pts',(204.814869825617,9.70836915528207,28.8096467972434));
#77567=CARTESIAN_POINT('Ctrl Pts',(204.817879172168,9.73540265495082,28.7613027214988));
#77568=CARTESIAN_POINT('Ctrl Pts',(204.82088851872,9.76502584936004,28.7147159130282));
#77569=CARTESIAN_POINT('Ctrl Pts',(204.823504985628,9.79078164269565,28.6742111587279));
#77570=CARTESIAN_POINT('Ctrl Pts',(204.826121452535,9.81849424882487,28.6350345149928));
#77571=CARTESIAN_POINT('Ctrl Pts',(204.828737919443,9.84800131355898,28.5973753402227));
#77572=CARTESIAN_POINT('Ctrl Pts',(204.831710460538,9.88152398578609,28.5545911397764));
#77573=CARTESIAN_POINT('Ctrl Pts',(204.834683001634,9.91751103353325,28.5135781388271));
#77574=CARTESIAN_POINT('Ctrl Pts',(204.837655542729,9.95574604316337,28.4746386375375));
#77575=CARTESIAN_POINT('Ctrl Pts',(204.840624029014,9.99392889683818,28.4357522531925));
#77576=CARTESIAN_POINT('Ctrl Pts',(204.843592515299,10.0343532692239,28.3989341555116));
#77577=CARTESIAN_POINT('Ctrl Pts',(204.846561001584,10.0767619821704,28.364454398787));
#77578=CARTESIAN_POINT('Ctrl Pts',(204.849526680816,10.1191305926865,28.3300072467315));
#77579=CARTESIAN_POINT('Ctrl Pts',(204.852492360048,10.1634794107131,28.2978943990209));
#77580=CARTESIAN_POINT('Ctrl Pts',(204.85545803928,10.2095156111155,28.26834798708));
#77581=CARTESIAN_POINT('Ctrl Pts',(204.858422154716,10.2555275367431,28.2388171548891));
#77582=CARTESIAN_POINT('Ctrl Pts',(204.861386270152,10.3032246264038,28.2118503695707));
#77583=CARTESIAN_POINT('Ctrl Pts',(204.864350385589,10.3522843261273,28.1876369954088));
#77584=CARTESIAN_POINT('Ctrl Pts',(204.867321184771,10.4014546499341,28.1633690228222));
#77585=CARTESIAN_POINT('Ctrl Pts',(204.870291983953,10.451993256,28.1418671547788));
#77586=CARTESIAN_POINT('Ctrl Pts',(204.873262783135,10.5035519629505,28.1232750468922));
#77587=CARTESIAN_POINT('Ctrl Pts',(204.876229173213,10.5550341491911,28.1047105324302));
#77588=CARTESIAN_POINT('Ctrl Pts',(204.879195563292,10.607532885305,28.0890472933377));
#77589=CARTESIAN_POINT('Ctrl Pts',(204.882161953371,10.6606857674985,28.0763785258637));
#77590=CARTESIAN_POINT('Ctrl Pts',(204.885134957104,10.713957155623,28.0636815129961));
#77591=CARTESIAN_POINT('Ctrl Pts',(204.888107960838,10.7678850709837,28.0539924264728));
#77592=CARTESIAN_POINT('Ctrl Pts',(204.891080964572,10.822096819896,28.0473532058656));
#77593=CARTESIAN_POINT('Ctrl Pts',(204.894053968305,10.8763085688083,28.0407139852585));
#77594=CARTESIAN_POINT('Ctrl Pts',(204.897026972039,10.9308036068453,28.0371246063304));
#77595=CARTESIAN_POINT('Ctrl Pts',(204.899999975772,10.9852095428848,28.0365747397361));
#77596=CARTESIAN_POINT('',(204.9,9.84750728139498,28.5980062175589));
#77597=CARTESIAN_POINT('Origin',(204.9,11.,29.5));
#77598=CARTESIAN_POINT('',(204.847155045794,9.53650147895644,29.5020806016713));
#77599=CARTESIAN_POINT('Ctrl Pts',(204.9,9.84750728139498,28.5980062175589));
#77600=CARTESIAN_POINT('Ctrl Pts',(204.896944428771,9.8128730288008,28.6422589881502));
#77601=CARTESIAN_POINT('Ctrl Pts',(204.893888857542,9.78075513505351,28.6885550368351));
#77602=CARTESIAN_POINT('Ctrl Pts',(204.890833286313,9.75139134325211,28.736580932715));
#77603=CARTESIAN_POINT('Ctrl Pts',(204.887780085735,9.722050333216,28.7845695679205));
#77604=CARTESIAN_POINT('Ctrl Pts',(204.884726885158,9.69545944481763,28.8342849570117));
#77605=CARTESIAN_POINT('Ctrl Pts',(204.88167368458,9.67181316691742,28.8853846841918));
#77606=CARTESIAN_POINT('Ctrl Pts',(204.878620835613,9.64816961215427,28.9364785266587));
#77607=CARTESIAN_POINT('Ctrl Pts',(204.875567986645,9.627470219116,28.988955939797));
#77608=CARTESIAN_POINT('Ctrl Pts',(204.872515137678,9.60986278229004,29.0424513512886));
#77609=CARTESIAN_POINT('Ctrl Pts',(204.869462692086,9.59225767194476,29.095939694401));
#77610=CARTESIAN_POINT('Ctrl Pts',(204.866410246493,9.57774385730325,29.150445287817));
#77611=CARTESIAN_POINT('Ctrl Pts',(204.863357800901,9.56641955808898,29.2055864021989));
#77612=CARTESIAN_POINT('Ctrl Pts',(204.860302850763,9.55508596723761,29.2607727601066));
#77613=CARTESIAN_POINT('Ctrl Pts',(204.857247900626,9.54694721616499,29.316595185212));
#77614=CARTESIAN_POINT('Ctrl Pts',(204.854192950489,9.54205031404698,29.3726620118367));
#77615=CARTESIAN_POINT('Ctrl Pts',(204.851846982273,9.53828986749146,29.4157170494868));
#77616=CARTESIAN_POINT('Ctrl Pts',(204.849501014058,9.53644011341938,29.4589159667267));
#77617=CARTESIAN_POINT('Ctrl Pts',(204.847155045843,9.53650147895516,29.5020806007706));
#77618=CARTESIAN_POINT('',(204.347155045812,9.53650002200871,29.4997461900754));
#77619=CARTESIAN_POINT('Ctrl Pts',(204.847155045794,9.53650147895644,29.5020806016713));
#77620=CARTESIAN_POINT('Ctrl Pts',(204.843480671734,9.5365975928036,29.5696872344555));
#77621=CARTESIAN_POINT('Ctrl Pts',(204.839806297674,9.54138208774555,29.6370889378409));
#77622=CARTESIAN_POINT('Ctrl Pts',(204.836131923613,9.55074824008612,29.70371938147));
#77623=CARTESIAN_POINT('Ctrl Pts',(204.832398190929,9.5602657003511,29.7714262237911));
#77624=CARTESIAN_POINT('Ctrl Pts',(204.828664458245,9.57451398745482,29.8383367658986));
#77625=CARTESIAN_POINT('Ctrl Pts',(204.824930725562,9.59333225587688,29.9038788279219));
#77626=CARTESIAN_POINT('Ctrl Pts',(204.823736517463,9.59935114647561,29.9248419947811));
#77627=CARTESIAN_POINT('Ctrl Pts',(204.822542309365,9.60583717740501,29.945665328066));
#77628=CARTESIAN_POINT('Ctrl Pts',(204.821348101266,9.61278405850875,29.9663305497955));
#77629=CARTESIAN_POINT('Ctrl Pts',(204.818357740167,9.63017942120929,30.0180773728522));
#77630=CARTESIAN_POINT('Ctrl Pts',(204.815367379068,9.65051610637708,30.0689738372223));
#77631=CARTESIAN_POINT('Ctrl Pts',(204.812377017968,9.67369195589128,30.1186592132447));
#77632=CARTESIAN_POINT('Ctrl Pts',(204.809392486883,9.69682262172008,30.1682477225524));
#77633=CARTESIAN_POINT('Ctrl Pts',(204.806407955799,9.72278124746231,30.216629345757));
#77634=CARTESIAN_POINT('Ctrl Pts',(204.803423424714,9.75141651626197,30.26346023743));
#77635=CARTESIAN_POINT('Ctrl Pts',(204.80044214556,9.78002058420834,30.310240102385));
#77636=CARTESIAN_POINT('Ctrl Pts',(204.797460866406,9.81129524343232,30.3554721258835));
#77637=CARTESIAN_POINT('Ctrl Pts',(204.794479587252,9.84504271709853,30.3988358719326));
#77638=CARTESIAN_POINT('Ctrl Pts',(204.791500335576,9.8787672401208,30.4421701275996));
#77639=CARTESIAN_POINT('Ctrl Pts',(204.788521083901,9.91496091787146,30.4836382002108));
#77640=CARTESIAN_POINT('Ctrl Pts',(204.785541832225,9.95338335630434,30.5229495838697));
#77641=CARTESIAN_POINT('Ctrl Pts',(204.782563386677,9.99179539837381,30.562250330634));
#77642=CARTESIAN_POINT('Ctrl Pts',(204.779584941129,10.0324346299407,30.5993951627963));
#77643=CARTESIAN_POINT('Ctrl Pts',(204.776606495581,10.0750228133266,30.6341293815671));
#77644=CARTESIAN_POINT('Ctrl Pts',(204.773625487682,10.1176476352518,30.6688934821253));
#77645=CARTESIAN_POINT('Ctrl Pts',(204.770644479783,10.1622243431096,30.7012424849852));
#77646=CARTESIAN_POINT('Ctrl Pts',(204.767663471883,10.2084417691068,30.7309621509637));
#77647=CARTESIAN_POINT('Ctrl Pts',(204.76468121849,10.2546785051806,30.760694234099));
#77648=CARTESIAN_POINT('Ctrl Pts',(204.761698965098,10.3025568579594,30.7877945260522));
#77649=CARTESIAN_POINT('Ctrl Pts',(204.758716711705,10.3517397670182,30.8120940973628));
#77650=CARTESIAN_POINT('Ctrl Pts',(204.755728826154,10.4010155608455,30.8364395598194));
#77651=CARTESIAN_POINT('Ctrl Pts',(204.752740940603,10.4516003371407,30.8579735262758));
#77652=CARTESIAN_POINT('Ctrl Pts',(204.749753055053,10.5031368856387,30.8765752052057));
#77653=CARTESIAN_POINT('Ctrl Pts',(204.747400770879,10.5437102628091,30.8912198206723));
#77654=CARTESIAN_POINT('Ctrl Pts',(204.745048486706,10.5848730993982,30.9040479657026));
#77655=CARTESIAN_POINT('Ctrl Pts',(204.742696202532,10.6264463316923,30.9150229351123));
#77656=CARTESIAN_POINT('Ctrl Pts',(204.739683723208,10.6796875617006,30.9290781537814));
#77657=CARTESIAN_POINT('Ctrl Pts',(204.736671243883,10.7338342815209,30.9401536806686));
#77658=CARTESIAN_POINT('Ctrl Pts',(204.733658764559,10.7885223279762,30.9481399946951));
#77659=CARTESIAN_POINT('Ctrl Pts',(204.730651668706,10.8431126438015,30.9561120367269));
#77660=CARTESIAN_POINT('Ctrl Pts',(204.727644572852,10.8982418488908,30.9610057468302));
#77661=CARTESIAN_POINT('Ctrl Pts',(204.724637476999,10.9535336079107,30.9627621557882));
#77662=CARTESIAN_POINT('Ctrl Pts',(204.721633374798,11.0087703223461,30.9645168161891));
#77663=CARTESIAN_POINT('Ctrl Pts',(204.718629272598,11.0641687458025,30.9631403463521));
#77664=CARTESIAN_POINT('Ctrl Pts',(204.715625170398,11.1193472528364,30.9586255459303));
#77665=CARTESIAN_POINT('Ctrl Pts',(204.712622877549,11.1744925261935,30.954113464745));
#77666=CARTESIAN_POINT('Ctrl Pts',(204.709620584701,11.2294176213348,30.9464668426916));
#77667=CARTESIAN_POINT('Ctrl Pts',(204.706618291853,11.2837430606454,30.9357305198176));
#77668=CARTESIAN_POINT('Ctrl Pts',(204.703616626739,11.3380571413316,30.9249964417456));
#77669=CARTESIAN_POINT('Ctrl Pts',(204.700614961625,11.3917712983336,30.9111740479915));
#77670=CARTESIAN_POINT('Ctrl Pts',(204.697613296511,11.4445156010062,30.8943593978821));
#77671=CARTESIAN_POINT('Ctrl Pts',(204.694608975607,11.4973065703731,30.8775298706372));
#77672=CARTESIAN_POINT('Ctrl Pts',(204.691604654702,11.5491254677475,30.8577029581842));
#77673=CARTESIAN_POINT('Ctrl Pts',(204.688600333798,11.599618372578,30.8350243657952));
#77674=CARTESIAN_POINT('Ctrl Pts',(204.685594677007,11.6501337293446,30.8123356892507));
#77675=CARTESIAN_POINT('Ctrl Pts',(204.682589020216,11.6993214493171,30.7867930478673));
#77676=CARTESIAN_POINT('Ctrl Pts',(204.679583363424,11.7468513984568,30.7585885898986));
#77677=CARTESIAN_POINT('Ctrl Pts',(204.67657221711,11.7944681561573,30.7303326193901));
#77678=CARTESIAN_POINT('Ctrl Pts',(204.673561070796,11.840420656537,30.6994054160022));
#77679=CARTESIAN_POINT('Ctrl Pts',(204.670549924482,11.8844080048257,30.6660423367101));
#77680=CARTESIAN_POINT('Ctrl Pts',(204.668381384254,11.9160864170777,30.6420152148005));
#77681=CARTESIAN_POINT('Ctrl Pts',(204.666212844026,11.9467462494712,30.6167256379604));
#77682=CARTESIAN_POINT('Ctrl Pts',(204.664044303798,11.9762868220711,30.5902734936934));
#77683=CARTESIAN_POINT('Ctrl Pts',(204.661028090037,12.017374684051,30.5534813140888));
#77684=CARTESIAN_POINT('Ctrl Pts',(204.658011876276,12.0564621266647,30.5142895979169));
#77685=CARTESIAN_POINT('Ctrl Pts',(204.654995662514,12.0932576001057,30.472944021931));
#77686=CARTESIAN_POINT('Ctrl Pts',(204.651984609947,12.1299901109792,30.4316691944195));
#77687=CARTESIAN_POINT('Ctrl Pts',(204.648973557379,12.1644380899798,30.3882482117569));
#77688=CARTESIAN_POINT('Ctrl Pts',(204.645962504812,12.1963456719334,30.3429645800663));
#77689=CARTESIAN_POINT('Ctrl Pts',(204.642954312931,12.2282229397049,30.2977239706346));
#77690=CARTESIAN_POINT('Ctrl Pts',(204.63994612105,12.2575642911831,30.2506246461356));
#77691=CARTESIAN_POINT('Ctrl Pts',(204.636937929169,12.2841543313563,30.2019828368691));
#77692=CARTESIAN_POINT('Ctrl Pts',(204.633931421654,12.3107294830621,30.1533682634392));
#77693=CARTESIAN_POINT('Ctrl Pts',(204.63092491414,12.3345561259627,30.1032133778017));
#77694=CARTESIAN_POINT('Ctrl Pts',(204.627918406625,12.3554636139356,30.0518610706478));
#77695=CARTESIAN_POINT('Ctrl Pts',(204.624912409678,12.3763675513833,30.0005174841813));
#77696=CARTESIAN_POINT('Ctrl Pts',(204.621906412731,12.3943531208892,29.9479773667534));
#77697=CARTESIAN_POINT('Ctrl Pts',(204.618900415784,12.4092977732584,29.8946036445458));
#77698=CARTESIAN_POINT('Ctrl Pts',(204.615891616779,12.4242563563722,29.8411801697128));
#77699=CARTESIAN_POINT('Ctrl Pts',(204.612882817774,12.4361682182349,29.7869220450714));
#77700=CARTESIAN_POINT('Ctrl Pts',(204.609874018769,12.4449611154638,29.7322059964722));
#77701=CARTESIAN_POINT('Ctrl Pts',(204.606863795824,12.4537581740084,29.6774640530233));
#77702=CARTESIAN_POINT('Ctrl Pts',(204.603853572879,12.4594332718064,29.6222642772503));
#77703=CARTESIAN_POINT('Ctrl Pts',(204.600843349933,12.4619660503887,29.5669889357338));
#77704=CARTESIAN_POINT('Ctrl Pts',(204.597827550221,12.4645035212199,29.5116111906123));
#77705=CARTESIAN_POINT('Ctrl Pts',(204.59481175051,12.4638870503377,29.4561581267354));
#77706=CARTESIAN_POINT('Ctrl Pts',(204.591795950798,12.460148443117,29.4010112427443));
#77707=CARTESIAN_POINT('Ctrl Pts',(204.589661435553,12.4575023409651,29.3619795178844));
#77708=CARTESIAN_POINT('Ctrl Pts',(204.587526920308,12.4532933123618,29.3231011244392));
#77709=CARTESIAN_POINT('Ctrl Pts',(204.585392405063,12.4475481247927,29.2845082915538));
#77710=CARTESIAN_POINT('Ctrl Pts',(204.582383124728,12.4394484496964,29.2300993791108));
#77711=CARTESIAN_POINT('Ctrl Pts',(204.579373844393,12.4282598493919,29.1760331613628));
#77712=CARTESIAN_POINT('Ctrl Pts',(204.576364564058,12.4140251108699,29.1226868199632));
#77713=CARTESIAN_POINT('Ctrl Pts',(204.573360635559,12.3998156880296,29.069435352031));
#77714=CARTESIAN_POINT('Ctrl Pts',(204.57035670706,12.3825710128448,29.016901726235));
#77715=CARTESIAN_POINT('Ctrl Pts',(204.567352778561,12.362385131464,28.9654543952422));
#77716=CARTESIAN_POINT('Ctrl Pts',(204.564351821726,12.3422192191539,28.9140579589998));
#77717=CARTESIAN_POINT('Ctrl Pts',(204.561350864892,12.3191180564608,28.863746178314));
#77718=CARTESIAN_POINT('Ctrl Pts',(204.558349908057,12.2932253495535,28.8148719497261));
#77719=CARTESIAN_POINT('Ctrl Pts',(204.555350732824,12.2673480145746,28.7660267366885));
#77720=CARTESIAN_POINT('Ctrl Pts',(204.552351557591,12.2386826671073,28.7186178501997));
#77721=CARTESIAN_POINT('Ctrl Pts',(204.549352382358,12.2074199818975,28.6729756730817));
#77722=CARTESIAN_POINT('Ctrl Pts',(204.54635380132,12.1761634904385,28.6273425385738));
#77723=CARTESIAN_POINT('Ctrl Pts',(204.543355220283,12.1423109816929,28.5834758540026));
#77724=CARTESIAN_POINT('Ctrl Pts',(204.540356639245,12.1060964142555,28.541676999978));
#77725=CARTESIAN_POINT('Ctrl Pts',(204.537355325727,12.069848846013,28.499840056424));
#77726=CARTESIAN_POINT('Ctrl Pts',(204.534354012209,12.0312352658389,28.4600751080151));
#77727=CARTESIAN_POINT('Ctrl Pts',(204.531352698691,11.9905289159791,28.4226492137612));
#77728=CARTESIAN_POINT('Ctrl Pts',(204.52835001098,11.9498039281474,28.385206183538));
#77729=CARTESIAN_POINT('Ctrl Pts',(204.525347323269,11.9069846700171,28.3501046777673));
#77730=CARTESIAN_POINT('Ctrl Pts',(204.522344635558,11.8623776271863,28.3175715336104));
#77731=CARTESIAN_POINT('Ctrl Pts',(204.519336359239,11.8176875616475,28.2849778387073));
#77732=CARTESIAN_POINT('Ctrl Pts',(204.51632808292,11.7712035099089,28.2549623410386));
#77733=CARTESIAN_POINT('Ctrl Pts',(204.513319806601,11.7232600749857,28.2277079289991));
#77734=CARTESIAN_POINT('Ctrl Pts',(204.51112670651,11.6883082486477,28.2078388587484));
#77735=CARTESIAN_POINT('Ctrl Pts',(204.50893360642,11.6525813804009,28.1894362919722));
#77736=CARTESIAN_POINT('Ctrl Pts',(204.506740506329,11.616215732215,28.1725549271737));
#77737=CARTESIAN_POINT('Ctrl Pts',(204.503728413225,11.5662696679212,28.1493693722983));
#77738=CARTESIAN_POINT('Ctrl Pts',(204.500716320121,11.5149098201128,28.1289586131801));
#77739=CARTESIAN_POINT('Ctrl Pts',(204.497704227016,11.4624755881642,28.1114941194391));
#77740=CARTESIAN_POINT('Ctrl Pts',(204.494697435409,11.4101336441761,28.0940603644436));
#77741=CARTESIAN_POINT('Ctrl Pts',(204.491690643802,11.3567215652475,28.0795627486606));
#77742=CARTESIAN_POINT('Ctrl Pts',(204.488683852195,11.3025995721126,28.0681250931184));
#77743=CARTESIAN_POINT('Ctrl Pts',(204.485680003688,11.2485305545185,28.0566986329507));
#77744=CARTESIAN_POINT('Ctrl Pts',(204.48267615518,11.1937535127567,28.0483263078363));
#77745=CARTESIAN_POINT('Ctrl Pts',(204.479672306672,11.1386429125202,28.0430818853457));
#77746=CARTESIAN_POINT('Ctrl Pts',(204.476670216574,11.0835645732319,28.0378405328641));
#77747=CARTESIAN_POINT('Ctrl Pts',(204.473668126476,11.0281535864119,28.0357235033241));
#77748=CARTESIAN_POINT('Ctrl Pts',(204.470666036378,10.9727913845649,28.0367529459295));
#77749=CARTESIAN_POINT('Ctrl Pts',(204.467664522619,10.9174398111179,28.0377821909031));
#77750=CARTESIAN_POINT('Ctrl Pts',(204.46466300886,10.8621375309362,28.0419566983604));
#77751=CARTESIAN_POINT('Ctrl Pts',(204.461661495101,10.8072655128246,28.0492465173389));
#77752=CARTESIAN_POINT('Ctrl Pts',(204.458657244735,10.7523434655693,28.0565429827542));
#77753=CARTESIAN_POINT('Ctrl Pts',(204.455652994369,10.6978529878251,28.066960364255));
#77754=CARTESIAN_POINT('Ctrl Pts',(204.452648744003,10.6441679554212,28.080417030938));
#77755=CARTESIAN_POINT('Ctrl Pts',(204.449643112758,10.5904582471296,28.0938798828682));
#77756=CARTESIAN_POINT('Ctrl Pts',(204.446637481513,10.5375552263495,28.1103846474473));
#77757=CARTESIAN_POINT('Ctrl Pts',(204.443631850267,10.4858174448169,28.1297998139157));
#77758=CARTESIAN_POINT('Ctrl Pts',(204.4406206558,10.4339839001211,28.149250916555));
#77759=CARTESIAN_POINT('Ctrl Pts',(204.437609461333,10.3833203862242,28.1716229680429));
#77760=CARTESIAN_POINT('Ctrl Pts',(204.434598266866,10.3341642058072,28.1967368089401));
#77761=CARTESIAN_POINT('Ctrl Pts',(204.432428380442,10.2987419407575,28.2148340069146));
#77762=CARTESIAN_POINT('Ctrl Pts',(204.430258494019,10.2641019226929,28.2343539436618));
#77763=CARTESIAN_POINT('Ctrl Pts',(204.428088607595,10.2303609019492,28.255215717985));
#77764=CARTESIAN_POINT('Ctrl Pts',(204.425076395235,10.1835219897325,28.2841758026142));
#77765=CARTESIAN_POINT('Ctrl Pts',(204.422064182875,10.1382231831636,28.3158430596894));
#77766=CARTESIAN_POINT('Ctrl Pts',(204.419051970515,10.0947943556126,28.3500282649694));
#77767=CARTESIAN_POINT('Ctrl Pts',(204.416045042677,10.0514417180964,28.3841534969063));
#77768=CARTESIAN_POINT('Ctrl Pts',(204.413038114838,10.0099529598516,28.4207875866823));
#77769=CARTESIAN_POINT('Ctrl Pts',(204.410031186999,9.9706296031815,28.4596977188558));
#77770=CARTESIAN_POINT('Ctrl Pts',(204.407027191949,9.93134460030811,28.4985699002687));
#77771=CARTESIAN_POINT('Ctrl Pts',(204.404023196899,9.89422118786101,28.5397133570908));
#77772=CARTESIAN_POINT('Ctrl Pts',(204.40101920185,9.8595269111191,28.5828558545471));
#77773=CARTESIAN_POINT('Ctrl Pts',(204.398016955171,9.82485282698333,28.6259732424021));
#77774=CARTESIAN_POINT('Ctrl Pts',(204.395014708493,9.79260540582357,28.6710869545319));
#77775=CARTESIAN_POINT('Ctrl Pts',(204.392012461815,9.76301290768435,28.7178905553284));
#77776=CARTESIAN_POINT('Ctrl Pts',(204.389010781698,9.73342599402148,28.7646853236972));
#77777=CARTESIAN_POINT('Ctrl Pts',(204.386009101582,9.70649328975003,28.8131689018786));
#77778=CARTESIAN_POINT('Ctrl Pts',(204.383007421465,9.68239928225008,28.8630065945515));
#77779=CARTESIAN_POINT('Ctrl Pts',(204.380002990889,9.65828319725208,28.912889953831));
#77780=CARTESIAN_POINT('Ctrl Pts',(204.376998560313,9.63701123510605,28.9641294306037));
#77781=CARTESIAN_POINT('Ctrl Pts',(204.373994129738,9.61872081752739,29.0163678359871));
#77782=CARTESIAN_POINT('Ctrl Pts',(204.370988310287,9.60042194473881,29.0686303898997));
#77783=CARTESIAN_POINT('Ctrl Pts',(204.367982490837,9.58510750986192,29.1218922853876));
#77784=CARTESIAN_POINT('Ctrl Pts',(204.364976671387,9.57286484592985,29.1757817062269));
#77785=CARTESIAN_POINT('Ctrl Pts',(204.36196527795,9.56059947922074,29.2297710595247));
#77786=CARTESIAN_POINT('Ctrl Pts',(204.358953884513,9.55141734928508,29.2843897415511));
#77787=CARTESIAN_POINT('Ctrl Pts',(204.355942491076,9.54535430667095,29.3392574826648));
#77788=CARTESIAN_POINT('Ctrl Pts',(204.353773897004,9.54098812917084,29.3787693766064));
#77789=CARTESIAN_POINT('Ctrl Pts',(204.351605302932,9.53823837420049,29.4184102735999));
#77790=CARTESIAN_POINT('Ctrl Pts',(204.349436708861,9.53710168569658,29.45803844607));
#77791=CARTESIAN_POINT('Ctrl Pts',(204.348676154521,9.53670303415301,29.4719365650972));
#77792=CARTESIAN_POINT('Ctrl Pts',(204.347915600182,9.53650243364758,29.4858404079313));
#77793=CARTESIAN_POINT('Ctrl Pts',(204.347155045843,9.5365000220088,29.4997461895053));
#77794=CARTESIAN_POINT('',(203.847155045875,9.53650022221242,29.4991935164512));
#77795=CARTESIAN_POINT('Ctrl Pts',(204.347155045812,9.5365000220087,29.4997461900754));
#77796=CARTESIAN_POINT('Ctrl Pts',(204.344157838136,9.53649051819596,29.5545463708471));
#77797=CARTESIAN_POINT('Ctrl Pts',(204.341160630459,9.53956326457731,29.6094653416477));
#77798=CARTESIAN_POINT('Ctrl Pts',(204.338163422783,9.54573220191339,29.6641262363192));
#77799=CARTESIAN_POINT('Ctrl Pts',(204.335171425959,9.55189041412612,29.7186920992526));
#77800=CARTESIAN_POINT('Ctrl Pts',(204.332179429135,9.5611340783862,29.7730002507101));
#77801=CARTESIAN_POINT('Ctrl Pts',(204.329187432311,9.5734251417044,29.8266747980468));
#77802=CARTESIAN_POINT('Ctrl Pts',(204.326198301077,9.58570443323677,29.8802979384987));
#77803=CARTESIAN_POINT('Ctrl Pts',(204.323209169843,9.60102522520536,29.9332881593667));
#77804=CARTESIAN_POINT('Ctrl Pts',(204.320220038609,9.61929804605378,29.9852776157717));
#77805=CARTESIAN_POINT('Ctrl Pts',(204.317232562801,9.63756074713743,30.0372382796289));
#77806=CARTESIAN_POINT('Ctrl Pts',(204.314245086993,9.65877206070803,30.0881987752968));
#77807=CARTESIAN_POINT('Ctrl Pts',(204.311257611186,9.68279275238454,30.1378066453317));
#77808=CARTESIAN_POINT('Ctrl Pts',(204.308270583197,9.70680984338501,30.1874070791999));
#77809=CARTESIAN_POINT('Ctrl Pts',(204.305283555209,9.73363524307626,30.2356548108838));
#77810=CARTESIAN_POINT('Ctrl Pts',(204.30229652722,9.76308267958039,30.282219785256));
#77811=CARTESIAN_POINT('Ctrl Pts',(204.299306701674,9.79255769563509,30.3288283709309));
#77812=CARTESIAN_POINT('Ctrl Pts',(204.296316876129,9.8246593653189,30.3737506016701));
#77813=CARTESIAN_POINT('Ctrl Pts',(204.293327050583,9.85915762894708,30.4166847519242));
#77814=CARTESIAN_POINT('Ctrl Pts',(204.290335680551,9.89367371370784,30.459641081126));
#77815=CARTESIAN_POINT('Ctrl Pts',(204.28734431052,9.93058849989877,30.5006068889149));
#77816=CARTESIAN_POINT('Ctrl Pts',(204.284352940488,9.96963329689886,30.5393154993266));
#77817=CARTESIAN_POINT('Ctrl Pts',(204.281356237518,10.0087477019789,30.5780931184732));
#77818=CARTESIAN_POINT('Ctrl Pts',(204.278359534547,10.0499992970677,30.614605155808));
#77819=CARTESIAN_POINT('Ctrl Pts',(204.275362831577,10.0930854954961,30.6486245389685));
#77820=CARTESIAN_POINT('Ctrl Pts',(204.273836824426,10.1150262241966,30.6659481851407));
#77821=CARTESIAN_POINT('Ctrl Pts',(204.272310817276,10.1374422109402,30.6826261395129));
#77822=CARTESIAN_POINT('Ctrl Pts',(204.270784810126,10.1602908369858,30.6986328760509));
#77823=CARTESIAN_POINT('Ctrl Pts',(204.267772962681,10.2053866781029,30.7302250272062));
#77824=CARTESIAN_POINT('Ctrl Pts',(204.264761115235,10.2523612927625,30.7593341490075));
#77825=CARTESIAN_POINT('Ctrl Pts',(204.26174926779,10.3009107130304,30.7857318611765));
#77826=CARTESIAN_POINT('Ctrl Pts',(204.258742718615,10.3493747279248,30.8120831359946));
#77827=CARTESIAN_POINT('Ctrl Pts',(204.25573616944,10.3994075908154,30.8357322173006));
#77828=CARTESIAN_POINT('Ctrl Pts',(204.252729620265,10.4506764672343,30.8564939757882));
#77829=CARTESIAN_POINT('Ctrl Pts',(204.249726012003,10.5018951940337,30.8772354257699));
#77830=CARTESIAN_POINT('Ctrl Pts',(204.246722403741,10.5543470526839,30.8950949511008));
#77831=CARTESIAN_POINT('Ctrl Pts',(204.243718795479,10.6076763956723,30.9099341968643));
#77832=CARTESIAN_POINT('Ctrl Pts',(204.240716942985,10.6609745648372,30.9247647683033));
#77833=CARTESIAN_POINT('Ctrl Pts',(204.237715090491,10.7151486944926,30.9365784187188));
#77834=CARTESIAN_POINT('Ctrl Pts',(204.234713237996,10.7698272156219,30.945286386614));
#77835=CARTESIAN_POINT('Ctrl Pts',(204.231711958743,10.8244952952208,30.9539926916165));
#77836=CARTESIAN_POINT('Ctrl Pts',(204.228710679489,10.8796670544413,30.9595944092412));
#77837=CARTESIAN_POINT('Ctrl Pts',(204.225709400235,10.934962234592,30.9620541505261));
#77838=CARTESIAN_POINT('Ctrl Pts',(204.222705377653,10.9903079574679,30.964516140145));
#77839=CARTESIAN_POINT('Ctrl Pts',(204.219701355071,11.0457767986833,30.9638303927569));
#77840=CARTESIAN_POINT('Ctrl Pts',(204.216697332489,11.1009864101636,30.960011642064));
#77841=CARTESIAN_POINT('Ctrl Pts',(204.213691925611,11.1562214630015,30.9561911316375));
#77842=CARTESIAN_POINT('Ctrl Pts',(204.210686518734,11.2111965239212,30.9492348063404));
#77843=CARTESIAN_POINT('Ctrl Pts',(204.207681111856,11.2655355774917,30.9392091950395));
#77844=CARTESIAN_POINT('Ctrl Pts',(204.20467013339,11.3199753678007,30.9291649977066));
#77845=CARTESIAN_POINT('Ctrl Pts',(204.201659154923,11.373776282128,30.9160402739218));
#77846=CARTESIAN_POINT('Ctrl Pts',(204.198648176456,11.4265748620129,30.8999521910046));
#77847=CARTESIAN_POINT('Ctrl Pts',(204.196476421435,11.4646573598624,30.8883481974043));
#77848=CARTESIAN_POINT('Ctrl Pts',(204.194304666413,11.50221868849,30.8752036044538));
#77849=CARTESIAN_POINT('Ctrl Pts',(204.192132911392,11.5391293734927,30.8605777334049));
#77850=CARTESIAN_POINT('Ctrl Pts',(204.189121084306,11.5903177440722,30.8402943247595));
#77851=CARTESIAN_POINT('Ctrl Pts',(204.186109257221,11.640465895444,30.8170761320679));
#77852=CARTESIAN_POINT('Ctrl Pts',(204.183097430135,11.6892159062062,30.7910513872935));
#77853=CARTESIAN_POINT('Ctrl Pts',(204.180090900248,11.7378801754961,30.7650724148152));
#77854=CARTESIAN_POINT('Ctrl Pts',(204.177084370361,11.7851507228236,30.7362969329501));
#77855=CARTESIAN_POINT('Ctrl Pts',(204.174077840474,11.8306898690518,30.7049010712314));
#77856=CARTESIAN_POINT('Ctrl Pts',(204.171074250825,11.876184480235,30.6735359131212));
#77857=CARTESIAN_POINT('Ctrl Pts',(204.168070661177,11.9199506126271,30.6395557498172));
#77858=CARTESIAN_POINT('Ctrl Pts',(204.165067071528,11.9616771018297,30.6031814908783));
#77859=CARTESIAN_POINT('Ctrl Pts',(204.162065236937,12.0033792094018,30.5668284861535));
#77860=CARTESIAN_POINT('Ctrl Pts',(204.159063402347,12.0430436394359,30.5280845046444));
#77861=CARTESIAN_POINT('Ctrl Pts',(204.156061567756,12.0803918872799,30.4872110310869));
#77862=CARTESIAN_POINT('Ctrl Pts',(204.15306030566,12.117733012261,30.446345352705));
#77863=CARTESIAN_POINT('Ctrl Pts',(204.150059043563,12.1527584769296,30.4033513780991));
#77864=CARTESIAN_POINT('Ctrl Pts',(204.147057781467,12.1852279000695,30.3585261061242));
#77865=CARTESIAN_POINT('Ctrl Pts',(204.144053774743,12.2177270162089,30.3136598418356));
#77866=CARTESIAN_POINT('Ctrl Pts',(204.141049768019,12.2476651112891,30.266959362668));
#77867=CARTESIAN_POINT('Ctrl Pts',(204.138045761295,12.2748441843811,30.2187520821185));
#77868=CARTESIAN_POINT('Ctrl Pts',(204.135040369574,12.3020357883833,30.1705225756048));
#77869=CARTESIAN_POINT('Ctrl Pts',(204.132034977853,12.3264656018709,30.1207853570473));
#77870=CARTESIAN_POINT('Ctrl Pts',(204.129029586132,12.3479823633306,30.0698910405942));
#77871=CARTESIAN_POINT('Ctrl Pts',(204.126018621485,12.369539023521,30.0189023503374));
#77872=CARTESIAN_POINT('Ctrl Pts',(204.123007656838,12.3881716640522,29.9667527740701));
#77873=CARTESIAN_POINT('Ctrl Pts',(204.119996692191,12.4037782203796,29.9138102922692));
#77874=CARTESIAN_POINT('Ctrl Pts',(204.117824799013,12.4150356668097,29.8756213965095));
#77875=CARTESIAN_POINT('Ctrl Pts',(204.115652905836,12.4247196494047,29.8370202873807));
#77876=CARTESIAN_POINT('Ctrl Pts',(204.113481012658,12.4328084900551,29.7981477499932));
#77877=CARTESIAN_POINT('Ctrl Pts',(204.110469256761,12.4440252542029,29.7442433522497));
#77878=CARTESIAN_POINT('Ctrl Pts',(204.107457500864,12.4522190964014,29.6895933604676));
#77879=CARTESIAN_POINT('Ctrl Pts',(204.104445744967,12.457300215849,29.6345671984045));
#77880=CARTESIAN_POINT('Ctrl Pts',(204.101439288488,12.462372394673,29.5796378591404));
#77881=CARTESIAN_POINT('Ctrl Pts',(204.098432832009,12.4643426724083,29.5243341842346));
#77882=CARTESIAN_POINT('Ctrl Pts',(204.09542637553,12.4631723826498,29.4690350415631));
#77883=CARTESIAN_POINT('Ctrl Pts',(204.092422860591,12.4620032379115,29.4137900039894));
#77884=CARTESIAN_POINT('Ctrl Pts',(204.089419345651,12.4576996241724,29.3585500146394));
#77885=CARTESIAN_POINT('Ctrl Pts',(204.086415830712,12.4502748564698,29.3036964323008));
#77886=CARTESIAN_POINT('Ctrl Pts',(204.083414071992,12.4428544301871,29.2488749240199));
#77887=CARTESIAN_POINT('Ctrl Pts',(204.080412313272,12.43231653811,29.1944398965253));
#77888=CARTESIAN_POINT('Ctrl Pts',(204.077410554552,12.4187263455936,29.1407677543447));
#77889=CARTESIAN_POINT('Ctrl Pts',(204.074409369348,12.405138749622,29.0871058667736));
#77890=CARTESIAN_POINT('Ctrl Pts',(204.071408184144,12.3885001409816,29.0342070859916));
#77891=CARTESIAN_POINT('Ctrl Pts',(204.068406998941,12.3689263142868,28.9824355150775));
#77892=CARTESIAN_POINT('Ctrl Pts',(204.065403070076,12.3493345933454,28.9306166149786));
#77893=CARTESIAN_POINT('Ctrl Pts',(204.062399141211,12.3268024807935,28.8799274776847));
#77894=CARTESIAN_POINT('Ctrl Pts',(204.059395212347,12.3014944833725,28.8307135443244));
#77895=CARTESIAN_POINT('Ctrl Pts',(204.056389899139,12.2761748229078,28.7814769310083));
#77896=CARTESIAN_POINT('Ctrl Pts',(204.053384585931,12.248076995451,28.7337173321117));
#77897=CARTESIAN_POINT('Ctrl Pts',(204.050379272723,12.2174105930739,28.6877539179095));
#77898=CARTESIAN_POINT('Ctrl Pts',(204.04736838669,12.1866873252437,28.6417052726342));
#77899=CARTESIAN_POINT('Ctrl Pts',(204.044357500657,12.1533862863945,28.5974598874003));
#77900=CARTESIAN_POINT('Ctrl Pts',(204.041346614624,12.1177586332827,28.5553053997603));
#77901=CARTESIAN_POINT('Ctrl Pts',(204.03917411439,12.0920515544219,28.5248888933827));
#77902=CARTESIAN_POINT('Ctrl Pts',(204.037001614157,12.0651340326139,28.4955602891252));
#77903=CARTESIAN_POINT('Ctrl Pts',(204.034829113924,12.0371118107902,28.4674152132055));
#77904=CARTESIAN_POINT('Ctrl Pts',(204.031817315547,11.9982638139436,28.4283969002588));
#77905=CARTESIAN_POINT('Ctrl Pts',(204.02880551717,11.9571303355798,28.3914930956449));
#77906=CARTESIAN_POINT('Ctrl Pts',(204.025793718793,11.9139705116544,28.3569819975931));
#77907=CARTESIAN_POINT('Ctrl Pts',(204.022787218906,11.8708866164197,28.3225316130071));
#77908=CARTESIAN_POINT('Ctrl Pts',(204.01978071902,11.8257838590416,28.2904659078781));
#77909=CARTESIAN_POINT('Ctrl Pts',(204.016774219133,11.7789573881038,28.2610255702726));
#77910=CARTESIAN_POINT('Ctrl Pts',(204.013770660253,11.7321767235706,28.2316140316772));
#77911=CARTESIAN_POINT('Ctrl Pts',(204.010767101372,11.6836761302667,28.2048230521918));
#77912=CARTESIAN_POINT('Ctrl Pts',(204.007763542492,11.6337814284563,28.1808512779281));
#77913=CARTESIAN_POINT('Ctrl Pts',(204.00476173938,11.583915893227,28.1568935166692));
#77914=CARTESIAN_POINT('Ctrl Pts',(204.001759936269,11.5326583393508,28.135751921877));
#77915=CARTESIAN_POINT('Ctrl Pts',(203.998758133157,11.4803589690574,28.117579112265));
#77916=CARTESIAN_POINT('Ctrl Pts',(203.995756903193,11.4280695845194,28.0994097724697));
#77917=CARTESIAN_POINT('Ctrl Pts',(203.992755673229,11.3747392765915,28.0842082649166));
#77918=CARTESIAN_POINT('Ctrl Pts',(203.989754443265,11.3207358221199,28.0720781595588));
#77919=CARTESIAN_POINT('Ctrl Pts',(203.986750469429,11.2666829950394,28.0599369642632));
#77920=CARTESIAN_POINT('Ctrl Pts',(203.983746495593,11.2119563076499,28.0508728965026));
#77921=CARTESIAN_POINT('Ctrl Pts',(203.980742521758,11.1569347452221,28.0449385800792));
#77922=CARTESIAN_POINT('Ctrl Pts',(203.977737163395,11.1018878234405,28.0390015285384));
#77923=CARTESIAN_POINT('Ctrl Pts',(203.974731805032,11.0465462832934,28.0361971304803));
#77924=CARTESIAN_POINT('Ctrl Pts',(203.971726446669,10.9912919693594,28.0365259072323));
#77925=CARTESIAN_POINT('Ctrl Pts',(203.968715515739,10.9359352022784,28.0368552936056));
#77926=CARTESIAN_POINT('Ctrl Pts',(203.965704584808,10.8806665119796,28.0403294261408));
#77927=CARTESIAN_POINT('Ctrl Pts',(203.962693653877,10.8258642715793,28.0468967696384));
#77928=CARTESIAN_POINT('Ctrl Pts',(203.960521507648,10.786328831353,28.0516345835379));
#77929=CARTESIAN_POINT('Ctrl Pts',(203.958349361419,10.7470360572612,28.057981147903));
#77930=CARTESIAN_POINT('Ctrl Pts',(203.95617721519,10.7081239039327,28.0659007724204));
#77931=CARTESIAN_POINT('Ctrl Pts',(203.953165422799,10.65417020333,28.0768817388678));
#77932=CARTESIAN_POINT('Ctrl Pts',(203.950153630408,10.6007252515191,28.0909344586892));
#77933=CARTESIAN_POINT('Ctrl Pts',(203.947141838017,10.548163917446,28.107995544367));
#77934=CARTESIAN_POINT('Ctrl Pts',(203.944135344093,10.4956950513916,28.1250266154947));
#77935=CARTESIAN_POINT('Ctrl Pts',(203.941128850168,10.4441072157058,28.145055387586));
#77936=CARTESIAN_POINT('Ctrl Pts',(203.938122356244,10.3937637624352,28.1679677653062));
#77937=CARTESIAN_POINT('Ctrl Pts',(203.935118803306,10.3434695557084,28.1908577298756));
#77938=CARTESIAN_POINT('Ctrl Pts',(203.932115250369,10.2944177976082,28.2166254944475));
#77939=CARTESIAN_POINT('Ctrl Pts',(203.929111697431,10.2469536008031,28.2451082235282));
#77940=CARTESIAN_POINT('Ctrl Pts',(203.926109900231,10.1995171493656,28.2735743029268));
#77941=CARTESIAN_POINT('Ctrl Pts',(203.923108103031,10.1536668710415,28.3047519301131));
#77942=CARTESIAN_POINT('Ctrl Pts',(203.920106305832,10.1097228510496,28.3384325899644));
#77943=CARTESIAN_POINT('Ctrl Pts',(203.917105081738,10.06578722089,28.3721068194735));
#77944=CARTESIAN_POINT('Ctrl Pts',(203.914103857644,10.0237575445048,28.4082828117572));
#77945=CARTESIAN_POINT('Ctrl Pts',(203.91110263355,9.9839226120019,28.4467103951909));
#77946=CARTESIAN_POINT('Ctrl Pts',(203.908098665471,9.94405125887923,28.4851731125213));
#77947=CARTESIAN_POINT('Ctrl Pts',(203.905094697393,9.90637903858919,28.5258911664901));
#77948=CARTESIAN_POINT('Ctrl Pts',(203.902090729314,9.87115835981009,28.5685770019087));
#77949=CARTESIAN_POINT('Ctrl Pts',(203.899085376654,9.83592144720398,28.6112825119756));
#77950=CARTESIAN_POINT('Ctrl Pts',(203.896080023994,9.80313864104508,28.6559571855371));
#77951=CARTESIAN_POINT('Ctrl Pts',(203.893074671334,9.77302041041059,28.702282420445));
#77952=CARTESIAN_POINT('Ctrl Pts',(203.890063745946,9.74284633252009,28.7486935547302));
#77953=CARTESIAN_POINT('Ctrl Pts',(203.887052820559,9.715346961854,28.7967609050465));
#77954=CARTESIAN_POINT('Ctrl Pts',(203.884041895171,9.69068738400953,28.8461401345791));
#77955=CARTESIAN_POINT('Ctrl Pts',(203.881869702266,9.67289705275423,28.8817641365818));
#77956=CARTESIAN_POINT('Ctrl Pts',(203.879697509361,9.65658377891154,28.9180704083684));
#77957=CARTESIAN_POINT('Ctrl Pts',(203.877525316456,9.64179364143364,28.9549240992762));
#77958=CARTESIAN_POINT('Ctrl Pts',(203.874154072383,9.61883934340668,29.0121210391798));
#77959=CARTESIAN_POINT('Ctrl Pts',(203.87078282831,9.59947538062231,29.070836036723));
#77960=CARTESIAN_POINT('Ctrl Pts',(203.867411584237,9.58387900170179,29.1306308510732));
#77961=CARTESIAN_POINT('Ctrl Pts',(203.86403549451,9.56826020534381,29.1905116114317));
#77962=CARTESIAN_POINT('Ctrl Pts',(203.860659404783,9.55642003399269,29.2514750466615));
#77963=CARTESIAN_POINT('Ctrl Pts',(203.857283315056,9.54848858019345,29.3130592388718));
#77964=CARTESIAN_POINT('Ctrl Pts',(203.853907225329,9.54055712639421,29.3746434310822));
#77965=CARTESIAN_POINT('Ctrl Pts',(203.850531135602,9.53653457858967,29.4368481027865));
#77966=CARTESIAN_POINT('Ctrl Pts',(203.847155045875,9.53650022221242,29.4991935164512));
#77967=CARTESIAN_POINT('',(203.34715504581,9.53650055029319,29.501269136656));
#77968=CARTESIAN_POINT('Ctrl Pts',(203.847155045843,9.5365002222121,29.4991935170432));
#77969=CARTESIAN_POINT('Ctrl Pts',(203.844124084037,9.53646937801091,29.5551655387819));
#77970=CARTESIAN_POINT('Ctrl Pts',(203.841093122232,9.539653874786,29.6111435828041));
#77971=CARTESIAN_POINT('Ctrl Pts',(203.838062160426,9.54602940369895,29.6667385830934));
#77972=CARTESIAN_POINT('Ctrl Pts',(203.835030400788,9.55240661082483,29.7223482175014));
#77973=CARTESIAN_POINT('Ctrl Pts',(203.831998641151,9.56197645602609,29.7775740993723));
#77974=CARTESIAN_POINT('Ctrl Pts',(203.828966881513,9.57466299303777,29.8320341346668));
#77975=CARTESIAN_POINT('Ctrl Pts',(203.825930949368,9.58736699009728,29.8865691214489));
#77976=CARTESIAN_POINT('Ctrl Pts',(203.822895017224,9.60319611861329,29.9403356592167));
#77977=CARTESIAN_POINT('Ctrl Pts',(203.819859085079,9.62202399893718,29.9929648978324));
#77978=CARTESIAN_POINT('Ctrl Pts',(203.816820713817,9.64086700588681,30.0456364196357));
#77979=CARTESIAN_POINT('Ctrl Pts',(203.813782342554,9.66271335885688,30.0971683524208));
#77980=CARTESIAN_POINT('Ctrl Pts',(203.810743971292,9.68738900762656,30.147212973217));
#77981=CARTESIAN_POINT('Ctrl Pts',(203.80769969221,9.71211263581529,30.1973549009515));
#77982=CARTESIAN_POINT('Ctrl Pts',(203.804655413128,9.7396762840394,30.2460033012221));
#77983=CARTESIAN_POINT('Ctrl Pts',(203.801611134046,9.76986121827386,30.2928372012547));
#77984=CARTESIAN_POINT('Ctrl Pts',(203.800698561938,9.77890964265523,30.3068764235911));
#77985=CARTESIAN_POINT('Ctrl Pts',(203.799785989829,9.7881933350171,30.3207528145843));
#77986=CARTESIAN_POINT('Ctrl Pts',(203.798873417721,9.79770570570672,30.334458315262));
#77987=CARTESIAN_POINT('Ctrl Pts',(203.795861627085,9.82909968402081,30.3796910133031));
#77988=CARTESIAN_POINT('Ctrl Pts',(203.792849836448,9.86311487818565,30.4232433266164));
#77989=CARTESIAN_POINT('Ctrl Pts',(203.789838045812,9.89954502329002,30.4647958821607));
#77990=CARTESIAN_POINT('Ctrl Pts',(203.786831553754,9.93591107761387,30.5062753351766));
#77991=CARTESIAN_POINT('Ctrl Pts',(203.783825061697,9.97468330624121,30.5457616190503));
#77992=CARTESIAN_POINT('Ctrl Pts',(203.78081856964,10.0156134051945,30.5829659652857));
#77993=CARTESIAN_POINT('Ctrl Pts',(203.777815018637,10.0565034649099,30.6201339169434));
#77994=CARTESIAN_POINT('Ctrl Pts',(203.774811467634,10.0995468246674,30.6550240002376));
#77995=CARTESIAN_POINT('Ctrl Pts',(203.771807916632,10.1444576037548,30.6873834503761));
#77996=CARTESIAN_POINT('Ctrl Pts',(203.768806121431,10.1893421291104,30.7197239839795));
#77997=CARTESIAN_POINT('Ctrl Pts',(203.76580432623,10.2360914828389,30.749536509104));
#77998=CARTESIAN_POINT('Ctrl Pts',(203.762802531029,10.2843876997944,30.7766092925381));
#77999=CARTESIAN_POINT('Ctrl Pts',(203.759801308994,10.3326746950134,30.803676906663));
#78000=CARTESIAN_POINT('Ctrl Pts',(203.756800086959,10.382507506974,30.8280055604714));
#78001=CARTESIAN_POINT('Ctrl Pts',(203.753798864924,10.4335422572665,30.8494287219773));
#78002=CARTESIAN_POINT('Ctrl Pts',(203.750794898982,10.4846236667601,30.8708714698944));
#78003=CARTESIAN_POINT('Ctrl Pts',(203.74779093304,10.5369087224968,30.8894032143634));
#78004=CARTESIAN_POINT('Ctrl Pts',(203.744786967098,10.5900335670003,30.9049056102862));
#78005=CARTESIAN_POINT('Ctrl Pts',(203.741781616621,10.6431828968728,30.9204151513006));
#78006=CARTESIAN_POINT('Ctrl Pts',(203.738776266144,10.6971722723627,30.9328924416287));
#78007=CARTESIAN_POINT('Ctrl Pts',(203.735770915667,10.7516258733907,30.9422699273129));
#78008=CARTESIAN_POINT('Ctrl Pts',(203.732759992511,10.8061804451494,30.9516648012241));
#78009=CARTESIAN_POINT('Ctrl Pts',(203.729749069355,10.8612004367267,30.9579483293454));
#78010=CARTESIAN_POINT('Ctrl Pts',(203.726738146199,10.916304305951,30.9611048151305));
#78011=CARTESIAN_POINT('Ctrl Pts',(203.724565937128,10.9560586000169,30.9633820393234));
#78012=CARTESIAN_POINT('Ctrl Pts',(203.722393728058,10.9958564520451,30.9640328028313));
#78013=CARTESIAN_POINT('Ctrl Pts',(203.720221518987,11.0355557713552,30.9630680220425));
#78014=CARTESIAN_POINT('Ctrl Pts',(203.717209729415,11.0905992740848,30.9617303438429));
#78015=CARTESIAN_POINT('Ctrl Pts',(203.714197939843,11.1456812449634,30.9572793119509));
#78016=CARTESIAN_POINT('Ctrl Pts',(203.711186150272,11.2004215096717,30.9497115121502));
#78017=CARTESIAN_POINT('Ctrl Pts',(203.708179659287,11.2550654708113,30.9421570262444));
#78018=CARTESIAN_POINT('Ctrl Pts',(203.705173168303,11.3093684005256,30.9314967261666));
#78019=CARTESIAN_POINT('Ctrl Pts',(203.702166677319,11.3629525595331,30.9177791398975));
#78020=CARTESIAN_POINT('Ctrl Pts',(203.699163127393,11.416484300571,30.9040749726691));
#78021=CARTESIAN_POINT('Ctrl Pts',(203.696159577467,11.4692981553777,30.8873195743526));
#78022=CARTESIAN_POINT('Ctrl Pts',(203.693156027541,11.5210257832318,30.8676126583239));
#78023=CARTESIAN_POINT('Ctrl Pts',(203.69015423342,11.5727231723453,30.8479172624894));
#78024=CARTESIAN_POINT('Ctrl Pts',(203.687152439298,11.6233351012891,30.8252739564425));
#78025=CARTESIAN_POINT('Ctrl Pts',(203.684150645176,11.6725098478943,30.7998318177692));
#78026=CARTESIAN_POINT('Ctrl Pts',(203.68114942422,11.7216752050103,30.7743945370505));
#78027=CARTESIAN_POINT('Ctrl Pts',(203.678148203265,11.7694034567133,30.7461597274536));
#78028=CARTESIAN_POINT('Ctrl Pts',(203.67514698231,11.8153663760569,30.7153229705703));
#78029=CARTESIAN_POINT('Ctrl Pts',(203.672143017438,11.8613713177592,30.6844580206723));
#78030=CARTESIAN_POINT('Ctrl Pts',(203.669139052567,11.9056072640122,30.6509866657256));
#78031=CARTESIAN_POINT('Ctrl Pts',(203.666135087696,11.947775240633,30.6151476777732));
#78032=CARTESIAN_POINT('Ctrl Pts',(203.663129738286,11.989962652628,30.5792921715007));
#78033=CARTESIAN_POINT('Ctrl Pts',(203.660124388876,12.0300798126047,30.5410672213843));
#78034=CARTESIAN_POINT('Ctrl Pts',(203.657119039466,12.0678635835183,30.5007495276019));
#78035=CARTESIAN_POINT('Ctrl Pts',(203.654108117359,12.105717415344,30.4603570743573));
#78036=CARTESIAN_POINT('Ctrl Pts',(203.651097195252,12.1412288766431,30.4178645318039));
#78037=CARTESIAN_POINT('Ctrl Pts',(203.648086273145,12.1741749905951,30.3735819031213));
#78038=CARTESIAN_POINT('Ctrl Pts',(203.645914055515,12.1979438318497,30.3416343789602));
#78039=CARTESIAN_POINT('Ctrl Pts',(203.643741837884,12.2203783159573,30.3087558315153));
#78040=CARTESIAN_POINT('Ctrl Pts',(203.641569620253,12.2414094013503,30.2750709311018));
#78041=CARTESIAN_POINT('Ctrl Pts',(203.638557831265,12.2705690907379,30.2283666733448));
#78042=CARTESIAN_POINT('Ctrl Pts',(203.635546042277,12.2971498863831,30.1799177811609));
#78043=CARTESIAN_POINT('Ctrl Pts',(203.632534253288,12.3209398209639,30.1300398712716));
#78044=CARTESIAN_POINT('Ctrl Pts',(203.62952776291,12.3446879021526,30.0802497110863));
#78045=CARTESIAN_POINT('Ctrl Pts',(203.626521272532,12.3656546412535,30.0290359948511));
#78046=CARTESIAN_POINT('Ctrl Pts',(203.623514782154,12.3836727888111,29.9767408766863));
#78047=CARTESIAN_POINT('Ctrl Pts',(203.620511232848,12.4016733102795,29.924496915746));
#78048=CARTESIAN_POINT('Ctrl Pts',(203.617507683542,12.4167307835348,29.8711741448606));
#78049=CARTESIAN_POINT('Ctrl Pts',(203.614504134235,12.4287258752695,29.8171350238235));
#78050=CARTESIAN_POINT('Ctrl Pts',(203.611502340745,12.4407139549089,29.7631274929957));
#78051=CARTESIAN_POINT('Ctrl Pts',(203.608500547255,12.4496430875533,29.7084049559746));
#78052=CARTESIAN_POINT('Ctrl Pts',(203.605498753764,12.4554443064973,29.6533431468458));
#78053=CARTESIAN_POINT('Ctrl Pts',(203.602497533452,12.4612444177277,29.598291851493));
#78054=CARTESIAN_POINT('Ctrl Pts',(203.599496313139,12.4639177463926,29.5429019369228));
#78055=CARTESIAN_POINT('Ctrl Pts',(203.596495092826,12.4634470862822,29.4875550953341));
#78056=CARTESIAN_POINT('Ctrl Pts',(203.593491128609,12.4629759958648,29.4321576521885));
#78057=CARTESIAN_POINT('Ctrl Pts',(203.590487164392,12.4593551789945,29.3768038891747));
#78058=CARTESIAN_POINT('Ctrl Pts',(203.587483200175,12.4526195896628,29.3218748256762));
#78059=CARTESIAN_POINT('Ctrl Pts',(203.584477851427,12.4458808958898,29.2669204453052));
#78060=CARTESIAN_POINT('Ctrl Pts',(203.58147250268,12.4360246619534,29.2123916744794));
#78061=CARTESIAN_POINT('Ctrl Pts',(203.578467153932,12.4231372290841,29.1586604664052));
#78062=CARTESIAN_POINT('Ctrl Pts',(203.575456232491,12.4102258995844,29.1048296267877));
#78063=CARTESIAN_POINT('Ctrl Pts',(203.57244531105,12.3942722963167,29.0517998101152));
#78064=CARTESIAN_POINT('Ctrl Pts',(203.56943438961,12.3754126630898,28.999927749008));
#78065=CARTESIAN_POINT('Ctrl Pts',(203.567262166913,12.3618064218923,28.9625047638233));
#78066=CARTESIAN_POINT('Ctrl Pts',(203.565089944216,12.3466886812148,28.9256840308773));
#78067=CARTESIAN_POINT('Ctrl Pts',(203.562917721519,12.3301255809467,28.8895917850231));
#78068=CARTESIAN_POINT('Ctrl Pts',(203.559905931974,12.3071608212593,28.8395498400247));
#78069=CARTESIAN_POINT('Ctrl Pts',(203.556894142429,12.2813205365589,28.7907019662624));
#78070=CARTESIAN_POINT('Ctrl Pts',(203.553882352884,12.2527517147781,28.7433987899029));
#78071=CARTESIAN_POINT('Ctrl Pts',(203.550875861935,12.2242331536969,28.6961788333118));
#78072=CARTESIAN_POINT('Ctrl Pts',(203.547869370986,12.1929958526426,28.6504986287517));
#78073=CARTESIAN_POINT('Ctrl Pts',(203.544862880037,12.1592335589007,28.6066860541118));
#78074=CARTESIAN_POINT('Ctrl Pts',(203.541859330152,12.1255042927199,28.5629163386004));
#78075=CARTESIAN_POINT('Ctrl Pts',(203.538855780267,12.0892552476063,28.5210110493451));
#78076=CARTESIAN_POINT('Ctrl Pts',(203.535852230382,12.0507234851196,28.481269217203));
#78077=CARTESIAN_POINT('Ctrl Pts',(203.532850436306,12.0122142474516,28.4415506172598));
#78078=CARTESIAN_POINT('Ctrl Pts',(203.52984864223,11.9714253039502,28.4039933454117));
#78079=CARTESIAN_POINT('Ctrl Pts',(203.526846848154,11.9286325062115,28.3688616714091));
#78080=CARTESIAN_POINT('Ctrl Pts',(203.52384562725,11.8858478794577,28.3337367055535));
#78081=CARTESIAN_POINT('Ctrl Pts',(203.520844406346,11.8410605658907,28.301036752032));
#78082=CARTESIAN_POINT('Ctrl Pts',(203.517843185441,11.7945798638993,28.2709861311256));
#78083=CARTESIAN_POINT('Ctrl Pts',(203.514839220628,11.7480566662743,28.2409080360176));
#78084=CARTESIAN_POINT('Ctrl Pts',(203.511835255816,11.6998374312439,28.2134843992042));
#78085=CARTESIAN_POINT('Ctrl Pts',(203.508831291003,11.6502595861629,28.1888956103333));
#78086=CARTESIAN_POINT('Ctrl Pts',(203.505825941656,11.6006588905431,28.1642954884351));
#78087=CARTESIAN_POINT('Ctrl Pts',(203.502820592309,11.5496988224808,28.1425330264411));
#78088=CARTESIAN_POINT('Ctrl Pts',(203.499815242963,11.4977375035818,28.123740712101));
#78089=CARTESIAN_POINT('Ctrl Pts',(203.496804320925,11.4456798350258,28.1049135519742));
#78090=CARTESIAN_POINT('Ctrl Pts',(203.493793398887,11.3926177136023,28.0890676917142));
#78091=CARTESIAN_POINT('Ctrl Pts',(203.490782476849,11.3389239987965,28.0762855718088));
#78092=CARTESIAN_POINT('Ctrl Pts',(203.488610258828,11.3001868765889,28.0670639609994));
#78093=CARTESIAN_POINT('Ctrl Pts',(203.486438040806,11.2611213103833,28.0594359122335));
#78094=CARTESIAN_POINT('Ctrl Pts',(203.484265822785,11.2218691021544,28.0534156258589));
#78095=CARTESIAN_POINT('Ctrl Pts',(203.4812540334,11.1674457510307,28.0450684735836));
#78096=CARTESIAN_POINT('Ctrl Pts',(203.478242244014,11.1124379139738,28.0397795600519));
#78097=CARTESIAN_POINT('Ctrl Pts',(203.475230454629,11.0572192604575,28.037618994163));
#78098=CARTESIAN_POINT('Ctrl Pts',(203.472223963842,11.0020977523338,28.0354622293271));
#78099=CARTESIAN_POINT('Ctrl Pts',(203.469217473055,10.9467666866493,28.0364229100576));
#78100=CARTESIAN_POINT('Ctrl Pts',(203.466210982268,10.891606455227,28.0405195823679));
#78101=CARTESIAN_POINT('Ctrl Pts',(203.463207432546,10.8365001836672,28.0446122471556));
#78102=CARTESIAN_POINT('Ctrl Pts',(203.460203882824,10.7815649387342,28.0518347871742));
#78103=CARTESIAN_POINT('Ctrl Pts',(203.457200333102,10.727180846372,28.0621537080015));
#78104=CARTESIAN_POINT('Ctrl Pts',(203.454198539189,10.6728285457684,28.072466596612));
#78105=CARTESIAN_POINT('Ctrl Pts',(203.451196745277,10.6190272762346,28.0858721799307));
#78106=CARTESIAN_POINT('Ctrl Pts',(203.448194951365,10.566149470245,28.1022854483725));
#78107=CARTESIAN_POINT('Ctrl Pts',(203.445193730625,10.5132817609122,28.1186955828125));
#78108=CARTESIAN_POINT('Ctrl Pts',(203.442192509885,10.4613376682902,28.1381121053616));
#78109=CARTESIAN_POINT('Ctrl Pts',(203.439191289145,10.4106746593596,28.1604000997017));
#78110=CARTESIAN_POINT('Ctrl Pts',(203.436187324496,10.3599653310518,28.182708471158));
#78111=CARTESIAN_POINT('Ctrl Pts',(203.433183359847,10.3105399099647,28.2078933460434));
#78112=CARTESIAN_POINT('Ctrl Pts',(203.430179395199,10.2627346477106,28.235772152532));
#78113=CARTESIAN_POINT('Ctrl Pts',(203.427174046016,10.2149073519034,28.2636638084253));
#78114=CARTESIAN_POINT('Ctrl Pts',(203.424168696833,10.1687021439269,28.2942515793454));
#78115=CARTESIAN_POINT('Ctrl Pts',(203.42116334765,10.1244266540162,28.3273092625066));
#78116=CARTESIAN_POINT('Ctrl Pts',(203.418152425774,10.0800690659184,28.3604282431456));
#78117=CARTESIAN_POINT('Ctrl Pts',(203.415141503898,10.0376487481492,28.3960259444461));
#78118=CARTESIAN_POINT('Ctrl Pts',(203.412130582022,9.99743964159003,28.4338363269437));
#78119=CARTESIAN_POINT('Ctrl Pts',(203.409958362698,9.9684309187308,28.4611144985057));
#78120=CARTESIAN_POINT('Ctrl Pts',(203.407786143375,9.94057236701064,28.4895435080927));
#78121=CARTESIAN_POINT('Ctrl Pts',(203.405613924051,9.91395384429548,28.5190127433654));
#78122=CARTESIAN_POINT('Ctrl Pts',(203.402635280967,9.87745335019704,28.55942226044));
#78123=CARTESIAN_POINT('Ctrl Pts',(203.399656637882,9.84312724817234,28.6019649688394));
#78124=CARTESIAN_POINT('Ctrl Pts',(203.396677994798,9.81123727986223,28.6463751144615));
#78125=CARTESIAN_POINT('Ctrl Pts',(203.393703653128,9.77939336338157,28.6907211280521));
#78126=CARTESIAN_POINT('Ctrl Pts',(203.390729311457,9.74997892838024,28.7369288058932));
#78127=CARTESIAN_POINT('Ctrl Pts',(203.387754969787,9.72321694902763,28.7846977626557));
#78128=CARTESIAN_POINT('Ctrl Pts',(203.384783688017,9.696482501479,28.8324175763585));
#78129=CARTESIAN_POINT('Ctrl Pts',(203.381812406248,9.67239536693559,28.8816950185289));
#78130=CARTESIAN_POINT('Ctrl Pts',(203.378841124478,9.65113506054209,28.9322010698309));
#78131=CARTESIAN_POINT('Ctrl Pts',(203.375870863786,9.62988206023233,28.9826897647771));
#78132=CARTESIAN_POINT('Ctrl Pts',(203.372900603095,9.61145418500448,29.0344057406854));
#78133=CARTESIAN_POINT('Ctrl Pts',(203.369930342403,9.59598385182221,29.0869976929168));
#78134=CARTESIAN_POINT('Ctrl Pts',(203.366960732882,9.58051691020423,29.1395781154039));
#78135=CARTESIAN_POINT('Ctrl Pts',(203.363991123361,9.56800636994545,29.1930336130972));
#78136=CARTESIAN_POINT('Ctrl Pts',(203.361021513841,9.55853468839566,29.2469980129695));
#78137=CARTESIAN_POINT('Ctrl Pts',(203.358049734099,9.54905608484591,29.3010018505669));
#78138=CARTESIAN_POINT('Ctrl Pts',(203.355077954358,9.54262085849238,29.3555147988211));
#78139=CARTESIAN_POINT('Ctrl Pts',(203.352106174617,9.53925994647032,29.4101626691508));
#78140=CARTESIAN_POINT('Ctrl Pts',(203.350455798359,9.53739346581252,29.4405113341236));
#78141=CARTESIAN_POINT('Ctrl Pts',(203.348805422101,9.53647421572529,29.4709015287949));
#78142=CARTESIAN_POINT('Ctrl Pts',(203.347155045843,9.53650055029265,29.5012691360414));
#78143=CARTESIAN_POINT('',(202.847155045809,9.53650021423239,29.4992081299609));
#78144=CARTESIAN_POINT('Ctrl Pts',(203.34715504581,9.53650055029319,29.501269136656));
#78145=CARTESIAN_POINT('Ctrl Pts',(203.343320363599,9.53656173921627,29.5718288788583));
#78146=CARTESIAN_POINT('Ctrl Pts',(203.339485681388,9.54172964003464,29.6421676990623));
#78147=CARTESIAN_POINT('Ctrl Pts',(203.335650999177,9.5518861311701,29.7116564974257));
#78148=CARTESIAN_POINT('Ctrl Pts',(203.332754674557,9.55955730017702,29.7641411901432));
#78149=CARTESIAN_POINT('Ctrl Pts',(203.329858349937,9.5700733053784,29.816141555552));
#78150=CARTESIAN_POINT('Ctrl Pts',(203.326962025317,9.58336551666075,29.8673948701522));
#78151=CARTESIAN_POINT('Ctrl Pts',(203.323950235916,9.59718763479828,29.9206914476964));
#78152=CARTESIAN_POINT('Ctrl Pts',(203.320938446514,9.61405025587103,29.9733173613119));
#78153=CARTESIAN_POINT('Ctrl Pts',(203.317926657113,9.63387023503536,30.0249016243809));
#78154=CARTESIAN_POINT('Ctrl Pts',(203.31492016631,9.65365534518888,30.0763951359807));
#78155=CARTESIAN_POINT('Ctrl Pts',(203.311913675507,9.67638730023825,30.1268501454996));
#78156=CARTESIAN_POINT('Ctrl Pts',(203.308907184704,9.70193292836923,30.1759098516429));
#78157=CARTESIAN_POINT('Ctrl Pts',(203.305903634967,9.72745356678049,30.2249215656875));
#78158=CARTESIAN_POINT('Ctrl Pts',(203.30290008523,9.75578218303147,30.2725402148732));
#78159=CARTESIAN_POINT('Ctrl Pts',(203.299896535492,9.7867378991367,30.3184297921073));
#78160=CARTESIAN_POINT('Ctrl Pts',(203.296894741565,9.81767551919959,30.3642925432867));
#78161=CARTESIAN_POINT('Ctrl Pts',(203.293892947638,9.85123690055986,30.4084277897234));
#78162=CARTESIAN_POINT('Ctrl Pts',(203.290891153711,9.88719687468086,30.4505269350628));
#78163=CARTESIAN_POINT('Ctrl Pts',(203.287889932956,9.92314998248528,30.492618041852));
#78164=CARTESIAN_POINT('Ctrl Pts',(203.284888712202,9.96150043095983,30.5326734189955));
#78165=CARTESIAN_POINT('Ctrl Pts',(203.281887491447,10.0019831103363,30.5704179267678));
#78166=CARTESIAN_POINT('Ctrl Pts',(203.278883526784,10.042502801569,30.6081969429847));
#78167=CARTESIAN_POINT('Ctrl Pts',(203.275879562121,10.0851582314585,30.6436605088547));
#78168=CARTESIAN_POINT('Ctrl Pts',(203.272875597459,10.1296488852503,30.6765717942625));
#78169=CARTESIAN_POINT('Ctrl Pts',(203.269870248262,10.1741600448792,30.7094982485517));
#78170=CARTESIAN_POINT('Ctrl Pts',(203.266864899066,10.2205076726589,30.7398697879506));
#78171=CARTESIAN_POINT('Ctrl Pts',(203.263859549869,10.26836247084,30.7674931068549));
#78172=CARTESIAN_POINT('Ctrl Pts',(203.26084862798,10.3163060041569,30.7951676465155));
#78173=CARTESIAN_POINT('Ctrl Pts',(203.257837706092,10.3657618181764,30.8200835488812));
#78174=CARTESIAN_POINT('Ctrl Pts',(203.254826784203,10.4163773193395,30.8420941906657));
#78175=CARTESIAN_POINT('Ctrl Pts',(203.252654564996,10.452893697996,30.8579736922296));
#78176=CARTESIAN_POINT('Ctrl Pts',(203.250482345789,10.4900132031085,30.8723420486208));
#78177=CARTESIAN_POINT('Ctrl Pts',(203.248310126582,10.5275987282865,30.8851603836681));
#78178=CARTESIAN_POINT('Ctrl Pts',(203.245298337202,10.5797111878374,30.9029330491689));
#78179=CARTESIAN_POINT('Ctrl Pts',(203.242286547822,10.6329359929293,30.9177975992496));
#78180=CARTESIAN_POINT('Ctrl Pts',(203.239274758443,10.686917587499,30.929619408438));
#78181=CARTESIAN_POINT('Ctrl Pts',(203.236268267662,10.7408042130008,30.941420419682));
#78182=CARTESIAN_POINT('Ctrl Pts',(203.233261776882,10.7954444745455,30.9501892017407));
#78183=CARTESIAN_POINT('Ctrl Pts',(203.230255286101,10.8504671451835,30.955840710837));
#78184=CARTESIAN_POINT('Ctrl Pts',(203.227251736387,10.9054359905166,30.9614866914085));
#78185=CARTESIAN_POINT('Ctrl Pts',(203.224248186672,10.9607859817116,30.9640213865873));
#78186=CARTESIAN_POINT('Ctrl Pts',(203.221244636957,11.0161370167667,30.9634110313544));
#78187=CARTESIAN_POINT('Ctrl Pts',(203.218242843052,11.0714556948001,30.9628010329221));
#78188=CARTESIAN_POINT('Ctrl Pts',(203.215241049148,11.1267748891342,30.959049634255));
#78189=CARTESIAN_POINT('Ctrl Pts',(203.212239255243,11.1817130271537,30.9521751360503));
#78190=CARTESIAN_POINT('Ctrl Pts',(203.209238034512,11.2366406751008,30.9453019504853));
#78191=CARTESIAN_POINT('Ctrl Pts',(203.20623681378,11.2911868882277,30.9353069153594));
#78192=CARTESIAN_POINT('Ctrl Pts',(203.203235593048,11.3449760647653,30.9222600903981));
#78193=CARTESIAN_POINT('Ctrl Pts',(203.200231628408,11.3988144188107,30.9092013371943));
#78194=CARTESIAN_POINT('Ctrl Pts',(203.197227663768,11.4518938400073,30.8930853449459));
#78195=CARTESIAN_POINT('Ctrl Pts',(203.194223699128,11.503851245476,30.8740328134482));
#78196=CARTESIAN_POINT('Ctrl Pts',(203.191218349954,11.5558325982232,30.8549715005982));
#78197=CARTESIAN_POINT('Ctrl Pts',(203.188213000781,11.6066904195552,30.8329711603155));
#78198=CARTESIAN_POINT('Ctrl Pts',(203.185207651607,11.6560821430479,30.808200470713));
#78199=CARTESIAN_POINT('Ctrl Pts',(203.182196729741,11.7055654515367,30.7833838498623));
#78200=CARTESIAN_POINT('Ctrl Pts',(203.179185807875,11.7535767737399,30.7557868821362));
#78201=CARTESIAN_POINT('Ctrl Pts',(203.176174886008,11.7997997151085,30.725623378413));
#78202=CARTESIAN_POINT('Ctrl Pts',(203.174002666622,11.8331470996684,30.7038620207721));
#78203=CARTESIAN_POINT('Ctrl Pts',(203.171830447235,11.8655642329307,30.6807657643867));
#78204=CARTESIAN_POINT('Ctrl Pts',(203.169658227848,11.8969432324656,30.6564277269826));
#78205=CARTESIAN_POINT('Ctrl Pts',(203.166646438471,11.9404503192905,30.6226829574814));
#78206=CARTESIAN_POINT('Ctrl Pts',(203.163634649094,11.9821406007112,30.5864096180324));
#78207=CARTESIAN_POINT('Ctrl Pts',(203.160622859717,12.0217060723746,30.5478305930221));
#78208=CARTESIAN_POINT('Ctrl Pts',(203.157616368939,12.0612019370519,30.5093194395558));
#78209=CARTESIAN_POINT('Ctrl Pts',(203.154609878161,12.0985800360574,30.4685110160496));
#78210=CARTESIAN_POINT('Ctrl Pts',(203.151603387384,12.1335651523796,30.4256685666644));
#78211=CARTESIAN_POINT('Ctrl Pts',(203.148599837672,12.1685160449063,30.3828680274221));
#78212=CARTESIAN_POINT('Ctrl Pts',(203.14559628796,12.2010782603043,30.3380378107425));
#78213=CARTESIAN_POINT('Ctrl Pts',(203.142592738248,12.2310145242394,30.2914767786307));
#78214=CARTESIAN_POINT('Ctrl Pts',(203.139590944346,12.2609332880791,30.2449429650959));
#78215=CARTESIAN_POINT('Ctrl Pts',(203.136589150444,12.2882288586422,30.1966807844995));
#78216=CARTESIAN_POINT('Ctrl Pts',(203.133587356543,12.312706634316,30.1470189658912));
#78217=CARTESIAN_POINT('Ctrl Pts',(203.130586135814,12.3371797361203,30.0973666298786));
#78218=CARTESIAN_POINT('Ctrl Pts',(203.127584915085,12.3588358787303,30.0463156595086));
#78219=CARTESIAN_POINT('Ctrl Pts',(203.124583694356,12.3775269703258,29.9942182675954));
#78220=CARTESIAN_POINT('Ctrl Pts',(203.121579729719,12.3962351505128,29.9420732449142));
#78221=CARTESIAN_POINT('Ctrl Pts',(203.118575765082,12.411972685845,29.8888803869602));
#78222=CARTESIAN_POINT('Ctrl Pts',(203.115571800446,12.4246406615891,29.8350093063586));
#78223=CARTESIAN_POINT('Ctrl Pts',(203.112566451275,12.4373144760299,29.7811133964629));
#78224=CARTESIAN_POINT('Ctrl Pts',(203.109561102105,12.4469158192182,29.7265391610833));
#78225=CARTESIAN_POINT('Ctrl Pts',(203.106555752934,12.4533971296812,29.6716654695462));
#78226=CARTESIAN_POINT('Ctrl Pts',(203.103544831071,12.4598904581654,29.6166900280316));
#78227=CARTESIAN_POINT('Ctrl Pts',(203.100533909208,12.4632521657108,29.5614145487942));
#78228=CARTESIAN_POINT('Ctrl Pts',(203.097522987345,12.4634867784783,29.5062208696472));
#78229=CARTESIAN_POINT('Ctrl Pts',(203.095350767935,12.4636560390672,29.4664015762093));
#78230=CARTESIAN_POINT('Ctrl Pts',(203.093178548524,12.4621987984612,29.4266248987027));
#78231=CARTESIAN_POINT('Ctrl Pts',(203.091006329114,12.4591334810299,29.3870321526377));
#78232=CARTESIAN_POINT('Ctrl Pts',(203.08799453973,12.4548834082921,29.3321366795165));
#78233=CARTESIAN_POINT('Ctrl Pts',(203.084982750347,12.4475223123273,29.277367628034));
#78234=CARTESIAN_POINT('Ctrl Pts',(203.081970960963,12.4370669119073,29.2231048200106));
#78235=CARTESIAN_POINT('Ctrl Pts',(203.078964470179,12.4266299055276,29.16893747579));
#78236=CARTESIAN_POINT('Ctrl Pts',(203.075957979395,12.4131094973649,29.1152751212828));
#78237=CARTESIAN_POINT('Ctrl Pts',(203.07295148861,12.3965741466135,29.0624923966251));
#78238=CARTESIAN_POINT('Ctrl Pts',(203.069947938892,12.3800549713818,29.0097613060705));
#78239=CARTESIAN_POINT('Ctrl Pts',(203.066944389173,12.3605268533572,28.9579086415404));
#78240=CARTESIAN_POINT('Ctrl Pts',(203.063940839454,12.3381088677356,28.9072969477998));
#78241=CARTESIAN_POINT('Ctrl Pts',(203.060939045546,12.315703987185,28.8567148405642));
#78242=CARTESIAN_POINT('Ctrl Pts',(203.057937251637,12.2904128008927,28.8073727474071));
#78243=CARTESIAN_POINT('Ctrl Pts',(203.054935457729,12.2624027991648,28.7596140042783));
#78244=CARTESIAN_POINT('Ctrl Pts',(203.051934236993,12.2343981457608,28.7118643803643));
#78245=CARTESIAN_POINT('Ctrl Pts',(203.048933016258,12.2036759747793,28.6656979606276));
#78246=CARTESIAN_POINT('Ctrl Pts',(203.045931795522,12.1704489713604,28.6214321566086));
#78247=CARTESIAN_POINT('Ctrl Pts',(203.042927830878,12.137191589689,28.5771258819592));
#78248=CARTESIAN_POINT('Ctrl Pts',(203.039923866234,12.1014251180251,28.5347241169849));
#78249=CARTESIAN_POINT('Ctrl Pts',(203.03691990159,12.0634038226036,28.4945127747843));
#78250=CARTESIAN_POINT('Ctrl Pts',(203.033914552413,12.0253650030869,28.4542828990912));
#78251=CARTESIAN_POINT('Ctrl Pts',(203.030909203236,11.9850696723617,28.4162458212242));
#78252=CARTESIAN_POINT('Ctrl Pts',(203.027903854058,11.9428080742143,28.3806496593129));
#78253=CARTESIAN_POINT('Ctrl Pts',(203.024892932188,11.9004681121639,28.3449874929365));
#78254=CARTESIAN_POINT('Ctrl Pts',(203.021882010318,11.8561550228794,28.3117756002876));
#78255=CARTESIAN_POINT('Ctrl Pts',(203.018871088448,11.8101901801663,28.2812202323791));
#78256=CARTESIAN_POINT('Ctrl Pts',(203.016698869092,11.7770290005155,28.2591761659861));
#78257=CARTESIAN_POINT('Ctrl Pts',(203.014526649736,11.74300874927,28.2385138803217));
#78258=CARTESIAN_POINT('Ctrl Pts',(203.01235443038,11.7082575776036,28.2192957196265));
#78259=CARTESIAN_POINT('Ctrl Pts',(203.009342640999,11.6600749622084,28.1926496757384));
#78260=CARTESIAN_POINT('Ctrl Pts',(203.006330851619,11.610286698379,28.1686712789441));
#78261=CARTESIAN_POINT('Ctrl Pts',(203.003319062238,11.5592191828815,28.1475554889396));
#78262=CARTESIAN_POINT('Ctrl Pts',(203.000312571457,11.508241509754,28.1264768476509));
#78263=CARTESIAN_POINT('Ctrl Pts',(202.997306080675,11.4559895349629,28.1082510183782));
#78264=CARTESIAN_POINT('Ctrl Pts',(202.994299589894,11.4028137878574,28.0930269006438));
#78265=CARTESIAN_POINT('Ctrl Pts',(202.991296040178,11.3496900593253,28.0778176757305));
#78266=CARTESIAN_POINT('Ctrl Pts',(202.988292490462,11.2956448533326,28.0656044895793));
#78267=CARTESIAN_POINT('Ctrl Pts',(202.985288940746,11.2410464394942,28.056487317684));
#78268=CARTESIAN_POINT('Ctrl Pts',(202.98228714684,11.1864799427118,28.0473754754908));
#78269=CARTESIAN_POINT('Ctrl Pts',(202.979285352935,11.131361398314,28.0413561467001));
#78270=CARTESIAN_POINT('Ctrl Pts',(202.97628355903,11.0760696649248,28.0384783080371));
#78271=CARTESIAN_POINT('Ctrl Pts',(202.973282338297,11.0207884891253,28.0356010188782));
#78272=CARTESIAN_POINT('Ctrl Pts',(202.970281117564,10.9653347164202,28.0358640557412));
#78273=CARTESIAN_POINT('Ctrl Pts',(202.967279896831,10.9100904147275,28.039264392001));
#78274=CARTESIAN_POINT('Ctrl Pts',(202.96427593219,10.8547956051594,28.0426678370658));
#78275=CARTESIAN_POINT('Ctrl Pts',(202.961271967549,10.7997111766841,28.0492142790211));
#78276=CARTESIAN_POINT('Ctrl Pts',(202.958268002909,10.7452157637248,28.058848639821));
#78277=CARTESIAN_POINT('Ctrl Pts',(202.955262653734,10.6906952337147,28.0684874411182));
#78278=CARTESIAN_POINT('Ctrl Pts',(202.95225730456,10.6367647745112,28.081216876905));
#78279=CARTESIAN_POINT('Ctrl Pts',(202.949251955385,10.5837912463799,28.0969310339794));
#78280=CARTESIAN_POINT('Ctrl Pts',(202.946241033518,10.5307194916642,28.1126743291542));
#78281=CARTESIAN_POINT('Ctrl Pts',(202.943230111651,10.4786087097176,28.131413221719));
#78282=CARTESIAN_POINT('Ctrl Pts',(202.940219189784,10.4278079194782,28.1529927717387));
#78283=CARTESIAN_POINT('Ctrl Pts',(202.938046970405,10.3911578614815,28.1685612649854));
#78284=CARTESIAN_POINT('Ctrl Pts',(202.935874751025,10.3551892352,28.1856072469522));
#78285=CARTESIAN_POINT('Ctrl Pts',(202.933702531646,10.320024596085,28.2040579873811));
#78286=CARTESIAN_POINT('Ctrl Pts',(202.930690742265,10.2712687072164,28.2296400002365));
#78287=CARTESIAN_POINT('Ctrl Pts',(202.927678952884,10.2238574588484,28.2580302847729));
#78288=CARTESIAN_POINT('Ctrl Pts',(202.924667163504,10.1781332030965,28.2890634954104));
#78289=CARTESIAN_POINT('Ctrl Pts',(202.921660672722,10.1324893893924,28.3200421097517));
#78290=CARTESIAN_POINT('Ctrl Pts',(202.918654181941,10.0885271111596,28.3536541286549));
#78291=CARTESIAN_POINT('Ctrl Pts',(202.915647691159,10.0465635284795,28.3896887171723));
#78292=CARTESIAN_POINT('Ctrl Pts',(202.912644141443,10.0046409961999,28.4256880552607));
#78293=CARTESIAN_POINT('Ctrl Pts',(202.909640591727,9.96471368425869,28.464104926136));
#78294=CARTESIAN_POINT('Ctrl Pts',(202.906637042011,9.92706765290005,28.5046867686268));
#78295=CARTESIAN_POINT('Ctrl Pts',(202.903635248106,9.88944362860013,28.545244887847));
#78296=CARTESIAN_POINT('Ctrl Pts',(202.900633454201,9.85409859940335,28.5879650840855));
#78297=CARTESIAN_POINT('Ctrl Pts',(202.897631660295,9.82128185947103,28.6325579009594));
#78298=CARTESIAN_POINT('Ctrl Pts',(202.894630439562,9.78847138567757,28.6771422031307));
#78299=CARTESIAN_POINT('Ctrl Pts',(202.891629218829,9.75818855464752,28.7235979911491));
#78300=CARTESIAN_POINT('Ctrl Pts',(202.888627998097,9.73064099627023,28.7716045238676));
#78301=CARTESIAN_POINT('Ctrl Pts',(202.885624033456,9.70306825215266,28.8196549472296));
#78302=CARTESIAN_POINT('Ctrl Pts',(202.882620068815,9.67823603942744,28.8692584891787));
#78303=CARTESIAN_POINT('Ctrl Pts',(202.879616104174,9.65630662968284,28.9200686449538));
#78304=CARTESIAN_POINT('Ctrl Pts',(202.876610755,9.6343671126271,28.9709022192368));
#78305=CARTESIAN_POINT('Ctrl Pts',(202.873605405825,9.61533324693363,29.0229430197891));
#78306=CARTESIAN_POINT('Ctrl Pts',(202.870600056651,9.59931837382386,29.075826412783));
#78307=CARTESIAN_POINT('Ctrl Pts',(202.867589134784,9.5832738050087,29.1288078652274));
#78308=CARTESIAN_POINT('Ctrl Pts',(202.864578212917,9.57025953488192,29.1826345172014));
#78309=CARTESIAN_POINT('Ctrl Pts',(202.86156729105,9.56033814730236,29.2369296674134));
#78310=CARTESIAN_POINT('Ctrl Pts',(202.859395071671,9.5531803958474,29.2761007195784));
#78311=CARTESIAN_POINT('Ctrl Pts',(202.857222852291,9.54763136280445,29.3155153844959));
#78312=CARTESIAN_POINT('Ctrl Pts',(202.855050632911,9.54369772092486,29.3550313069641));
#78313=CARTESIAN_POINT('Ctrl Pts',(202.852418770555,9.53893171796851,29.4029088232889));
#78314=CARTESIAN_POINT('Ctrl Pts',(202.849786908199,9.53652628509325,29.4510251361842));
#78315=CARTESIAN_POINT('Ctrl Pts',(202.847155045843,9.53650021423273,29.4992081293359));
#78316=CARTESIAN_POINT('',(202.347155045874,9.5365000353343,29.4996784047698));
#78317=CARTESIAN_POINT('Ctrl Pts',(202.847155045809,9.53650021423239,29.4992081299609));
#78318=CARTESIAN_POINT('Ctrl Pts',(202.844182904519,9.53647077263956,29.5536208020761));
#78319=CARTESIAN_POINT('Ctrl Pts',(202.841210763228,9.5394801612605,29.608151560332));
#78320=CARTESIAN_POINT('Ctrl Pts',(202.838238621938,9.54554158352536,29.6624283372632));
#78321=CARTESIAN_POINT('Ctrl Pts',(202.835270150082,9.55159552230065,29.7166381035694));
#78322=CARTESIAN_POINT('Ctrl Pts',(202.832301678225,9.56069397931198,29.7705939747778));
#78323=CARTESIAN_POINT('Ctrl Pts',(202.829333206369,9.57279816347795,29.8239246329443));
#78324=CARTESIAN_POINT('Ctrl Pts',(202.826367158666,9.58489246296194,29.8772117395101));
#78325=CARTESIAN_POINT('Ctrl Pts',(202.823401110963,9.5999875107837,29.9298741172893));
#78326=CARTESIAN_POINT('Ctrl Pts',(202.82043506326,9.6179931298954,29.9815488147464));
#78327=CARTESIAN_POINT('Ctrl Pts',(202.817470198313,9.63599156899636,30.0332029061427));
#78328=CARTESIAN_POINT('Ctrl Pts',(202.814505333366,9.65689810096678,30.0838695866816));
#78329=CARTESIAN_POINT('Ctrl Pts',(202.81154046842,9.68057291225944,30.1332017136241));
#78330=CARTESIAN_POINT('Ctrl Pts',(202.808573410788,9.70426523240693,30.1825703244497));
#78331=CARTESIAN_POINT('Ctrl Pts',(202.805606353157,9.730729693571,30.2306019171568));
#78332=CARTESIAN_POINT('Ctrl Pts',(202.802639295526,9.75977927637045,30.2769715610496));
#78333=CARTESIAN_POINT('Ctrl Pts',(202.799671292272,9.78883811748051,30.3233559832808));
#78334=CARTESIAN_POINT('Ctrl Pts',(202.796703289018,9.82048341153653,30.3680769557165));
#78335=CARTESIAN_POINT('Ctrl Pts',(202.793735285764,9.85448520143498,30.4108392263559));
#78336=CARTESIAN_POINT('Ctrl Pts',(202.790761646491,9.88855155822017,30.4536826993876));
#78337=CARTESIAN_POINT('Ctrl Pts',(202.787788007219,9.92498299101151,30.494559632155));
#78338=CARTESIAN_POINT('Ctrl Pts',(202.784814367946,9.96351052718381,30.5332094766993));
#78339=CARTESIAN_POINT('Ctrl Pts',(202.78200915669,9.99985584960956,30.5696701799061));
#78340=CARTESIAN_POINT('Ctrl Pts',(202.779203945433,10.0380659299903,30.6041490219623));
#78341=CARTESIAN_POINT('Ctrl Pts',(202.776398734177,10.0778892147288,30.6364611518598));
#78342=CARTESIAN_POINT('Ctrl Pts',(202.773386944796,10.1206451197699,30.6711527742773));
#78343=CARTESIAN_POINT('Ctrl Pts',(202.770375155415,10.1654500942286,30.7035000924404));
#78344=CARTESIAN_POINT('Ctrl Pts',(202.767363366034,10.2120170406476,30.7332538691487));
#78345=CARTESIAN_POINT('Ctrl Pts',(202.764356875252,10.2585020624853,30.7629553004513));
#78346=CARTESIAN_POINT('Ctrl Pts',(202.761350384471,10.3067424634887,30.79007196385));
#78347=CARTESIAN_POINT('Ctrl Pts',(202.758343893689,10.3564193016363,30.8143957298674));
#78348=CARTESIAN_POINT('Ctrl Pts',(202.755340343973,10.4060475439786,30.8386957014357));
#78349=CARTESIAN_POINT('Ctrl Pts',(202.752336794256,10.4571089682818,30.8602079573718));
#78350=CARTESIAN_POINT('Ctrl Pts',(202.74933324454,10.5092585781739,30.8787694175982));
#78351=CARTESIAN_POINT('Ctrl Pts',(202.746331450634,10.5613777025278,30.8973200271949));
#78352=CARTESIAN_POINT('Ctrl Pts',(202.743329656729,10.6145832556133,30.9129230838526));
#78353=CARTESIAN_POINT('Ctrl Pts',(202.740327862823,10.6685108626173,30.9254638549599));
#78354=CARTESIAN_POINT('Ctrl Pts',(202.73732664209,10.7224281725025,30.9380022314903));
#78355=CARTESIAN_POINT('Ctrl Pts',(202.734325421357,10.7770667490338,30.9474793645404));
#78356=CARTESIAN_POINT('Ctrl Pts',(202.731324200624,10.8320499276654,30.9538311536086));
#78357=CARTESIAN_POINT('Ctrl Pts',(202.728320235982,10.8870833754366,30.9601887498886));
#78358=CARTESIAN_POINT('Ctrl Pts',(202.725316271341,10.94246152968,30.9634152334097));
#78359=CARTESIAN_POINT('Ctrl Pts',(202.7223123067,10.9978019672819,30.9634983493848));
#78360=CARTESIAN_POINT('Ctrl Pts',(202.719306957526,11.0531679114081,30.9635815036684));
#78361=CARTESIAN_POINT('Ctrl Pts',(202.716301608351,11.1084955767833,30.9605184316654));
#78362=CARTESIAN_POINT('Ctrl Pts',(202.713296259176,11.1634052063721,30.9543489913121));
#78363=CARTESIAN_POINT('Ctrl Pts',(202.710285337309,11.2184166525767,30.9481681112251));
#78364=CARTESIAN_POINT('Ctrl Pts',(202.707274415441,11.2730079936089,30.9388694460215));
#78365=CARTESIAN_POINT('Ctrl Pts',(202.704263493574,11.3268084289459,30.9265442512484));
#78366=CARTESIAN_POINT('Ctrl Pts',(202.702091274197,11.3656225706884,30.9176522812498));
#78367=CARTESIAN_POINT('Ctrl Pts',(202.69991905482,11.404025270005,30.9071861329833));
#78368=CARTESIAN_POINT('Ctrl Pts',(202.697746835443,11.4418831057935,30.895195889764));
#78369=CARTESIAN_POINT('Ctrl Pts',(202.694735046062,11.4943731208542,30.8785713777163));
#78370=CARTESIAN_POINT('Ctrl Pts',(202.691723256681,11.5460324336264,30.8589461354871));
#78371=CARTESIAN_POINT('Ctrl Pts',(202.6887114673,11.5964949799208,30.8364228331368));
#78372=CARTESIAN_POINT('Ctrl Pts',(202.685704976518,11.646868748159,30.8139391557192));
#78373=CARTESIAN_POINT('Ctrl Pts',(202.682698485736,11.6960494505891,30.7885677499365));
#78374=CARTESIAN_POINT('Ctrl Pts',(202.679691994954,11.74368783712,30.760460491614));
#78375=CARTESIAN_POINT('Ctrl Pts',(202.676688445238,11.7912796219378,30.7323807288992));
#78376=CARTESIAN_POINT('Ctrl Pts',(202.673684895522,11.8373316277677,30.701570682381));
#78377=CARTESIAN_POINT('Ctrl Pts',(202.670681345806,11.8815178953516,30.668228766199));
#78378=CARTESIAN_POINT('Ctrl Pts',(202.6676795519,11.9256783325958,30.6349063409826));
#78379=CARTESIAN_POINT('Ctrl Pts',(202.664677757994,11.9679747733647,30.5990552970014));
#78380=CARTESIAN_POINT('Ctrl Pts',(202.661675964089,12.0081109756505,30.5609168255679));
#78381=CARTESIAN_POINT('Ctrl Pts',(202.658674743355,12.0482395141946,30.5227856364226));
#78382=CARTESIAN_POINT('Ctrl Pts',(202.655673522622,12.0862082514783,30.4823682504933));
#78383=CARTESIAN_POINT('Ctrl Pts',(202.652672301889,12.1217564698807,30.4399439729477));
#78384=CARTESIAN_POINT('Ctrl Pts',(202.649668337248,12.1573371887388,30.3974809084133));
#78385=CARTESIAN_POINT('Ctrl Pts',(202.646664372607,12.1904926284475,30.3530076919667));
#78386=CARTESIAN_POINT('Ctrl Pts',(202.643660407966,12.2210022017771,30.3068369558068));
#78387=CARTESIAN_POINT('Ctrl Pts',(202.640655058791,12.2515258370332,30.2606449394573));
#78388=CARTESIAN_POINT('Ctrl Pts',(202.637649709616,12.2794009093005,30.2127543003707));
#78389=CARTESIAN_POINT('Ctrl Pts',(202.634644360441,12.3044518187262,30.1635041089714));
#78390=CARTESIAN_POINT('Ctrl Pts',(202.631633438574,12.3295491789992,30.1141625950144));
#78391=CARTESIAN_POINT('Ctrl Pts',(202.628622516707,12.3518117036761,30.063456977127));
#78392=CARTESIAN_POINT('Ctrl Pts',(202.625611594839,12.3711116431405,30.0117471172801));
#78393=CARTESIAN_POINT('Ctrl Pts',(202.623439375463,12.3850355190573,29.9744412141446));
#78394=CARTESIAN_POINT('Ctrl Pts',(202.621267156086,12.3974184365851,29.9366130377746));
#78395=CARTESIAN_POINT('Ctrl Pts',(202.619094936709,12.408228833152,29.8984015605883));
#78396=CARTESIAN_POINT('Ctrl Pts',(202.616083147328,12.4232174838996,29.8454212205477));
#78397=CARTESIAN_POINT('Ctrl Pts',(202.613071357947,12.4352432050487,29.7914840648974));
#78398=CARTESIAN_POINT('Ctrl Pts',(202.610059568566,12.4441903848178,29.7369522787393));
#78399=CARTESIAN_POINT('Ctrl Pts',(202.607053077784,12.453121823938,29.6825164295945));
#78400=CARTESIAN_POINT('Ctrl Pts',(202.604046587002,12.4589853856003,29.6274885424128));
#78401=CARTESIAN_POINT('Ctrl Pts',(202.60104009622,12.4617157998699,29.5722438261069));
#78402=CARTESIAN_POINT('Ctrl Pts',(202.598036546504,12.4644435431427,29.5170531523201));
#78403=CARTESIAN_POINT('Ctrl Pts',(202.595032996788,12.4640441850761,29.4616465938575));
#78404=CARTESIAN_POINT('Ctrl Pts',(202.592029447071,12.4605041324605,29.4064055072888));
#78405=CARTESIAN_POINT('Ctrl Pts',(202.589027653165,12.4569661492833,29.3511967134687));
#78406=CARTESIAN_POINT('Ctrl Pts',(202.58602585926,12.4502911445459,29.2961537251037));
#78407=CARTESIAN_POINT('Ctrl Pts',(202.583024065354,12.4405175955905,29.2416566107017));
#78408=CARTESIAN_POINT('Ctrl Pts',(202.580022844621,12.4307459128295,29.1871699021622));
#78409=CARTESIAN_POINT('Ctrl Pts',(202.577021623887,12.4178769541139,29.1332293793805));
#78410=CARTESIAN_POINT('Ctrl Pts',(202.574020403154,12.4020005670935,29.0802064080176));
#78411=CARTESIAN_POINT('Ctrl Pts',(202.571016438513,12.3861096648643,29.0271349596619));
#78412=CARTESIAN_POINT('Ctrl Pts',(202.568012473872,12.3672059931612,28.9749832448325));
#78413=CARTESIAN_POINT('Ctrl Pts',(202.56500850923,12.3454293058665,28.9241074467268));
#78414=CARTESIAN_POINT('Ctrl Pts',(202.562003160056,12.3236425816508,28.8732081998585));
#78415=CARTESIAN_POINT('Ctrl Pts',(202.558997810881,12.2989804373979,28.823586515012));
#78416=CARTESIAN_POINT('Ctrl Pts',(202.555992461706,12.2716294517743,28.7755755474998));
#78417=CARTESIAN_POINT('Ctrl Pts',(202.552981539839,12.2442277503688,28.7274755552706));
#78418=CARTESIAN_POINT('Ctrl Pts',(202.549970617971,12.2141275358225,28.6809926898822));
#78419=CARTESIAN_POINT('Ctrl Pts',(202.546959696104,12.1815590705988,28.6364315819313));
#78420=CARTESIAN_POINT('Ctrl Pts',(202.544787476728,12.158062661748,28.6042831216318));
#78421=CARTESIAN_POINT('Ctrl Pts',(202.542615257351,12.1332824784799,28.5731342839266));
#78422=CARTESIAN_POINT('Ctrl Pts',(202.540443037975,12.1073172197368,28.5430878698259));
#78423=CARTESIAN_POINT('Ctrl Pts',(202.537431248594,12.0713163022358,28.5014284168645));
#78424=CARTESIAN_POINT('Ctrl Pts',(202.534419459213,12.0328865517901,28.4617170959423));
#78425=CARTESIAN_POINT('Ctrl Pts',(202.531407669832,11.9922668474289,28.4242496788318));
#78426=CARTESIAN_POINT('Ctrl Pts',(202.52840117905,11.9517186047489,28.3868481776273));
#78427=CARTESIAN_POINT('Ctrl Pts',(202.525394688268,11.9089884389232,28.3516831004702));
#78428=CARTESIAN_POINT('Ctrl Pts',(202.522388197486,11.8643537962268,28.3190153409344));
#78429=CARTESIAN_POINT('Ctrl Pts',(202.51938464777,11.819762816865,28.286379538265));
#78430=CARTESIAN_POINT('Ctrl Pts',(202.516381098054,11.773271475018,28.2562365234736));
#78431=CARTESIAN_POINT('Ctrl Pts',(202.513377548338,11.7251907759786,28.2288074148912));
#78432=CARTESIAN_POINT('Ctrl Pts',(202.510375754432,11.6771381838797,28.2013943407747));
#78433=CARTESIAN_POINT('Ctrl Pts',(202.507373960526,11.6274985334929,28.1766922889209));
#78434=CARTESIAN_POINT('Ctrl Pts',(202.50437216662,11.5766103959632,28.154878183484));
#78435=CARTESIAN_POINT('Ctrl Pts',(202.501370945887,11.5257319751857,28.1330682433059));
#78436=CARTESIAN_POINT('Ctrl Pts',(202.498369725154,11.4736060252663,28.1141453618837));
#78437=CARTESIAN_POINT('Ctrl Pts',(202.495368504421,11.4205921057218,28.0982387754669));
#78438=CARTESIAN_POINT('Ctrl Pts',(202.49236453978,11.3675297174603,28.0823176462311));
#78439=CARTESIAN_POINT('Ctrl Pts',(202.489360575138,11.3135782439922,28.069418472845));
#78440=CARTESIAN_POINT('Ctrl Pts',(202.486356610497,11.2591120165662,28.0596204622146));
#78441=CARTESIAN_POINT('Ctrl Pts',(202.483351261322,11.2046206855411,28.0498179356604));
#78442=CARTESIAN_POINT('Ctrl Pts',(202.480345912147,11.1496146520238,28.0431194848871));
#78443=CARTESIAN_POINT('Ctrl Pts',(202.477340562973,11.0944747720894,28.0395525454715));
#78444=CARTESIAN_POINT('Ctrl Pts',(202.474329641105,11.0392326485958,28.0359789920304));
#78445=CARTESIAN_POINT('Ctrl Pts',(202.471318719238,10.9838567114718,28.0355485526982));
#78446=CARTESIAN_POINT('Ctrl Pts',(202.468307797371,10.9287280233432,28.038236491308));
#78447=CARTESIAN_POINT('Ctrl Pts',(202.466135577994,10.8889556181346,28.0401756955081));
#78448=CARTESIAN_POINT('Ctrl Pts',(202.463963358617,10.8493118839798,28.0437368632858));
#78449=CARTESIAN_POINT('Ctrl Pts',(202.461791139241,10.8099369627027,28.0488941141828));
#78450=CARTESIAN_POINT('Ctrl Pts',(202.45877934986,10.7553435035612,28.0560446596822));
#78451=CARTESIAN_POINT('Ctrl Pts',(202.455767560479,10.7010410014664,28.066295171619));
#78452=CARTESIAN_POINT('Ctrl Pts',(202.452755771098,10.6474078603407,28.0796088450534));
#78453=CARTESIAN_POINT('Ctrl Pts',(202.449749280316,10.5938690752545,28.0928990959273));
#78454=CARTESIAN_POINT('Ctrl Pts',(202.446742789534,10.5409978219095,28.1092416872979));
#78455=CARTESIAN_POINT('Ctrl Pts',(202.443736298752,10.4891645904217,28.1285484207159));
#78456=CARTESIAN_POINT('Ctrl Pts',(202.440732749036,10.4373820642065,28.1478362675401));
#78457=CARTESIAN_POINT('Ctrl Pts',(202.437729199319,10.3866360400535,28.1700823287675));
#78458=CARTESIAN_POINT('Ctrl Pts',(202.434725649603,10.3372822498144,28.1951485013271));
#78459=CARTESIAN_POINT('Ctrl Pts',(202.431723855697,10.2879573107374,28.2202000207424));
#78460=CARTESIAN_POINT('Ctrl Pts',(202.428722061791,10.2400234616233,28.2480681452834));
#78461=CARTESIAN_POINT('Ctrl Pts',(202.425720267885,10.1938146891182,28.2785674416824));
#78462=CARTESIAN_POINT('Ctrl Pts',(202.422719047152,10.1476147398716,28.309060914443));
#78463=CARTESIAN_POINT('Ctrl Pts',(202.419717826419,10.1031396528728,28.3421842707461));
#78464=CARTESIAN_POINT('Ctrl Pts',(202.416716605686,10.0606951338846,28.377708318443));
#78465=CARTESIAN_POINT('Ctrl Pts',(202.413712641045,10.0182118094015,28.4132648444973));
#78466=CARTESIAN_POINT('Ctrl Pts',(202.410708676403,9.97776316684075,28.451226107364));
#78467=CARTESIAN_POINT('Ctrl Pts',(202.407704711762,9.93962125619621,28.4913230598011));
#78468=CARTESIAN_POINT('Ctrl Pts',(202.404699362587,9.90146176586465,28.531438493008));
#78469=CARTESIAN_POINT('Ctrl Pts',(202.401694013412,9.86561146851262,28.5736911751225));
#78470=CARTESIAN_POINT('Ctrl Pts',(202.398688664238,9.83230276734794,28.6177781328618));
#78471=CARTESIAN_POINT('Ctrl Pts',(202.39567774237,9.79893230326019,28.6619468391919));
#78472=CARTESIAN_POINT('Ctrl Pts',(202.392666820503,9.76811314319873,28.7079561758911));
#78473=CARTESIAN_POINT('Ctrl Pts',(202.389655898636,9.74003423380136,28.7554742999685));
#78474=CARTESIAN_POINT('Ctrl Pts',(202.387483679259,9.71977679978217,28.7897560895348));
#78475=CARTESIAN_POINT('Ctrl Pts',(202.385311459882,9.70094469191825,28.8248225876061));
#78476=CARTESIAN_POINT('Ctrl Pts',(202.383139240506,9.68359338206267,28.8605425219369));
#78477=CARTESIAN_POINT('Ctrl Pts',(202.379914219016,9.65783247238003,28.9135747143088));
#78478=CARTESIAN_POINT('Ctrl Pts',(202.376689197525,9.6352427898551,28.9682422387701));
#78479=CARTESIAN_POINT('Ctrl Pts',(202.373464176035,9.61601745292213,29.0241591028675));
#78480=CARTESIAN_POINT('Ctrl Pts',(202.370246978428,9.59683875654359,29.0799403129811));
#78481=CARTESIAN_POINT('Ctrl Pts',(202.367029780821,9.58100830934031,29.1369644532309));
#78482=CARTESIAN_POINT('Ctrl Pts',(202.363812583214,9.56867188081793,29.194824533688));
#78483=CARTESIAN_POINT('Ctrl Pts',(202.360606820318,9.55637929899555,29.2524789651938));
#78484=CARTESIAN_POINT('Ctrl Pts',(202.357401057422,9.54755609808255,29.3109630249618));
#78485=CARTESIAN_POINT('Ctrl Pts',(202.354195294526,9.54229812331524,29.3698558925278));
#78486=CARTESIAN_POINT('Ctrl Pts',(202.351848544976,9.53844907074235,29.4129678802155));
#78487=CARTESIAN_POINT('Ctrl Pts',(202.349501795425,9.53650956779653,29.4562985383023));
#78488=CARTESIAN_POINT('Ctrl Pts',(202.347155045874,9.5365000353343,29.4996784047699));
#78489=CARTESIAN_POINT('',(201.847155045881,9.53650048906759,29.5011964533363));
#78490=CARTESIAN_POINT('Ctrl Pts',(202.347155045843,9.53650003533417,29.4996784053507));
#78491=CARTESIAN_POINT('Ctrl Pts',(202.344062800078,9.53648747469995,29.5568388331947));
#78492=CARTESIAN_POINT('Ctrl Pts',(202.340970554314,9.53982804448367,29.613961635679));
#78493=CARTESIAN_POINT('Ctrl Pts',(202.337878308549,9.54648255526969,29.6706437454601));
#78494=CARTESIAN_POINT('Ctrl Pts',(202.334779716217,9.55315072386491,29.7274421903807));
#78495=CARTESIAN_POINT('Ctrl Pts',(202.331681123884,9.56314635575235,29.783797658737));
#78496=CARTESIAN_POINT('Ctrl Pts',(202.328582531552,9.57637867983794,29.8393148785126));
#78497=CARTESIAN_POINT('Ctrl Pts',(202.325480570849,9.58962538832023,29.8948924491162));
#78498=CARTESIAN_POINT('Ctrl Pts',(202.322378610145,9.60611565823238,29.9496294963648));
#78499=CARTESIAN_POINT('Ctrl Pts',(202.319276649441,9.62570903982726,30.0031467050349));
#78500=CARTESIAN_POINT('Ctrl Pts',(202.316167117876,9.64535024239885,30.0567945315454));
#78501=CARTESIAN_POINT('Ctrl Pts',(202.31305758631,9.66810949601393,30.1092161302731));
#78502=CARTESIAN_POINT('Ctrl Pts',(202.309948054744,9.69379870287798,30.160053347387));
#78503=CARTESIAN_POINT('Ctrl Pts',(202.308127817087,9.70883648613593,30.1898121116977));
#78504=CARTESIAN_POINT('Ctrl Pts',(202.30630757943,9.72487739373735,30.2190284520927));
#78505=CARTESIAN_POINT('Ctrl Pts',(202.304487341773,9.7418768384148,30.2476351786017));
#78506=CARTESIAN_POINT('Ctrl Pts',(202.301475552392,9.77000434514925,30.2949682478755));
#78507=CARTESIAN_POINT('Ctrl Pts',(202.298463763011,9.80086499296815,30.3408098790084));
#78508=CARTESIAN_POINT('Ctrl Pts',(202.29545197363,9.83427554241027,30.3848269542555));
#78509=CARTESIAN_POINT('Ctrl Pts',(202.292445482848,9.86762731313721,30.4287665908741));
#78510=CARTESIAN_POINT('Ctrl Pts',(202.289438992066,9.90351976623064,30.4708876252146));
#78511=CARTESIAN_POINT('Ctrl Pts',(202.286432501284,9.94172557045227,30.5108845046618));
#78512=CARTESIAN_POINT('Ctrl Pts',(202.283428951568,9.97989400027782,30.5508422576139));
#78513=CARTESIAN_POINT('Ctrl Pts',(202.280425401851,10.0203709354635,30.588679592687));
#78514=CARTESIAN_POINT('Ctrl Pts',(202.277421852135,10.0628890236482,30.6241242226734));
#78515=CARTESIAN_POINT('Ctrl Pts',(202.274420058229,10.1053822566748,30.6595481324929));
#78516=CARTESIAN_POINT('Ctrl Pts',(202.271418264324,10.1499138731675,30.6925817727536));
#78517=CARTESIAN_POINT('Ctrl Pts',(202.268416470418,10.1961816238766,30.722991524176));
#78518=CARTESIAN_POINT('Ctrl Pts',(202.265415249684,10.2424405400657,30.7533954690581));
#78519=CARTESIAN_POINT('Ctrl Pts',(202.262414028951,10.2904344915036,30.7811762307775));
#78520=CARTESIAN_POINT('Ctrl Pts',(202.259412808218,10.3398321939651,30.8061434522575));
#78521=CARTESIAN_POINT('Ctrl Pts',(202.256408843577,10.3892750589667,30.8311335003688));
#78522=CARTESIAN_POINT('Ctrl Pts',(202.253404878935,10.4401237671261,30.8533046311918));
#78523=CARTESIAN_POINT('Ctrl Pts',(202.250400914294,10.4920237082286,30.8725131463845));
#78524=CARTESIAN_POINT('Ctrl Pts',(202.247395565119,10.5439475701233,30.8917305148222));
#78525=CARTESIAN_POINT('Ctrl Pts',(202.244390215944,10.5969231257384,30.9079823908173));
#78526=CARTESIAN_POINT('Ctrl Pts',(202.24138486677,10.6505802518315,30.9211748976076));
#78527=CARTESIAN_POINT('Ctrl Pts',(202.238373944902,10.7043368720758,30.9343918667081));
#78528=CARTESIAN_POINT('Ctrl Pts',(202.235363023035,10.7587770676294,30.9445380383248));
#78529=CARTESIAN_POINT('Ctrl Pts',(202.232352101167,10.8135213520535,30.9515708607781));
#78530=CARTESIAN_POINT('Ctrl Pts',(202.230179881791,10.8530164305113,30.9566446667013));
#78531=CARTESIAN_POINT('Ctrl Pts',(202.228007662414,10.8926696066492,30.9600991125008));
#78532=CARTESIAN_POINT('Ctrl Pts',(202.225835443038,10.9323383716403,30.961935071762));
#78533=CARTESIAN_POINT('Ctrl Pts',(202.222823653657,10.9873392460684,30.9644806353762));
#78534=CARTESIAN_POINT('Ctrl Pts',(202.219811864276,11.0425979477148,30.9639233014669));
#78535=CARTESIAN_POINT('Ctrl Pts',(202.216800074895,11.097735488617,30.9602328664514));
#78536=CARTESIAN_POINT('Ctrl Pts',(202.213793584113,11.15277602681,30.9565489239668));
#78537=CARTESIAN_POINT('Ctrl Pts',(202.210787093331,11.2076953052168,30.9497428544513));
#78538=CARTESIAN_POINT('Ctrl Pts',(202.207780602549,11.2621131035355,30.9398364389593));
#78539=CARTESIAN_POINT('Ctrl Pts',(202.204777052833,11.3164776682581,30.9299397143063));
#78540=CARTESIAN_POINT('Ctrl Pts',(202.201773503116,11.3703412083566,30.9169487460775));
#78541=CARTESIAN_POINT('Ctrl Pts',(202.1987699534,11.4233292707362,30.9009370358935));
#78542=CARTESIAN_POINT('Ctrl Pts',(202.195768159494,11.4762863574364,30.8849346858101));
#78543=CARTESIAN_POINT('Ctrl Pts',(202.192766365589,11.5283684770106,30.86591524636));
#78544=CARTESIAN_POINT('Ctrl Pts',(202.189764571683,11.579214273977,30.8440026319994));
#78545=CARTESIAN_POINT('Ctrl Pts',(202.18676335095,11.6300503622757,30.8220942017071));
#78546=CARTESIAN_POINT('Ctrl Pts',(202.183762130217,11.6796501128072,30.7972939024439));
#78547=CARTESIAN_POINT('Ctrl Pts',(202.180760909483,11.7276723288805,30.7697736931365));
#78548=CARTESIAN_POINT('Ctrl Pts',(202.177756944842,11.7757384499363,30.7422283230931));
#78549=CARTESIAN_POINT('Ctrl Pts',(202.174752980201,11.8222236967836,30.7119583381411));
#78550=CARTESIAN_POINT('Ctrl Pts',(202.17174901556,11.8668130083111,30.6791808422047));
#78551=CARTESIAN_POINT('Ctrl Pts',(202.168743666385,11.9114228711462,30.6463882390514));
#78552=CARTESIAN_POINT('Ctrl Pts',(202.16573831721,11.9541346496012,30.6110861577062));
#78553=CARTESIAN_POINT('Ctrl Pts',(202.162732968036,11.9946663570722,30.5735320619845));
#78554=CARTESIAN_POINT('Ctrl Pts',(202.159722046168,12.0352732207829,30.5359083312833));
#78555=CARTESIAN_POINT('Ctrl Pts',(202.156711124301,12.073691572175,30.4960246257544));
#78556=CARTESIAN_POINT('Ctrl Pts',(202.153700202434,12.1096771375035,30.4541744602021));
#78557=CARTESIAN_POINT('Ctrl Pts',(202.151527983057,12.1356388016468,30.4239818001038));
#78558=CARTESIAN_POINT('Ctrl Pts',(202.149355763681,12.1603350517917,30.3927663743924));
#78559=CARTESIAN_POINT('Ctrl Pts',(202.147183544304,12.1836882301215,30.3606476769688));
#78560=CARTESIAN_POINT('Ctrl Pts',(202.144171754923,12.2160674894485,30.3161149963016));
#78561=CARTESIAN_POINT('Ctrl Pts',(202.141159965542,12.2459972448394,30.2696602390536));
#78562=CARTESIAN_POINT('Ctrl Pts',(202.138148176161,12.2732438090024,30.2215832958411));
#78563=CARTESIAN_POINT('Ctrl Pts',(202.135141685379,12.3004424386639,30.1735909337265));
#78564=CARTESIAN_POINT('Ctrl Pts',(202.132135194597,12.3249669873978,30.1239825046809));
#78565=CARTESIAN_POINT('Ctrl Pts',(202.129128703815,12.3466265039856,30.0730875227777));
#78566=CARTESIAN_POINT('Ctrl Pts',(202.126125154099,12.3682648323962,30.0222423283152));
#78567=CARTESIAN_POINT('Ctrl Pts',(202.123121604383,12.3870434754876,29.9701135572659));
#78568=CARTESIAN_POINT('Ctrl Pts',(202.120118054667,12.4028178477007,29.9170543563763));
#78569=CARTESIAN_POINT('Ctrl Pts',(202.117116260761,12.4185829985557,29.8640261727521));
#78570=CARTESIAN_POINT('Ctrl Pts',(202.114114466855,12.4313472097717,29.8100691419928));
#78571=CARTESIAN_POINT('Ctrl Pts',(202.111112672949,12.4410152014346,29.7555532023561));
#78572=CARTESIAN_POINT('Ctrl Pts',(202.108111452216,12.4506813470586,29.7010476721765));
#78573=CARTESIAN_POINT('Ctrl Pts',(202.105110231483,12.4572523554203,29.6459839641154));
#78574=CARTESIAN_POINT('Ctrl Pts',(202.10210901075,12.4606841583787,29.5907416082155));
#78575=CARTESIAN_POINT('Ctrl Pts',(202.099105046108,12.4641190989109,29.5354487462195));
#78576=CARTESIAN_POINT('Ctrl Pts',(202.096101081467,12.464409067828,29.4799774375864));
#78577=CARTESIAN_POINT('Ctrl Pts',(202.093097116826,12.4615620748737,29.4247102178855));
#78578=CARTESIAN_POINT('Ctrl Pts',(202.090091767651,12.4587137697344,29.3694175254064));
#78579=CARTESIAN_POINT('Ctrl Pts',(202.087086418476,12.4527256777536,29.3143296345363));
#78580=CARTESIAN_POINT('Ctrl Pts',(202.084081069302,12.4436577071515,29.2598236594038));
#78581=CARTESIAN_POINT('Ctrl Pts',(202.081070147434,12.434572922193,29.205216616135));
#78582=CARTESIAN_POINT('Ctrl Pts',(202.078059225567,12.4223969674231,29.1511941595467));
#78583=CARTESIAN_POINT('Ctrl Pts',(202.0750483037,12.4072406023832,29.0981217385773));
#78584=CARTESIAN_POINT('Ctrl Pts',(202.072876084323,12.3963060941934,29.059832820343));
#78585=CARTESIAN_POINT('Ctrl Pts',(202.070703864946,12.3838213993874,29.0220381121263));
#78586=CARTESIAN_POINT('Ctrl Pts',(202.06853164557,12.3698435949984,28.9848681962431));
#78587=CARTESIAN_POINT('Ctrl Pts',(202.065519856189,12.3504633227827,28.933331984403));
#78588=CARTESIAN_POINT('Ctrl Pts',(202.062508066808,12.3281305105252,28.8827841830126));
#78589=CARTESIAN_POINT('Ctrl Pts',(202.059496277427,12.3029670655067,28.8335849069799));
#78590=CARTESIAN_POINT('Ctrl Pts',(202.056489786645,12.2778478901871,28.7844721865496));
#78591=CARTESIAN_POINT('Ctrl Pts',(202.053483295863,12.24990820344,28.736703748984));
#78592=CARTESIAN_POINT('Ctrl Pts',(202.050476805081,12.2193181590764,28.690620313483));
#78593=CARTESIAN_POINT('Ctrl Pts',(202.047473255365,12.1887580390779,28.6445819585817));
#78594=CARTESIAN_POINT('Ctrl Pts',(202.044469705649,12.1555529880724,28.6002257775559));
#78595=CARTESIAN_POINT('Ctrl Pts',(202.041466155932,12.1199183997819,28.5578667674739));
#78596=CARTESIAN_POINT('Ctrl Pts',(202.038464362027,12.0843046427038,28.5155325195564));
#78597=CARTESIAN_POINT('Ctrl Pts',(202.035462568121,12.0462645024623,28.4751935311365));
#78598=CARTESIAN_POINT('Ctrl Pts',(202.032460774215,12.0060545165792,28.437132858881));
#78599=CARTESIAN_POINT('Ctrl Pts',(202.029459553482,11.9658522085262,28.3990794540584));
#78600=CARTESIAN_POINT('Ctrl Pts',(202.026458332749,11.923481260625,28.3633038636331));
#78601=CARTESIAN_POINT('Ctrl Pts',(202.023457112016,11.8792343899608,28.3300516517768));
#78602=CARTESIAN_POINT('Ctrl Pts',(202.020453147374,11.8349470659765,28.2967690386209));
#78603=CARTESIAN_POINT('Ctrl Pts',(202.017449182733,11.7887808155381,28.2660147302413));
#78604=CARTESIAN_POINT('Ctrl Pts',(202.014445218092,11.7410595113205,28.237992452209));
#78605=CARTESIAN_POINT('Ctrl Pts',(202.011439868917,11.6933162122531,28.2099572586497));
#78606=CARTESIAN_POINT('Ctrl Pts',(202.008434519742,11.6440169007015,28.1846568466644));
#78607=CARTESIAN_POINT('Ctrl Pts',(202.005429170567,11.5935094686339,28.1622486177761));
#78608=CARTESIAN_POINT('Ctrl Pts',(202.0024182487,11.54290838276,28.1397988382518));
#78609=CARTESIAN_POINT('Ctrl Pts',(201.999407326833,11.491095196204,28.1202521405945));
#78610=CARTESIAN_POINT('Ctrl Pts',(201.996396404965,11.4384360298945,28.1037170423978));
#78611=CARTESIAN_POINT('Ctrl Pts',(201.994224185589,11.4004452528341,28.0917878518449));
#78612=CARTESIAN_POINT('Ctrl Pts',(201.992051966212,11.3620145209045,28.0814251100782));
#78613=CARTESIAN_POINT('Ctrl Pts',(201.989879746836,11.3232842826823,28.0726529775242));
#78614=CARTESIAN_POINT('Ctrl Pts',(201.986867957455,11.2695846787362,28.0604903865994));
#78615=CARTESIAN_POINT('Ctrl Pts',(201.983856168074,11.2150864731016,28.0513372280561));
#78616=CARTESIAN_POINT('Ctrl Pts',(201.980844378693,11.1601574639435,28.0452897756793));
#78617=CARTESIAN_POINT('Ctrl Pts',(201.977837887911,11.1053250906276,28.0392529625013));
#78618=CARTESIAN_POINT('Ctrl Pts',(201.974831397129,11.0500639380232,28.0363110692666));
#78619=CARTESIAN_POINT('Ctrl Pts',(201.971824906347,10.9947521444968,28.0365094089771));
#78620=CARTESIAN_POINT('Ctrl Pts',(201.968821356631,10.9394944591071,28.0367075546639));
#78621=CARTESIAN_POINT('Ctrl Pts',(201.965817806914,10.8841867558119,28.0400398457189));
#78622=CARTESIAN_POINT('Ctrl Pts',(201.962814257198,10.8292105759947,28.0464996654118));
#78623=CARTESIAN_POINT('Ctrl Pts',(201.959812463292,10.7742665340674,28.0529557088333));
#78624=CARTESIAN_POINT('Ctrl Pts',(201.956810669386,10.7196541542458,28.0625355953953));
#78625=CARTESIAN_POINT('Ctrl Pts',(201.95380887548,10.6657509347894,28.0751807790439));
#78626=CARTESIAN_POINT('Ctrl Pts',(201.950807654747,10.6118580077953,28.0878235481787));
#78627=CARTESIAN_POINT('Ctrl Pts',(201.947806434014,10.5586744853758,28.1035303314076));
#78628=CARTESIAN_POINT('Ctrl Pts',(201.944805213281,10.5065664553562,28.1221917451909));
#78629=CARTESIAN_POINT('Ctrl Pts',(201.94180124864,10.4544107848416,28.1408702204326));
#78630=CARTESIAN_POINT('Ctrl Pts',(201.938797283998,10.4033330685613,28.162508544375));
#78631=CARTESIAN_POINT('Ctrl Pts',(201.935793319357,10.3536815908919,28.1869483010757));
#78632=CARTESIAN_POINT('Ctrl Pts',(201.932787970182,10.3040072287516,28.2113993221119));
#78633=CARTESIAN_POINT('Ctrl Pts',(201.929782621007,10.2557608755156,28.2386540898696));
#78634=CARTESIAN_POINT('Ctrl Pts',(201.926777271833,10.2092653408415,28.2685086485056));
#78635=CARTESIAN_POINT('Ctrl Pts',(201.923766349965,10.1626835914537,28.2984185651936));
#78636=CARTESIAN_POINT('Ctrl Pts',(201.920755428098,10.1178595732152,28.3309375916142));
#78637=CARTESIAN_POINT('Ctrl Pts',(201.917744506231,10.0750852982425,28.365819659634));
#78638=CARTESIAN_POINT('Ctrl Pts',(201.915572286854,10.0442259425348,28.3909852093838));
#78639=CARTESIAN_POINT('Ctrl Pts',(201.913400067478,10.0144327766592,28.4173798080866));
#78640=CARTESIAN_POINT('Ctrl Pts',(201.911227848101,9.98580323183818,28.4448994524454));
#78641=CARTESIAN_POINT('Ctrl Pts',(201.908260856627,9.94669870293719,28.4824879902618));
#78642=CARTESIAN_POINT('Ctrl Pts',(201.905293865153,9.90959419544,28.5223426406126));
#78643=CARTESIAN_POINT('Ctrl Pts',(201.902326873679,9.87476830483212,28.5642191056718));
#78644=CARTESIAN_POINT('Ctrl Pts',(201.89936403944,9.83999121092743,28.6060368950332));
#78645=CARTESIAN_POINT('Ctrl Pts',(201.896401205201,9.80748676148437,28.6498704794296));
#78646=CARTESIAN_POINT('Ctrl Pts',(201.893438370961,9.77749742944438,28.6954381844849));
#78647=CARTESIAN_POINT('Ctrl Pts',(201.890478438173,9.74753746542456,28.7409612658961));
#78648=CARTESIAN_POINT('Ctrl Pts',(201.887518505385,9.72008804040117,28.788214653367));
#78649=CARTESIAN_POINT('Ctrl Pts',(201.884558572597,9.69535034671186,28.8368849781711));
#78650=CARTESIAN_POINT('Ctrl Pts',(201.881600290387,9.67062644776295,28.88552816243));
#78651=CARTESIAN_POINT('Ctrl Pts',(201.878642008177,9.64861152914048,28.9355862335433));
#78652=CARTESIAN_POINT('Ctrl Pts',(201.875683725967,9.62946126115605,28.9867205290214));
#78653=CARTESIAN_POINT('Ctrl Pts',(201.872724575187,9.61030537053443,29.0378698378452));
#78654=CARTESIAN_POINT('Ctrl Pts',(201.869765424407,9.59401600912527,29.0900954949097));
#78655=CARTESIAN_POINT('Ctrl Pts',(201.866806273628,9.58070022768504,29.1430400494359));
#78656=CARTESIAN_POINT('Ctrl Pts',(201.863846530107,9.56738177899201,29.1959952091611));
#78657=CARTESIAN_POINT('Ctrl Pts',(201.860886786587,9.55703820822609,29.249669020086));
#78658=CARTESIAN_POINT('Ctrl Pts',(201.857927043067,9.54972558659084,29.3036931590323));
#78659=CARTESIAN_POINT('Ctrl Pts',(201.854963934922,9.54240465199745,29.3577787123971));
#78660=CARTESIAN_POINT('Ctrl Pts',(201.852000826778,9.53812158435973,29.4122148459862));
#78661=CARTESIAN_POINT('Ctrl Pts',(201.849037718633,9.53688050593125,29.4666294130105));
#78662=CARTESIAN_POINT('Ctrl Pts',(201.848410161049,9.53661765754973,29.4781538908724));
#78663=CARTESIAN_POINT('Ctrl Pts',(201.847782603465,9.53649107191448,29.4896774090577));
#78664=CARTESIAN_POINT('Ctrl Pts',(201.847155045881,9.53650048906759,29.5011964533363));
#78665=CARTESIAN_POINT('',(201.347155045797,9.53650045493154,29.498846057016));
#78666=CARTESIAN_POINT('Ctrl Pts',(201.847155045843,9.53650048906816,29.5011964540331));
#78667=CARTESIAN_POINT('Ctrl Pts',(201.842722901861,9.53656699802896,29.5825500446616));
#78668=CARTESIAN_POINT('Ctrl Pts',(201.838290757878,9.54342041677501,29.6636298191095));
#78669=CARTESIAN_POINT('Ctrl Pts',(201.833858613895,9.5569049506719,29.7435342452402));
#78670=CARTESIAN_POINT('Ctrl Pts',(201.833431059052,9.55820576079773,29.7512423712611));
#78671=CARTESIAN_POINT('Ctrl Pts',(201.833003504209,9.55956824594497,29.7589395808399));
#78672=CARTESIAN_POINT('Ctrl Pts',(201.832575949366,9.56099224510919,29.7666250763977));
#78673=CARTESIAN_POINT('Ctrl Pts',(201.829564159985,9.57102320519047,29.8207633800449));
#78674=CARTESIAN_POINT('Ctrl Pts',(201.826552370604,9.58413437912649,29.8744470074067));
#78675=CARTESIAN_POINT('Ctrl Pts',(201.823540581222,9.60026897905191,29.9273000339289));
#78676=CARTESIAN_POINT('Ctrl Pts',(201.82053409044,9.61637519359999,29.9800600768564));
#78677=CARTESIAN_POINT('Ctrl Pts',(201.817527599659,9.63549412516181,30.031991918523));
#78678=CARTESIAN_POINT('Ctrl Pts',(201.814521108877,9.65751808344034,30.0827302581043));
#78679=CARTESIAN_POINT('Ctrl Pts',(201.81151755916,9.67952049703066,30.1334189634785));
#78680=CARTESIAN_POINT('Ctrl Pts',(201.808514009444,9.70442209847273,30.1829159982691));
#78681=CARTESIAN_POINT('Ctrl Pts',(201.805510459728,9.73206614421684,30.2308734414102));
#78682=CARTESIAN_POINT('Ctrl Pts',(201.802508665822,9.75969402984755,30.2788028496636));
#78683=CARTESIAN_POINT('Ctrl Pts',(201.799506871917,9.7900609190577,30.3251939942497));
#78684=CARTESIAN_POINT('Ctrl Pts',(201.796505078011,9.82296395578155,30.3697231747002));
#78685=CARTESIAN_POINT('Ctrl Pts',(201.793503857278,9.8558607098888,30.4142438525991));
#78686=CARTESIAN_POINT('Ctrl Pts',(201.790502636545,9.89129233635037,30.4569028486328));
#78687=CARTESIAN_POINT('Ctrl Pts',(201.787501415812,9.92901377892201,30.4974070203588));
#78688=CARTESIAN_POINT('Ctrl Pts',(201.784497451171,9.96676970884983,30.5379482235901));
#78689=CARTESIAN_POINT('Ctrl Pts',(201.78149348653,10.0068192768218,30.576330280188));
#78690=CARTESIAN_POINT('Ctrl Pts',(201.778489521889,10.0488794092996,30.6122957663975));
#78691=CARTESIAN_POINT('Ctrl Pts',(201.775484172714,10.0909589273811,30.6482778291753));
#78692=CARTESIAN_POINT('Ctrl Pts',(201.77247882354,10.1350504368179,30.6818407813944));
#78693=CARTESIAN_POINT('Ctrl Pts',(201.769473474365,10.1808390847084,30.7127685866886));
#78694=CARTESIAN_POINT('Ctrl Pts',(201.766462552498,10.2267126365622,30.7437537401108));
#78695=CARTESIAN_POINT('Ctrl Pts',(201.763451630631,10.2742891587209,30.772093715934));
#78696=CARTESIAN_POINT('Ctrl Pts',(201.760440708763,10.3232272698689,30.7976174019143));
#78697=CARTESIAN_POINT('Ctrl Pts',(201.758268489387,10.3585335042961,30.8160313786603));
#78698=CARTESIAN_POINT('Ctrl Pts',(201.75609627001,10.3945478829151,30.8329804820701));
#78699=CARTESIAN_POINT('Ctrl Pts',(201.753924050634,10.4311363806478,30.8484162682857));
#78700=CARTESIAN_POINT('Ctrl Pts',(201.750912261253,10.4818664542887,30.8698180371461));
#78701=CARTESIAN_POINT('Ctrl Pts',(201.747900471872,10.5339110943134,30.8883973313584));
#78702=CARTESIAN_POINT('Ctrl Pts',(201.744888682491,10.5869251185626,30.9039947978271));
#78703=CARTESIAN_POINT('Ctrl Pts',(201.741882191709,10.6398458759761,30.9195648238898));
#78704=CARTESIAN_POINT('Ctrl Pts',(201.738875700927,10.6937321310723,30.9321632854896));
#78705=CARTESIAN_POINT('Ctrl Pts',(201.735869210145,10.7482195748634,30.9416791832853));
#78706=CARTESIAN_POINT('Ctrl Pts',(201.732865660429,10.8026537169286,30.9511857722615));
#78707=CARTESIAN_POINT('Ctrl Pts',(201.729862110713,10.8576873655468,30.9576156810671));
#78708=CARTESIAN_POINT('Ctrl Pts',(201.726858560997,10.9129437442086,30.9609084359834));
#78709=CARTESIAN_POINT('Ctrl Pts',(201.723856767091,10.9681678211823,30.9641992660262));
#78710=CARTESIAN_POINT('Ctrl Pts',(201.720854973185,11.0236138446584,30.9643565460904));
#78711=CARTESIAN_POINT('Ctrl Pts',(201.717853179279,11.0788999011562,30.9613716350051));
#78712=CARTESIAN_POINT('Ctrl Pts',(201.714851958546,11.1341754011483,30.9583872938688));
#78713=CARTESIAN_POINT('Ctrl Pts',(201.711850737812,11.1892904684896,30.9522619817705));
#78714=CARTESIAN_POINT('Ctrl Pts',(201.708849517079,11.2438654972957,30.9430391086969));
#78715=CARTESIAN_POINT('Ctrl Pts',(201.705845552438,11.2984904220849,30.9338078034827));
#78716=CARTESIAN_POINT('Ctrl Pts',(201.702841587797,11.3525738009007,30.9214733679745));
#78717=CARTESIAN_POINT('Ctrl Pts',(201.699837623155,11.4057449460853,30.9061306087011));
#78718=CARTESIAN_POINT('Ctrl Pts',(201.69683227398,11.4589405979627,30.8907807779177));
#78719=CARTESIAN_POINT('Ctrl Pts',(201.693826924805,11.511222679679,30.8724200345367));
#78720=CARTESIAN_POINT('Ctrl Pts',(201.690821575631,11.5622375870957,30.851192490231));
#78721=CARTESIAN_POINT('Ctrl Pts',(201.687810653763,11.6133470893088,30.8299255845831));
#78722=CARTESIAN_POINT('Ctrl Pts',(201.684799731896,11.6631842481321,30.8057814902572));
#78723=CARTESIAN_POINT('Ctrl Pts',(201.681788810028,11.7114183848775,30.7789511842358));
#78724=CARTESIAN_POINT('Ctrl Pts',(201.679616590652,11.7462167393563,30.7595945508906));
#78725=CARTESIAN_POINT('Ctrl Pts',(201.677444371275,11.7801812509772,30.7388407675266));
#78726=CARTESIAN_POINT('Ctrl Pts',(201.675272151899,11.8131977419609,30.7167751158163));
#78727=CARTESIAN_POINT('Ctrl Pts',(201.672260362518,11.8589752163816,30.6861810164238));
#78728=CARTESIAN_POINT('Ctrl Pts',(201.669248573136,11.9031186386945,30.6529365733508));
#78729=CARTESIAN_POINT('Ctrl Pts',(201.666236783755,11.9453050599633,30.6172424059298));
#78730=CARTESIAN_POINT('Ctrl Pts',(201.663230292973,11.9874172632476,30.5816110347613));
#78731=CARTESIAN_POINT('Ctrl Pts',(201.660223802192,12.0275788988573,30.543538830358));
#78732=CARTESIAN_POINT('Ctrl Pts',(201.65721731141,12.0654968787575,30.5032689825555));
#78733=CARTESIAN_POINT('Ctrl Pts',(201.654213761694,12.1033777658226,30.4630385282764));
#78734=CARTESIAN_POINT('Ctrl Pts',(201.651210211977,12.1390189855094,30.4206150717139));
#78735=CARTESIAN_POINT('Ctrl Pts',(201.648206662261,12.1721627874468,30.3762800064619));
#78736=CARTESIAN_POINT('Ctrl Pts',(201.645204868355,12.2052872142318,30.3319708585337));
#78737=CARTESIAN_POINT('Ctrl Pts',(201.642203074449,12.2359168020119,30.2857527386157));
#78738=CARTESIAN_POINT('Ctrl Pts',(201.639201280544,12.2638342617209,30.2379398409764));
#78739=CARTESIAN_POINT('Ctrl Pts',(201.636200059811,12.2917463907762,30.1901360728928));
#78740=CARTESIAN_POINT('Ctrl Pts',(201.633198839077,12.316947154631,30.1407385871525));
#78741=CARTESIAN_POINT('Ctrl Pts',(201.630197618344,12.3392640029974,30.0900882817643));
#78742=CARTESIAN_POINT('Ctrl Pts',(201.627193653703,12.3616012548543,30.0393916686263));
#78743=CARTESIAN_POINT('Ctrl Pts',(201.624189689062,12.3810491109476,29.987440431328));
#78744=CARTESIAN_POINT('Ctrl Pts',(201.621185724421,12.3974828492734,29.9345962908109));
#78745=CARTESIAN_POINT('Ctrl Pts',(201.618180375246,12.4139241619439,29.881727794318));
#78746=CARTESIAN_POINT('Ctrl Pts',(201.615175026071,12.4273484596738,29.8279660867879));
#78747=CARTESIAN_POINT('Ctrl Pts',(201.612169676896,12.4376815934965,29.7736857426347));
#78748=CARTESIAN_POINT('Ctrl Pts',(201.609158755029,12.4480338876144,29.7193047487232));
#78749=CARTESIAN_POINT('Ctrl Pts',(201.606147833162,12.4552834994295,29.664403721238));
#78750=CARTESIAN_POINT('Ctrl Pts',(201.603136911295,12.4594080288043,29.6093638672573));
#78751=CARTESIAN_POINT('Ctrl Pts',(201.600964691918,12.4623836565428,29.5696555511454));
#78752=CARTESIAN_POINT('Ctrl Pts',(201.598792472542,12.4637338249514,29.5298750959088));
#78753=CARTESIAN_POINT('Ctrl Pts',(201.596620253165,12.4634669515017,29.4901647642452));
#78754=CARTESIAN_POINT('Ctrl Pts',(201.593608463784,12.4630969305772,29.4351062574866));
#78755=CARTESIAN_POINT('Ctrl Pts',(201.590596674403,12.4596147135106,29.3799545676392));
#78756=CARTESIAN_POINT('Ctrl Pts',(201.587584885022,12.4530102045503,29.3250897502356));
#78757=CARTESIAN_POINT('Ctrl Pts',(201.58457839424,12.4464173148108,29.2703214557425));
#78758=CARTESIAN_POINT('Ctrl Pts',(201.581571903458,12.4367130971049,29.2158395515752));
#78759=CARTESIAN_POINT('Ctrl Pts',(201.578565412676,12.4239394326528,29.1620225715577));
#78760=CARTESIAN_POINT('Ctrl Pts',(201.57556186296,12.4111782638935,29.1082582373925));
#78761=CARTESIAN_POINT('Ctrl Pts',(201.572558313244,12.3953537181153,29.0551580494608));
#78762=CARTESIAN_POINT('Ctrl Pts',(201.569554763527,12.3765590192188,29.0030920441296));
#78763=CARTESIAN_POINT('Ctrl Pts',(201.566552969621,12.3577753072983,28.9510564754631));
#78764=CARTESIAN_POINT('Ctrl Pts',(201.563551175716,12.3360250626919,28.9000543861345));
#78765=CARTESIAN_POINT('Ctrl Pts',(201.56054938181,12.3114511579773,28.8504400641665));
#78766=CARTESIAN_POINT('Ctrl Pts',(201.557548161076,12.2868819454868,28.8008352157242));
#78767=CARTESIAN_POINT('Ctrl Pts',(201.554546940343,12.2594903777988,28.752618080638));
#78768=CARTESIAN_POINT('Ctrl Pts',(201.55154571961,12.2294662372717,28.7061202727056));
#78769=CARTESIAN_POINT('Ctrl Pts',(201.548541754969,12.1994146467543,28.6595799535022));
#78770=CARTESIAN_POINT('Ctrl Pts',(201.545537790328,12.1667259619551,28.6147625456171));
#78771=CARTESIAN_POINT('Ctrl Pts',(201.542533825686,12.131633663166,28.5719711737292));
#78772=CARTESIAN_POINT('Ctrl Pts',(201.539528476511,12.0965251902624,28.5291600792078));
#78773=CARTESIAN_POINT('Ctrl Pts',(201.536523127336,12.0590112527024,28.4883772708833));
#78774=CARTESIAN_POINT('Ctrl Pts',(201.533517778162,12.0193638829366,28.4498907084668));
#78775=CARTESIAN_POINT('Ctrl Pts',(201.530506856294,11.9796429967213,28.411332782037));
#78776=CARTESIAN_POINT('Ctrl Pts',(201.527495934427,11.9377811759394,28.3750799524755));
#78777=CARTESIAN_POINT('Ctrl Pts',(201.524485012559,11.894084456764,28.3413606108141));
#78778=CARTESIAN_POINT('Ctrl Pts',(201.522312793183,11.8625596068125,28.3170339060546));
#78779=CARTESIAN_POINT('Ctrl Pts',(201.520140573806,11.8300804229227,28.2940249906641));
#78780=CARTESIAN_POINT('Ctrl Pts',(201.51796835443,11.7967703429812,28.2724050869502));
#78781=CARTESIAN_POINT('Ctrl Pts',(201.514956565049,11.7505858064956,28.2424290186358));
#78782=CARTESIAN_POINT('Ctrl Pts',(201.511944775668,11.7026115779343,28.2150007827707));
#78783=CARTESIAN_POINT('Ctrl Pts',(201.508932986287,11.6531594998416,28.1903378612151));
#78784=CARTESIAN_POINT('Ctrl Pts',(201.505926495505,11.6037944221024,28.1657183287946));
#78785=CARTESIAN_POINT('Ctrl Pts',(201.502920004723,11.5529571229392,28.1438546891898));
#78786=CARTESIAN_POINT('Ctrl Pts',(201.499913513941,11.5009867641489,28.1249201797177));
#78787=CARTESIAN_POINT('Ctrl Pts',(201.496909964225,11.4490672447745,28.1060041927154));
#78788=CARTESIAN_POINT('Ctrl Pts',(201.493906414509,11.3960173547821,28.0900118389401));
#78789=CARTESIAN_POINT('Ctrl Pts',(201.490902864792,11.3421974006717,28.0770688038512));
#78790=CARTESIAN_POINT('Ctrl Pts',(201.487901070887,11.2884089085467,28.0641333349817));
#78791=CARTESIAN_POINT('Ctrl Pts',(201.484899276981,11.2338517564166,28.0542437744356));
#78792=CARTESIAN_POINT('Ctrl Pts',(201.481897483075,11.1789004082605,28.0474756821574));
#78793=CARTESIAN_POINT('Ctrl Pts',(201.478896262342,11.1239595526997,28.0407088822014));
#78794=CARTESIAN_POINT('Ctrl Pts',(201.475895041609,11.0686251737817,28.037062431038));
#78795=CARTESIAN_POINT('Ctrl Pts',(201.472893820875,11.0132786024162,28.0365602408306));
#78796=CARTESIAN_POINT('Ctrl Pts',(201.469889856234,10.9578814296741,28.0360575914887));
#78797=CARTESIAN_POINT('Ctrl Pts',(201.466885891593,10.9024725706955,28.0387049505745));
#78798=CARTESIAN_POINT('Ctrl Pts',(201.463881926952,10.8474336004443,28.0444740662817));
#78799=CARTESIAN_POINT('Ctrl Pts',(201.460876577777,10.7923692626156,28.0502458409865));
#78800=CARTESIAN_POINT('Ctrl Pts',(201.457871228602,10.7376756747593,28.0591421555882));
#78801=CARTESIAN_POINT('Ctrl Pts',(201.454865879428,10.6837262502445,28.0710832196326));
#78802=CARTESIAN_POINT('Ctrl Pts',(201.45185495756,10.6296767895818,28.0830464254896));
#78803=CARTESIAN_POINT('Ctrl Pts',(201.448844035693,10.576374757268,28.0980655147301));
#78804=CARTESIAN_POINT('Ctrl Pts',(201.445833113826,10.5241792255266,28.1160105345128));
#78805=CARTESIAN_POINT('Ctrl Pts',(201.443660894449,10.4865229360539,28.1289569082154));
#78806=CARTESIAN_POINT('Ctrl Pts',(201.441488675073,10.4494422378693,28.1434251284135));
#78807=CARTESIAN_POINT('Ctrl Pts',(201.439316455696,10.4130645082021,28.1593512844641));
#78808=CARTESIAN_POINT('Ctrl Pts',(201.436304666315,10.3626266651817,28.1814329527306));
#78809=CARTESIAN_POINT('Ctrl Pts',(201.433292876934,10.3133321681557,28.2064106886505));
#78810=CARTESIAN_POINT('Ctrl Pts',(201.430281087553,10.2655341725827,28.2341436896882));
#78811=CARTESIAN_POINT('Ctrl Pts',(201.427274596771,10.2178202673589,28.2618279004426));
#78812=CARTESIAN_POINT('Ctrl Pts',(201.424268105989,10.171598091173,28.2922574937954));
#78813=CARTESIAN_POINT('Ctrl Pts',(201.421261615207,10.1271988765727,28.3252445152526));
#78814=CARTESIAN_POINT('Ctrl Pts',(201.418258065491,10.0828430950021,28.3581992675291));
#78815=CARTESIAN_POINT('Ctrl Pts',(201.415254515775,10.0403071634838,28.3937061786499));
#78816=CARTESIAN_POINT('Ctrl Pts',(201.412250966059,9.99989423328979,28.431533479517));
#78817=CARTESIAN_POINT('Ctrl Pts',(201.409249172153,9.95950492762379,28.4693386673593));
#78818=CARTESIAN_POINT('Ctrl Pts',(201.406247378247,9.92123654752231,28.5094611964513));
#78819=CARTESIAN_POINT('Ctrl Pts',(201.403245584341,9.88535817030107,28.5516299026828));
#78820=CARTESIAN_POINT('Ctrl Pts',(201.400244363608,9.84948664381794,28.5937905570796));
#78821=CARTESIAN_POINT('Ctrl Pts',(201.397243142875,9.81600455531122,28.6379962110796));
#78822=CARTESIAN_POINT('Ctrl Pts',(201.394241922142,9.78514162666474,28.6839415567882));
#78823=CARTESIAN_POINT('Ctrl Pts',(201.3912379575,9.75425048115431,28.7299289086715));
#78824=CARTESIAN_POINT('Ctrl Pts',(201.388233992859,9.72598357383232,28.7776586909242));
#78825=CARTESIAN_POINT('Ctrl Pts',(201.385230028218,9.70052719713442,28.8267966988995));
#78826=CARTESIAN_POINT('Ctrl Pts',(201.382224679043,9.67505908753884,28.8759573546861));
#78827=CARTESIAN_POINT('Ctrl Pts',(201.379219329868,9.65240430669399,28.9265270478923));
#78828=CARTESIAN_POINT('Ctrl Pts',(201.376213980694,9.63270161626161,28.9781500408869));
#78829=CARTESIAN_POINT('Ctrl Pts',(201.373203058826,9.61296239195937,29.0298687562252));
#78830=CARTESIAN_POINT('Ctrl Pts',(201.370192136959,9.59618635228284,29.0826441689016));
#78831=CARTESIAN_POINT('Ctrl Pts',(201.367181215092,9.58246247839736,29.1361049260451));
#78832=CARTESIAN_POINT('Ctrl Pts',(201.365008995715,9.57256143609598,29.1746740080957));
#78833=CARTESIAN_POINT('Ctrl Pts',(201.362836776339,9.56424793889115,29.2135994925215));
#78834=CARTESIAN_POINT('Ctrl Pts',(201.360664556962,9.55753867729102,29.2527398485629));
#78835=CARTESIAN_POINT('Ctrl Pts',(201.356161386589,9.54362988502569,29.3338806825054));
#78836=CARTESIAN_POINT('Ctrl Pts',(201.351658216216,9.53656559886766,29.4162266799627));
#78837=CARTESIAN_POINT('Ctrl Pts',(201.347155045843,9.53650045493221,29.498846056164));
#78838=CARTESIAN_POINT('',(200.847155045799,9.5365000165217,29.5002199068106));
#78839=CARTESIAN_POINT('Ctrl Pts',(201.347155045797,9.53650045493154,29.498846057016));
#78840=CARTESIAN_POINT('Ctrl Pts',(201.344192093687,9.53645759219208,29.553207148138));
#78841=CARTESIAN_POINT('Ctrl Pts',(201.341229141578,9.53944780435113,29.6076722695148));
#78842=CARTESIAN_POINT('Ctrl Pts',(201.338266189469,9.54547934964435,29.661870095104));
#78843=CARTESIAN_POINT('Ctrl Pts',(201.335306223428,9.55150481633468,29.7160133000208));
#78844=CARTESIAN_POINT('Ctrl Pts',(201.332346257388,9.56056549112173,29.7698892039572));
#78845=CARTESIAN_POINT('Ctrl Pts',(201.329386291347,9.57261762047123,29.8231281365198));
#78846=CARTESIAN_POINT('Ctrl Pts',(201.326428059793,9.58466268749527,29.8763358720502));
#78847=CARTESIAN_POINT('Ctrl Pts',(201.323469828238,9.59969561773625,29.9289068453346));
#78848=CARTESIAN_POINT('Ctrl Pts',(201.320511596683,9.6176214115198,29.9804806844312));
#78849=CARTESIAN_POINT('Ctrl Pts',(201.31755385102,9.63554426097183,30.0320460524675));
#78850=CARTESIAN_POINT('Ctrl Pts',(201.314596105358,9.65635885098129,30.0826140977086));
#78851=CARTESIAN_POINT('Ctrl Pts',(201.311638359696,9.67992084960482,30.1318411878724));
#78852=CARTESIAN_POINT('Ctrl Pts',(201.308677930102,9.70350422897435,30.1811129479271));
#78853=CARTESIAN_POINT('Ctrl Pts',(201.305717500507,9.72983975539072,30.2290408332694));
#78854=CARTESIAN_POINT('Ctrl Pts',(201.302757070913,9.75873639576856,30.2753044013872));
#78855=CARTESIAN_POINT('Ctrl Pts',(201.299795054642,9.78764852363554,30.3215927650002));
#78856=CARTESIAN_POINT('Ctrl Pts',(201.296833038371,9.81912418044058,30.3662145931671));
#78857=CARTESIAN_POINT('Ctrl Pts',(201.2938710221,9.85293006357957,30.4088799761027));
#78858=CARTESIAN_POINT('Ctrl Pts',(201.290903953149,9.88679361362549,30.4516181386978));
#78859=CARTESIAN_POINT('Ctrl Pts',(201.287936884198,9.9229949535335,30.4923927964874));
#78860=CARTESIAN_POINT('Ctrl Pts',(201.284969815247,9.96126292918511,30.5309498279329));
#78861=CARTESIAN_POINT('Ctrl Pts',(201.28398409624,9.97397630779195,30.5437592365932));
#78862=CARTESIAN_POINT('Ctrl Pts',(201.282998377234,9.98691750783958,30.5563242146305));
#78863=CARTESIAN_POINT('Ctrl Pts',(201.282012658228,10.000075815232,30.568636455824));
#78864=CARTESIAN_POINT('Ctrl Pts',(201.279000868847,10.040280021733,30.6062555714649));
#78865=CARTESIAN_POINT('Ctrl Pts',(201.275989079466,10.0826934464971,30.6416806491432));
#78866=CARTESIAN_POINT('Ctrl Pts',(201.272977290085,10.1270472744573,30.6746428346385));
#78867=CARTESIAN_POINT('Ctrl Pts',(201.269970799303,10.1713230713445,30.7075470302191));
#78868=CARTESIAN_POINT('Ctrl Pts',(201.266964308521,10.2175320766006,30.7379966206306));
#78869=CARTESIAN_POINT('Ctrl Pts',(201.263957817739,10.2653708121964,30.7657615124608));
#78870=CARTESIAN_POINT('Ctrl Pts',(201.260954268023,10.31316275009,30.7934992435995));
#78871=CARTESIAN_POINT('Ctrl Pts',(201.257950718307,10.362580805985,30.8185572155652));
#78872=CARTESIAN_POINT('Ctrl Pts',(201.254947168591,10.4132923368601,30.8407484357675));
#78873=CARTESIAN_POINT('Ctrl Pts',(201.251945374685,10.4639742228671,30.8629266834606));
#78874=CARTESIAN_POINT('Ctrl Pts',(201.248943580779,10.5159476027901,30.8822412902575));
#78875=CARTESIAN_POINT('Ctrl Pts',(201.245941786873,10.5688570954449,30.8985521248247));
#78876=CARTESIAN_POINT('Ctrl Pts',(201.24294056614,10.621756485383,30.9148598449463));
#78877=CARTESIAN_POINT('Ctrl Pts',(201.239939345407,10.6755911292852,30.9281647768232));
#78878=CARTESIAN_POINT('Ctrl Pts',(201.236938124674,10.7299898178405,30.9383764290095));
#78879=CARTESIAN_POINT('Ctrl Pts',(201.233934160032,10.7844382411575,30.9485974173417));
#78880=CARTESIAN_POINT('Ctrl Pts',(201.230930195391,10.8394512198701,30.9557193789124));
#78881=CARTESIAN_POINT('Ctrl Pts',(201.22792623075,10.8946481459147,30.9597031331202));
#78882=CARTESIAN_POINT('Ctrl Pts',(201.224920881575,10.9498705123389,30.9636887234486));
#78883=CARTESIAN_POINT('Ctrl Pts',(201.2219155324,11.0052764668911,30.9645332151621));
#78884=CARTESIAN_POINT('Ctrl Pts',(201.218910183226,11.0604843876251,30.9622495986847));
#78885=CARTESIAN_POINT('Ctrl Pts',(201.215899261358,11.1157946780836,30.9599617477934));
#78886=CARTESIAN_POINT('Ctrl Pts',(201.212888339491,11.170905675232,30.9545342544754));
#78887=CARTESIAN_POINT('Ctrl Pts',(201.209877417624,11.2254410684357,30.9460320102482));
#78888=CARTESIAN_POINT('Ctrl Pts',(201.207705198247,11.2647854430297,30.9398980949666));
#78889=CARTESIAN_POINT('Ctrl Pts',(201.205532978871,11.303830359524,30.9321649151874));
#78890=CARTESIAN_POINT('Ctrl Pts',(201.203360759494,11.3424391984059,30.922873025043));
#78891=CARTESIAN_POINT('Ctrl Pts',(201.200348970113,11.3959704817639,30.9099897884927));
#78892=CARTESIAN_POINT('Ctrl Pts',(201.197337180732,11.4488846450223,30.8940547310599));
#78893=CARTESIAN_POINT('Ctrl Pts',(201.194325391351,11.5008092975111,30.8751444642387));
#78894=CARTESIAN_POINT('Ctrl Pts',(201.191318900569,11.5526425996807,30.8562674659871));
#78895=CARTESIAN_POINT('Ctrl Pts',(201.188312409787,11.6034893542792,30.8344258252572));
#78896=CARTESIAN_POINT('Ctrl Pts',(201.185305919005,11.6529904744886,30.8097464221089));
#78897=CARTESIAN_POINT('Ctrl Pts',(201.182302369289,11.7024431707867,30.7850911613078));
#78898=CARTESIAN_POINT('Ctrl Pts',(201.179298819573,11.7505523707667,30.7576038717952));
#78899=CARTESIAN_POINT('Ctrl Pts',(201.176295269857,11.7969789401109,30.7274594979142));
#78900=CARTESIAN_POINT('Ctrl Pts',(201.173293475951,11.8433783694832,30.6973327457845));
#78901=CARTESIAN_POINT('Ctrl Pts',(201.170291682045,11.888096676508,30.6645522748734));
#78902=CARTESIAN_POINT('Ctrl Pts',(201.167289888139,11.9308213549158,30.6293377950077));
#78903=CARTESIAN_POINT('Ctrl Pts',(201.164288667406,11.9735378753296,30.5941300391133));
#78904=CARTESIAN_POINT('Ctrl Pts',(201.161287446673,12.0142611165139,30.5564895326906));
#78905=CARTESIAN_POINT('Ctrl Pts',(201.15828622594,12.0527113216486,30.5166765086658));
#78906=CARTESIAN_POINT('Ctrl Pts',(201.155282261299,12.091196680421,30.4768270850271));
#78907=CARTESIAN_POINT('Ctrl Pts',(201.152278296657,12.1274044845283,30.4348015560576));
#78908=CARTESIAN_POINT('Ctrl Pts',(201.149274332016,12.161092658561,30.3908962275348));
#78909=CARTESIAN_POINT('Ctrl Pts',(201.146268982841,12.1947963595441,30.3469706629535));
#78910=CARTESIAN_POINT('Ctrl Pts',(201.143263633666,12.2259778183005,30.3011640084597));
#78911=CARTESIAN_POINT('Ctrl Pts',(201.140258284492,12.2544379713151,30.2538021133712));
#78912=CARTESIAN_POINT('Ctrl Pts',(201.137247362624,12.2829508967939,30.2063523971135));
#78913=CARTESIAN_POINT('Ctrl Pts',(201.134236440757,12.3087321911588,30.1573421476625));
#78914=CARTESIAN_POINT('Ctrl Pts',(201.131225518889,12.3316290565517,30.1071213270404));
#78915=CARTESIAN_POINT('Ctrl Pts',(201.129053299513,12.3481479224871,30.0708896862116));
#78916=CARTESIAN_POINT('Ctrl Pts',(201.126881080136,12.3631664770608,30.0340284519386));
#78917=CARTESIAN_POINT('Ctrl Pts',(201.12470886076,12.3766434403009,29.9966740261746));
#78918=CARTESIAN_POINT('Ctrl Pts',(201.121697071379,12.3953292945997,29.9448819907726));
#78919=CARTESIAN_POINT('Ctrl Pts',(201.118685281998,12.4111270334017,29.8919266683069));
#78920=CARTESIAN_POINT('Ctrl Pts',(201.115673492617,12.4238958027391,29.8381611937258));
#78921=CARTESIAN_POINT('Ctrl Pts',(201.112667001835,12.436642108158,29.7844903079966));
#78922=CARTESIAN_POINT('Ctrl Pts',(201.109660511053,12.4463698987706,29.7300126078546));
#78923=CARTESIAN_POINT('Ctrl Pts',(201.106654020271,12.4529876192118,29.6750977681673));
#78924=CARTESIAN_POINT('Ctrl Pts',(201.103650470555,12.4595988659429,29.620236648301));
#78925=CARTESIAN_POINT('Ctrl Pts',(201.100646920838,12.4631060069446,29.5649397571637));
#78926=CARTESIAN_POINT('Ctrl Pts',(201.097643371122,12.4634686017004,29.509586544585));
#78927=CARTESIAN_POINT('Ctrl Pts',(201.094641577216,12.4638309844912,29.4542656903015));
#78928=CARTESIAN_POINT('Ctrl Pts',(201.09163978331,12.4610524613765,29.3988891062102));
#78929=CARTESIAN_POINT('Ctrl Pts',(201.088637989405,12.4551446236655,29.3438386276398));
#78930=CARTESIAN_POINT('Ctrl Pts',(201.085636768671,12.4492379140169,29.2887986605932));
#78931=CARTESIAN_POINT('Ctrl Pts',(201.082635547938,12.440203132903,29.2340851994841));
#78932=CARTESIAN_POINT('Ctrl Pts',(201.079634327205,12.4281037276099,29.1800750194395));
#78933=CARTESIAN_POINT('Ctrl Pts',(201.076630362564,12.4159932602664,29.1260154598326));
#78934=CARTESIAN_POINT('Ctrl Pts',(201.073626397923,12.4008126870476,29.072660981481));
#78935=CARTESIAN_POINT('Ctrl Pts',(201.070622433281,12.3826763075204,29.0203767326102));
#78936=CARTESIAN_POINT('Ctrl Pts',(201.067617084106,12.3645315688977,28.9680683858188));
#78937=CARTESIAN_POINT('Ctrl Pts',(201.064611734932,12.3434285095276,28.916831740229));
#78938=CARTESIAN_POINT('Ctrl Pts',(201.061606385757,12.319529760483,28.8670122740529));
#78939=CARTESIAN_POINT('Ctrl Pts',(201.058595463889,12.2955866969936,28.8171004297369));
#78940=CARTESIAN_POINT('Ctrl Pts',(201.055584542022,12.2688378443226,28.7686114766531));
#78941=CARTESIAN_POINT('Ctrl Pts',(201.052573620155,12.2394914193359,28.72186551844));
#78942=CARTESIAN_POINT('Ctrl Pts',(201.050401400778,12.21831954049,28.6881408053184));
#78943=CARTESIAN_POINT('Ctrl Pts',(201.048229181402,12.1957966189195,28.6553227374654));
#78944=CARTESIAN_POINT('Ctrl Pts',(201.046056962025,12.1720138618117,28.6235208172916));
#78945=CARTESIAN_POINT('Ctrl Pts',(201.043045172644,12.1390389900826,28.5794273493344));
#78946=CARTESIAN_POINT('Ctrl Pts',(201.040033383263,12.1035040066266,28.5371059637289));
#78947=CARTESIAN_POINT('Ctrl Pts',(201.037021593882,12.0656263478846,28.4968685346904));
#78948=CARTESIAN_POINT('Ctrl Pts',(201.0340151031,12.027815326781,28.4567018948014));
#78949=CARTESIAN_POINT('Ctrl Pts',(201.031008612318,11.9876701684204,28.4186123163942));
#78950=CARTESIAN_POINT('Ctrl Pts',(201.028002121536,11.9454492390576,28.3828796007747));
#78951=CARTESIAN_POINT('Ctrl Pts',(201.02499857182,11.9032696118417,28.3471818402802));
#78952=CARTESIAN_POINT('Ctrl Pts',(201.021995022103,11.8590186370682,28.3138367141126));
#78953=CARTESIAN_POINT('Ctrl Pts',(201.018991472387,11.8129909602191,28.2830867127843));
#78954=CARTESIAN_POINT('Ctrl Pts',(201.015989678481,11.7669901901578,28.2523546872441));
#78955=CARTESIAN_POINT('Ctrl Pts',(201.012987884575,11.7192152144912,28.2242150718159));
#78956=CARTESIAN_POINT('Ctrl Pts',(201.00998609067,11.669991291152,28.1988682158288));
#78957=CARTESIAN_POINT('Ctrl Pts',(201.006984869936,11.6207767667944,28.1735261996557));
#78958=CARTESIAN_POINT('Ctrl Pts',(201.003983649203,11.5701143129518,28.1509761249983));
#78959=CARTESIAN_POINT('Ctrl Pts',(201.00098242847,11.5183534851549,28.1313722513306));
#78960=CARTESIAN_POINT('Ctrl Pts',(200.997978463829,11.4665453342977,28.1117504545474));
#78961=CARTESIAN_POINT('Ctrl Pts',(200.994974499188,11.4136372976572,28.0950804268823));
#78962=CARTESIAN_POINT('Ctrl Pts',(200.991970534546,11.3599971922288,28.0814675641398));
#78963=CARTESIAN_POINT('Ctrl Pts',(200.988965185372,11.3063323639627,28.0678484272002));
#78964=CARTESIAN_POINT('Ctrl Pts',(200.985959836197,11.2519353129124,28.0572893645905));
#78965=CARTESIAN_POINT('Ctrl Pts',(200.982954487022,11.1971840139354,28.0498445894842));
#78966=CARTESIAN_POINT('Ctrl Pts',(200.979943565154,11.1423311919285,28.0423860098447));
#78967=CARTESIAN_POINT('Ctrl Pts',(200.976932643287,11.0871233368434,28.0380532939104));
#78968=CARTESIAN_POINT('Ctrl Pts',(200.97392172142,11.0319423070637,28.0368486274416));
#78969=CARTESIAN_POINT('Ctrl Pts',(200.971749502044,10.9921321401553,28.0359795249007));
#78970=CARTESIAN_POINT('Ctrl Pts',(200.969577282667,10.9523359950373,28.0367374212764));
#78971=CARTESIAN_POINT('Ctrl Pts',(200.967405063291,10.9126954892126,28.0391063788228));
#78972=CARTESIAN_POINT('Ctrl Pts',(200.96439327391,10.8577337962055,28.0423909463303));
#78973=CARTESIAN_POINT('Ctrl Pts',(200.961381484529,10.8028438256294,28.0487882784945));
#78974=CARTESIAN_POINT('Ctrl Pts',(200.958369695148,10.7484056344831,28.0582883349157));
#78975=CARTESIAN_POINT('Ctrl Pts',(200.955363204366,10.6940632156898,28.0677716780196));
#78976=CARTESIAN_POINT('Ctrl Pts',(200.952356713584,10.6401715144009,28.0803468223565));
#78977=CARTESIAN_POINT('Ctrl Pts',(200.949350222803,10.5871063161268,28.0959519040227));
#78978=CARTESIAN_POINT('Ctrl Pts',(200.946346673086,10.534093028283,28.111541720194));
#78979=CARTESIAN_POINT('Ctrl Pts',(200.94334312337,10.4819051452679,28.1301554536672));
#78980=CARTESIAN_POINT('Ctrl Pts',(200.940339573654,10.4309072487217,28.1516804197659));
#78981=CARTESIAN_POINT('Ctrl Pts',(200.937337779748,10.3799391644468,28.1731928028335));
#78982=CARTESIAN_POINT('Ctrl Pts',(200.934335985842,10.330160172681,28.1976128404063));
#78983=CARTESIAN_POINT('Ctrl Pts',(200.931334191937,10.2819165001657,28.2247791025607));
#78984=CARTESIAN_POINT('Ctrl Pts',(200.928332971203,10.2336820394597,28.2519401774976));
#78985=CARTESIAN_POINT('Ctrl Pts',(200.92533175047,10.1869827749869,28.281846176795));
#78986=CARTESIAN_POINT('Ctrl Pts',(200.922330529737,10.1421398074332,28.3142900270263));
#78987=CARTESIAN_POINT('Ctrl Pts',(200.919326565096,10.0972558415695,28.3467635395012));
#78988=CARTESIAN_POINT('Ctrl Pts',(200.916322600455,10.0542319911496,28.3817792282481));
#78989=CARTESIAN_POINT('Ctrl Pts',(200.913318635814,10.0133585941167,28.4190878915487));
#78990=CARTESIAN_POINT('Ctrl Pts',(200.910313286639,9.97246635844887,28.456413750491));
#78991=CARTESIAN_POINT('Ctrl Pts',(200.907307937464,9.93372692119503,28.4960343129212));
#78992=CARTESIAN_POINT('Ctrl Pts',(200.904302588289,9.89739346351284,28.5376637408391));
#78993=CARTESIAN_POINT('Ctrl Pts',(200.901291666422,9.86099263422881,28.5793703604537));
#78994=CARTESIAN_POINT('Ctrl Pts',(200.898280744555,9.8270070202741,28.6230928687812));
#78995=CARTESIAN_POINT('Ctrl Pts',(200.895269822687,9.79564848930181,28.6685135667499));
#78996=CARTESIAN_POINT('Ctrl Pts',(200.89309760331,9.77302498340972,28.7012821753632));
#78997=CARTESIAN_POINT('Ctrl Pts',(200.890925383934,9.75176794569159,28.7349340092125));
#78998=CARTESIAN_POINT('Ctrl Pts',(200.888753164557,9.73194196315828,28.7693420326848));
#78999=CARTESIAN_POINT('Ctrl Pts',(200.885626860487,9.70340798977802,28.8188627877939));
#79000=CARTESIAN_POINT('Ctrl Pts',(200.882500556418,9.67772949073588,28.8701424352536));
#79001=CARTESIAN_POINT('Ctrl Pts',(200.879374252349,9.65511699549504,28.9228328195456));
#79002=CARTESIAN_POINT('Ctrl Pts',(200.876256197382,9.63256416585403,28.9753841743607));
#79003=CARTESIAN_POINT('Ctrl Pts',(200.873138142416,9.61306143181151,29.0293384316797));
#79004=CARTESIAN_POINT('Ctrl Pts',(200.87002008745,9.59677327652103,29.0843234279942));
#79005=CARTESIAN_POINT('Ctrl Pts',(200.86690698055,9.58051096903304,29.1392211681831));
#79006=CARTESIAN_POINT('Ctrl Pts',(200.86379387365,9.56745324435004,29.1951459509428));
#79007=CARTESIAN_POINT('Ctrl Pts',(200.86068076675,9.55771612755834,29.2517068641813));
#79008=CARTESIAN_POINT('Ctrl Pts',(200.857572952157,9.54799556394529,29.3081716234019));
#79009=CARTESIAN_POINT('Ctrl Pts',(200.854465137565,9.54158446134469,29.3652699002605));
#79010=CARTESIAN_POINT('Ctrl Pts',(200.851357322972,9.53854821497931,29.42259890143));
#79011=CARTESIAN_POINT('Ctrl Pts',(200.849956563929,9.53717971327944,29.4484383182992));
#79012=CARTESIAN_POINT('Ctrl Pts',(200.848555804886,9.5364961254632,29.4743244608338));
#79013=CARTESIAN_POINT('Ctrl Pts',(200.847155045843,9.53650001652158,29.5002199060039));
#79014=CARTESIAN_POINT('',(200.347155045877,9.53650026306434,29.5008774903221));
#79015=CARTESIAN_POINT('Ctrl Pts',(200.847155045799,9.5365000165217,29.5002199068106));
#79016=CARTESIAN_POINT('Ctrl Pts',(200.84396942673,9.53650886563482,29.55911156583));
#79017=CARTESIAN_POINT('Ctrl Pts',(200.840783807662,9.54007672876269,29.6179197105645));
#79018=CARTESIAN_POINT('Ctrl Pts',(200.837598188593,9.54714789381235,29.6762186356379));
#79019=CARTESIAN_POINT('Ctrl Pts',(200.834406499263,9.55423253310804,29.7346286504759));
#79020=CARTESIAN_POINT('Ctrl Pts',(200.831214809934,9.56483370669795,29.7925270926805));
#79021=CARTESIAN_POINT('Ctrl Pts',(200.828023120604,9.5788446640183,29.8494993004439));
#79022=CARTESIAN_POINT('Ctrl Pts',(200.824820092136,9.59290539816992,29.9066739137893));
#79023=CARTESIAN_POINT('Ctrl Pts',(200.821617063669,9.61040001838629,29.9629153027575));
#79024=CARTESIAN_POINT('Ctrl Pts',(200.818414035201,9.63117184102155,30.0178240253094));
#79025=CARTESIAN_POINT('Ctrl Pts',(200.815643112075,9.64914143582681,30.065325273171));
#79026=CARTESIAN_POINT('Ctrl Pts',(200.812872188948,9.66956278947609,30.1118293448901));
#79027=CARTESIAN_POINT('Ctrl Pts',(200.810101265822,9.69230685329164,30.1570927514834));
#79028=CARTESIAN_POINT('Ctrl Pts',(200.807089476441,9.71702797573658,30.2062907411541));
#79029=CARTESIAN_POINT('Ctrl Pts',(200.80407768706,9.74458056961052,30.2541936565157));
#79030=CARTESIAN_POINT('Ctrl Pts',(200.801065897678,9.77480533209191,30.3004562922044));
#79031=CARTESIAN_POINT('Ctrl Pts',(200.798059406896,9.80497692056885,30.3466375386813));
#79032=CARTESIAN_POINT('Ctrl Pts',(200.795052916114,9.83781106166955,30.3911837944356));
#79033=CARTESIAN_POINT('Ctrl Pts',(200.792046425332,9.8731025274536,30.4337742427207));
#79034=CARTESIAN_POINT('Ctrl Pts',(200.789042875615,9.90835946976022,30.4763230273812));
#79035=CARTESIAN_POINT('Ctrl Pts',(200.786039325899,9.94606863962023,30.516919390722));
#79036=CARTESIAN_POINT('Ctrl Pts',(200.783035776182,9.98598254270118,30.555272877645));
#79037=CARTESIAN_POINT('Ctrl Pts',(200.780033982276,10.0258731129746,30.5936039439462));
#79038=CARTESIAN_POINT('Ctrl Pts',(200.77703218837,10.067965482149,30.6296943680802));
#79039=CARTESIAN_POINT('Ctrl Pts',(200.774030394464,10.111974620175,30.6632898068782));
#79040=CARTESIAN_POINT('Ctrl Pts',(200.771029173731,10.155975354948,30.69687883085));
#79041=CARTESIAN_POINT('Ctrl Pts',(200.768027952997,10.2018917125966,30.7279734959418));
#79042=CARTESIAN_POINT('Ctrl Pts',(200.765026732264,10.2494066508443,30.7563605669565));
#79043=CARTESIAN_POINT('Ctrl Pts',(200.762022767622,10.2969650302885,30.7847735912477));
#79044=CARTESIAN_POINT('Ctrl Pts',(200.759018802981,10.3461244562801,30.8104738052582));
#79045=CARTESIAN_POINT('Ctrl Pts',(200.756014838339,10.396541329686,30.8332928722613));
#79046=CARTESIAN_POINT('Ctrl Pts',(200.753009489164,10.4469814403351,30.8561224566205));
#79047=CARTESIAN_POINT('Ctrl Pts',(200.750004139989,10.4986796608108,30.8760680567951));
#79048=CARTESIAN_POINT('Ctrl Pts',(200.746998790814,10.5512734057079,30.8930099402283));
#79049=CARTESIAN_POINT('Ctrl Pts',(200.743987868947,10.6039646729731,30.9099832382832));
#79050=CARTESIAN_POINT('Ctrl Pts',(200.740976947079,10.6575542700626,30.9239415610611));
#79051=CARTESIAN_POINT('Ctrl Pts',(200.737966025212,10.7116666538547,30.9348157134283));
#79052=CARTESIAN_POINT('Ctrl Pts',(200.735793805837,10.7507058496962,30.9426608337893));
#79053=CARTESIAN_POINT('Ctrl Pts',(200.733621586463,10.7900168956643,30.9489017660119));
#79054=CARTESIAN_POINT('Ctrl Pts',(200.731449367089,10.8294575758292,30.9535293363252));
#79055=CARTESIAN_POINT('Ctrl Pts',(200.728437577709,10.8841422099411,30.9599454779422));
#79056=CARTESIAN_POINT('Ctrl Pts',(200.725425788328,10.9393027474571,30.9632846138945));
#79057=CARTESIAN_POINT('Ctrl Pts',(200.722413998947,10.9945632720978,30.9634899015674));
#79058=CARTESIAN_POINT('Ctrl Pts',(200.719407508166,11.0497265776658,30.9636948280805));
#79059=CARTESIAN_POINT('Ctrl Pts',(200.716401017385,11.1049889980205,30.9607768461116));
#79060=CARTESIAN_POINT('Ctrl Pts',(200.713394526603,11.1599697233074,30.9547308815121));
#79061=CARTESIAN_POINT('Ctrl Pts',(200.710390976887,11.2148966643214,30.9486908313091));
#79062=CARTESIAN_POINT('Ctrl Pts',(200.707387427171,11.2695419344519,30.9395289178023));
#79063=CARTESIAN_POINT('Ctrl Pts',(200.704383877456,11.3235268310191,30.9272920652798));
#79064=CARTESIAN_POINT('Ctrl Pts',(200.70138208355,11.3774801691792,30.9150623661576));
#79065=CARTESIAN_POINT('Ctrl Pts',(200.698380289645,11.4307733856348,30.8997614075139));
#79066=CARTESIAN_POINT('Ctrl Pts',(200.695378495739,11.4830372892332,30.8814873243031));
#79067=CARTESIAN_POINT('Ctrl Pts',(200.692377275006,11.5352912133859,30.8632167304073));
#79068=CARTESIAN_POINT('Ctrl Pts',(200.689376054274,11.5865157175064,30.8419743135672));
#79069=CARTESIAN_POINT('Ctrl Pts',(200.686374833541,11.6363583325243,30.8179075546588));
#79070=CARTESIAN_POINT('Ctrl Pts',(200.6833708689,11.68624651685,30.7938187923797));
#79071=CARTESIAN_POINT('Ctrl Pts',(200.680366904259,11.7347498122671,30.7669007594579));
#79072=CARTESIAN_POINT('Ctrl Pts',(200.677362939618,11.7815386380886,30.7373478117226));
#79073=CARTESIAN_POINT('Ctrl Pts',(200.674357590444,11.8283490289786,30.7077812429713));
#79074=CARTESIAN_POINT('Ctrl Pts',(200.671352241269,11.8734429452229,30.675577645609));
#79075=CARTESIAN_POINT('Ctrl Pts',(200.668346892095,11.9165209534788,30.6409739663263));
#79076=CARTESIAN_POINT('Ctrl Pts',(200.665335970228,11.9596788394731,30.6063061228969));
#79077=CARTESIAN_POINT('Ctrl Pts',(200.662325048361,12.0008129582586,30.5692296618826));
#79078=CARTESIAN_POINT('Ctrl Pts',(200.659314126494,12.039658954378,30.5300201495998));
#79079=CARTESIAN_POINT('Ctrl Pts',(200.657141907114,12.0676842666655,30.5017325798079));
#79080=CARTESIAN_POINT('Ctrl Pts',(200.654969687734,12.0945194053748,30.4723355917197));
#79081=CARTESIAN_POINT('Ctrl Pts',(200.652797468355,12.1200784829496,30.4419429080541));
#79082=CARTESIAN_POINT('Ctrl Pts',(200.649785678974,12.1555162288508,30.3998033512626));
#79083=CARTESIAN_POINT('Ctrl Pts',(200.646773889593,12.1886460472905,30.3555738378347));
#79084=CARTESIAN_POINT('Ctrl Pts',(200.643762100212,12.2192136935125,30.3095370402592));
#79085=CARTESIAN_POINT('Ctrl Pts',(200.640755609431,12.2497275624994,30.2635812345818));
#79086=CARTESIAN_POINT('Ctrl Pts',(200.637749118649,12.2776879155885,30.215824890738));
#79087=CARTESIAN_POINT('Ctrl Pts',(200.634742627868,12.3028810496936,30.1665832433757));
#79088=CARTESIAN_POINT('Ctrl Pts',(200.631739078152,12.3280495389001,30.1173897660983));
#79089=CARTESIAN_POINT('Ctrl Pts',(200.628735528436,12.3504559328577,30.0667143310579));
#79090=CARTESIAN_POINT('Ctrl Pts',(200.62573197872,12.3699311129871,30.0148990150214));
#79091=CARTESIAN_POINT('Ctrl Pts',(200.622730184815,12.3893949083458,29.9631139891021));
#79092=CARTESIAN_POINT('Ctrl Pts',(200.619728390909,12.4059307012672,29.9101908957679));
#79093=CARTESIAN_POINT('Ctrl Pts',(200.616726597004,12.4194173725723,29.8564920369937));
#79094=CARTESIAN_POINT('Ctrl Pts',(200.613725376271,12.432901468687,29.8028034316604));
#79095=CARTESIAN_POINT('Ctrl Pts',(200.610724155538,12.4433374712575,29.7483398663532));
#79096=CARTESIAN_POINT('Ctrl Pts',(200.607722934805,12.450654669387,29.6934768207966));
#79097=CARTESIAN_POINT('Ctrl Pts',(200.604718970164,12.4579785573673,29.6385636159337));
#79098=CARTESIAN_POINT('Ctrl Pts',(200.601715005523,12.4621778748553,29.583250725073));
#79099=CARTESIAN_POINT('Ctrl Pts',(200.598711040883,12.4632336474477,29.5279202968632));
#79100=CARTESIAN_POINT('Ctrl Pts',(200.595705691708,12.4642899066479,29.4725643667424));
#79101=CARTESIAN_POINT('Ctrl Pts',(200.592700342534,12.4621997527736,29.4171914110496));
#79102=CARTESIAN_POINT('Ctrl Pts',(200.589694993359,12.456996362954,29.3621818287057));
#79103=CARTESIAN_POINT('Ctrl Pts',(200.586684071492,12.4517833247075,29.3070702444078));
#79104=CARTESIAN_POINT('Ctrl Pts',(200.583673149625,12.443445599141,29.2523239018628));
#79105=CARTESIAN_POINT('Ctrl Pts',(200.580662227758,12.4320679104757,29.1983151482327));
#79106=CARTESIAN_POINT('Ctrl Pts',(200.578490008379,12.4238595155374,29.1593507159164));
#79107=CARTESIAN_POINT('Ctrl Pts',(200.576317788999,12.4140699539376,29.1207699945449));
#79108=CARTESIAN_POINT('Ctrl Pts',(200.57414556962,12.4027469562315,29.0827072648808));
#79109=CARTESIAN_POINT('Ctrl Pts',(200.571133780236,12.3870475823078,29.0299331637935));
#79110=CARTESIAN_POINT('Ctrl Pts',(200.568121990853,12.3683333412133,28.9779368955227));
#79111=CARTESIAN_POINT('Ctrl Pts',(200.565110201469,12.346700453166,28.9270862722516));
#79112=CARTESIAN_POINT('Ctrl Pts',(200.562103710685,12.3251056235578,28.8763251097748));
#79113=CARTESIAN_POINT('Ctrl Pts',(200.5590972199,12.3006025422001,28.8267060737916));
#79114=CARTESIAN_POINT('Ctrl Pts',(200.556090729116,12.2733369230014,28.7785810298299));
#79115=CARTESIAN_POINT('Ctrl Pts',(200.553087179397,12.2460979760864,28.7305030636483));
#79116=CARTESIAN_POINT('Ctrl Pts',(200.550083629678,12.2161021037954,28.6839166508456));
#79117=CARTESIAN_POINT('Ctrl Pts',(200.547080079959,12.1835419605243,28.6391511876768));
#79118=CARTESIAN_POINT('Ctrl Pts',(200.544078286051,12.1510008512114,28.5944118934331));
#79119=CARTESIAN_POINT('Ctrl Pts',(200.541076492142,12.1158987519287,28.5514918644598));
#79120=CARTESIAN_POINT('Ctrl Pts',(200.538074698234,12.078471609951,28.5106915362084));
#79121=CARTESIAN_POINT('Ctrl Pts',(200.535073477498,12.0410516144378,28.4698989985091));
#79122=CARTESIAN_POINT('Ctrl Pts',(200.532072256763,12.0013078143925,28.4312257460071));
#79123=CARTESIAN_POINT('Ctrl Pts',(200.529071036027,11.9595148894375,28.3949373651472));
#79124=CARTESIAN_POINT('Ctrl Pts',(200.526067071383,11.917683754717,28.3586158071283));
#79125=CARTESIAN_POINT('Ctrl Pts',(200.523063106739,11.8738001516277,28.324683822981));
#79126=CARTESIAN_POINT('Ctrl Pts',(200.520059142096,11.8281727870113,28.2933674607181));
#79127=CARTESIAN_POINT('Ctrl Pts',(200.517053792918,11.7825243926466,28.262036664678));
#79128=CARTESIAN_POINT('Ctrl Pts',(200.514048443741,11.7351310865055,28.2333241673284));
#79129=CARTESIAN_POINT('Ctrl Pts',(200.511043094564,11.6863288002742,28.2074115009354));
#79130=CARTESIAN_POINT('Ctrl Pts',(200.508032172694,11.6374360220179,28.1814507857758));
#79131=CARTESIAN_POINT('Ctrl Pts',(200.505021250824,11.5871295251715,28.1583004926788));
#79132=CARTESIAN_POINT('Ctrl Pts',(200.502010328954,11.5357668707768,28.1380946764998));
#79133=CARTESIAN_POINT('Ctrl Pts',(200.499838109598,11.4987114582219,28.1235172590485));
#79134=CARTESIAN_POINT('Ctrl Pts',(200.497665890242,11.4611067690704,28.1104713823924));
#79135=CARTESIAN_POINT('Ctrl Pts',(200.495493670886,11.4230911995218,28.0989910468212));
#79136=CARTESIAN_POINT('Ctrl Pts',(200.492481881509,11.3703824856468,28.0830735232907));
#79137=CARTESIAN_POINT('Ctrl Pts',(200.489470092133,11.3166650271965,28.0701016545677));
#79138=CARTESIAN_POINT('Ctrl Pts',(200.486458302756,11.2622989213193,28.0601974003792));
#79139=CARTESIAN_POINT('Ctrl Pts',(200.483451811979,11.2080284609759,28.0503105706073));
#79140=CARTESIAN_POINT('Ctrl Pts',(200.480445321201,11.1531121327064,28.0434807386608));
#79141=CARTESIAN_POINT('Ctrl Pts',(200.477438830424,11.0979239402719,28.0397797591043));
#79142=CARTESIAN_POINT('Ctrl Pts',(200.474435280712,11.0427897350623,28.0360823999891));
#79143=CARTESIAN_POINT('Ctrl Pts',(200.471431731,10.9873847162564,28.0355078647442));
#79144=CARTESIAN_POINT('Ctrl Pts',(200.468428181288,10.9320899425985,28.0380764472437));
#79145=CARTESIAN_POINT('Ctrl Pts',(200.465426387386,10.876827493073,28.0406435282051));
#79146=CARTESIAN_POINT('Ctrl Pts',(200.462424593485,10.821675686762,28.0463500603523));
#79147=CARTESIAN_POINT('Ctrl Pts',(200.459422799583,10.7670152097446,28.0551642524115));
#79148=CARTESIAN_POINT('Ctrl Pts',(200.456421578855,10.712365169782,28.0639767614592));
#79149=CARTESIAN_POINT('Ctrl Pts',(200.453420358126,10.6582067931507,28.0758956678317));
#79150=CARTESIAN_POINT('Ctrl Pts',(200.450419137397,10.6049129673173,28.0908376649207));
#79151=CARTESIAN_POINT('Ctrl Pts',(200.44741517276,10.551570416857,28.10579332294));
#79152=CARTESIAN_POINT('Ctrl Pts',(200.444411208123,10.4990945050881,28.1237774503732));
#79153=CARTESIAN_POINT('Ctrl Pts',(200.441407243486,10.4478438165162,28.1446565752398));
#79154=CARTESIAN_POINT('Ctrl Pts',(200.438401894315,10.3965695063931,28.1655453233395));
#79155=CARTESIAN_POINT('Ctrl Pts',(200.435396545144,10.3465220222501,28.189331501865));
#79156=CARTESIAN_POINT('Ctrl Pts',(200.432391195974,10.2980377472623,28.2158344165446));
#79157=CARTESIAN_POINT('Ctrl Pts',(200.42938027411,10.2494635699212,28.2423864744649));
#79158=CARTESIAN_POINT('Ctrl Pts',(200.426369352247,10.2024588402598,28.2716650514699));
#79159=CARTESIAN_POINT('Ctrl Pts',(200.423358430384,10.1573321889348,28.3034452748852));
#79160=CARTESIAN_POINT('Ctrl Pts',(200.421186210973,10.1247757187265,28.3263730097481));
#79161=CARTESIAN_POINT('Ctrl Pts',(200.419013991563,10.093196152973,28.3506018902364));
#79162=CARTESIAN_POINT('Ctrl Pts',(200.416841772152,10.0626980115527,28.3760350394907));
#79163=CARTESIAN_POINT('Ctrl Pts',(200.413870697636,10.0209838779215,28.4108214801473));
#79164=CARTESIAN_POINT('Ctrl Pts',(200.410899623119,9.98111135542615,28.4480149358457));
#79165=CARTESIAN_POINT('Ctrl Pts',(200.407928548603,9.94337598668605,28.4873905271585));
#79166=CARTESIAN_POINT('Ctrl Pts',(200.404961581688,9.90569278824966,28.5267116805096));
#79167=CARTESIAN_POINT('Ctrl Pts',(200.401994614774,9.87014126963611,28.568208612504));
#79168=CARTESIAN_POINT('Ctrl Pts',(200.399027647859,9.83698355660046,28.6116166354651));
#79169=CARTESIAN_POINT('Ctrl Pts',(200.396063538184,9.80385777500556,28.654982855763));
#79170=CARTESIAN_POINT('Ctrl Pts',(200.393099428508,9.77312156356463,28.7002560946092));
#79171=CARTESIAN_POINT('Ctrl Pts',(200.390135318833,9.74499809966876,28.7471371438536));
#79172=CARTESIAN_POINT('Ctrl Pts',(200.387172820682,9.71688992590959,28.7939927048559));
#79173=CARTESIAN_POINT('Ctrl Pts',(200.384210322531,9.69139196386493,28.8424538795948));
#79174=CARTESIAN_POINT('Ctrl Pts',(200.38124782438,9.66868376907831,28.8921930049066));
#79175=CARTESIAN_POINT('Ctrl Pts',(200.378283897527,9.64596462297552,28.9419561175451));
#79176=CARTESIAN_POINT('Ctrl Pts',(200.375319970673,9.62603816850224,28.9929979224341));
#79177=CARTESIAN_POINT('Ctrl Pts',(200.372356043819,9.60903685951709,29.0449683617396));
#79178=CARTESIAN_POINT('Ctrl Pts',(200.369391528461,9.592032174825,29.0969491200725));
#79179=CARTESIAN_POINT('Ctrl Pts',(200.366427013103,9.57795394172056,29.1498583572275));
#79180=CARTESIAN_POINT('Ctrl Pts',(200.363462497745,9.56688449072814,29.2033315199007));
#79181=CARTESIAN_POINT('Ctrl Pts',(200.36049322523,9.55579727659043,29.2568904909449));
#79182=CARTESIAN_POINT('Ctrl Pts',(200.357523952715,9.54772857477361,29.3110146575876));
#79183=CARTESIAN_POINT('Ctrl Pts',(200.354554680199,9.54270915193531,29.3653313913828));
#79184=CARTESIAN_POINT('Ctrl Pts',(200.352088135425,9.53853956793558,29.410451755107));
#79185=CARTESIAN_POINT('Ctrl Pts',(200.349621590651,9.53647317822599,29.4557047370735));
#79186=CARTESIAN_POINT('Ctrl Pts',(200.347155045877,9.53650026306434,29.5008774903221));
#79187=CARTESIAN_POINT('',(199.847155045885,9.53650055522948,29.4987251837867));
#79188=CARTESIAN_POINT('Ctrl Pts',(200.347155045843,9.53650026306472,29.5008774909522));
#79189=CARTESIAN_POINT('Ctrl Pts',(200.344166655035,9.53653307825662,29.5556074281586));
#79190=CARTESIAN_POINT('Ctrl Pts',(200.341178264226,9.53963588953091,29.6102432280142));
#79191=CARTESIAN_POINT('Ctrl Pts',(200.338189873417,9.54577770069793,29.6645288856481));
#79192=CARTESIAN_POINT('Ctrl Pts',(200.335178084014,9.55196760120643,29.7192395907894));
#79193=CARTESIAN_POINT('Ctrl Pts',(200.332166294612,9.56126210323049,29.7737138691559));
#79194=CARTESIAN_POINT('Ctrl Pts',(200.329154505209,9.57363105838014,29.827572728386));
#79195=CARTESIAN_POINT('Ctrl Pts',(200.326148014405,9.58597825299936,29.8813368344755));
#79196=CARTESIAN_POINT('Ctrl Pts',(200.323141523602,9.60138904926402,29.9344871601829));
#79197=CARTESIAN_POINT('Ctrl Pts',(200.320135032799,9.61978177411941,29.986651722433));
#79198=CARTESIAN_POINT('Ctrl Pts',(200.317131483061,9.63815650649988,30.0387652552906));
#79199=CARTESIAN_POINT('Ctrl Pts',(200.314127933323,9.65950721403042,30.0898944400664));
#79200=CARTESIAN_POINT('Ctrl Pts',(200.311124383585,9.68370206735094,30.1396811725413));
#79201=CARTESIAN_POINT('Ctrl Pts',(200.308122589658,9.70788277688154,30.1894388007652));
#79202=CARTESIAN_POINT('Ctrl Pts',(200.305120795731,9.73490410643084,30.2378550588371));
#79203=CARTESIAN_POINT('Ctrl Pts',(200.302119001804,9.76458652155721,30.2845927525041));
#79204=CARTESIAN_POINT('Ctrl Pts',(200.29911778105,9.79426326902277,30.3313215219176));
#79205=CARTESIAN_POINT('Ctrl Pts',(200.296116560295,9.826599810181,30.3763719186109));
#79206=CARTESIAN_POINT('Ctrl Pts',(200.293115339541,9.86137236140119,30.419434255735));
#79207=CARTESIAN_POINT('Ctrl Pts',(200.290111374879,9.89617670390919,30.4625359631987));
#79208=CARTESIAN_POINT('Ctrl Pts',(200.287107410217,9.93342117357896,30.5036455689202));
#79209=CARTESIAN_POINT('Ctrl Pts',(200.284103445555,9.97284154630521,30.5424863361231));
#79210=CARTESIAN_POINT('Ctrl Pts',(200.281098096359,10.0122800879627,30.5813450051158));
#79211=CARTESIAN_POINT('Ctrl Pts',(200.278092747164,10.0538961350287,30.6179324023142));
#79212=CARTESIAN_POINT('Ctrl Pts',(200.275087397968,10.0973908457618,30.6520108353159));
#79213=CARTESIAN_POINT('Ctrl Pts',(200.272076476081,10.1409662068999,30.6861524585167));
#79214=CARTESIAN_POINT('Ctrl Pts',(200.269065554193,10.1864267560934,30.7177755228739));
#79215=CARTESIAN_POINT('Ctrl Pts',(200.266054632305,10.2334440225545,30.7466852784254));
#79216=CARTESIAN_POINT('Ctrl Pts',(200.263882413099,10.2673644672104,30.7675421218153));
#79217=CARTESIAN_POINT('Ctrl Pts',(200.261710193892,10.3020945507117,30.7869876515616));
#79218=CARTESIAN_POINT('Ctrl Pts',(200.259537974685,10.3375039961018,30.8049640971379));
#79219=CARTESIAN_POINT('Ctrl Pts',(200.256526185348,10.3865993128694,30.829888500223));
#79220=CARTESIAN_POINT('Ctrl Pts',(200.253514396011,10.4372048771768,30.8520901106701));
#79221=CARTESIAN_POINT('Ctrl Pts',(200.250502606675,10.4889875979802,30.8713856405045));
#79222=CARTESIAN_POINT('Ctrl Pts',(200.247496115937,10.5406792181654,30.8906472239825));
#79223=CARTESIAN_POINT('Ctrl Pts',(200.244489625199,10.5935433945327,30.9070126906442));
#79224=CARTESIAN_POINT('Ctrl Pts',(200.241483134461,10.6472245484176,30.9203456377801));
#79225=CARTESIAN_POINT('Ctrl Pts',(200.238479584788,10.7008531893231,30.9336655421118));
#79226=CARTESIAN_POINT('Ctrl Pts',(200.235476035116,10.755296715062,30.9439586773447));
#79227=CARTESIAN_POINT('Ctrl Pts',(200.232472485443,10.8101835490024,30.9511381619028));
#79228=CARTESIAN_POINT('Ctrl Pts',(200.229470691581,10.8650382972867,30.9583134494895));
#79229=CARTESIAN_POINT('Ctrl Pts',(200.226468897718,10.9203353181472,30.9623786261168));
#79230=CARTESIAN_POINT('Ctrl Pts',(200.223467103856,10.9756942571773,30.9632981517332));
#79231=CARTESIAN_POINT('Ctrl Pts',(200.220465883166,11.0310426257912,30.9642175017724));
#79232=CARTESIAN_POINT('Ctrl Pts',(200.217464662476,11.0864523620517,30.961992385128));
#79233=CARTESIAN_POINT('Ctrl Pts',(200.214463441785,11.1415417444191,30.9566393460932));
#79234=CARTESIAN_POINT('Ctrl Pts',(200.211459477186,11.1966814930408,30.951281412966));
#79235=CARTESIAN_POINT('Ctrl Pts',(200.208455512587,11.2514997766515,30.9427898957246));
#79236=CARTESIAN_POINT('Ctrl Pts',(200.205451547988,11.3056201469078,30.9312332359906));
#79237=CARTESIAN_POINT('Ctrl Pts',(200.202446198855,11.3597654613646,30.919671249766));
#79238=CARTESIAN_POINT('Ctrl Pts',(200.199440849722,11.4132117117433,30.9050414444456));
#79239=CARTESIAN_POINT('Ctrl Pts',(200.196435500589,11.4655960152989,30.8874626483397));
#79240=CARTESIAN_POINT('Ctrl Pts',(200.193424578762,11.5180774528864,30.8698512566045));
#79241=CARTESIAN_POINT('Ctrl Pts',(200.190413656936,11.5694925196308,30.8492801478071));
#79242=CARTESIAN_POINT('Ctrl Pts',(200.187402735109,11.6194978977645,30.8259165149682));
#79243=CARTESIAN_POINT('Ctrl Pts',(200.185230515389,11.6555741145356,30.8090608983462));
#79244=CARTESIAN_POINT('Ctrl Pts',(200.183058295669,11.6909170448264,30.7907528304533));
#79245=CARTESIAN_POINT('Ctrl Pts',(200.180886075948,11.7254067834574,30.7710693326935));
#79246=CARTESIAN_POINT('Ctrl Pts',(200.177874286558,11.7732269132098,30.7437781019039));
#79247=CARTESIAN_POINT('Ctrl Pts',(200.174862497168,11.819603873189,30.7137279385383));
#79248=CARTESIAN_POINT('Ctrl Pts',(200.171850707778,11.8642013764692,30.6810961988377));
#79249=CARTESIAN_POINT('Ctrl Pts',(200.168844216988,11.9087204199704,30.6485218677115));
#79250=CARTESIAN_POINT('Ctrl Pts',(200.165837726198,11.9514657974227,30.6133752827255));
#79251=CARTESIAN_POINT('Ctrl Pts',(200.162831235409,11.9921280078101,30.5758783695747));
#79252=CARTESIAN_POINT('Ctrl Pts',(200.159827685685,12.0327504408434,30.5384181373613));
#79253=CARTESIAN_POINT('Ctrl Pts',(200.156824135961,12.0712933580795,30.4986124876854));
#79254=CARTESIAN_POINT('Ctrl Pts',(200.153820586237,12.1074798153552,30.4567239458594));
#79255=CARTESIAN_POINT('Ctrl Pts',(200.150818792324,12.1436451188019,30.4148598911791));
#79256=CARTESIAN_POINT('Ctrl Pts',(200.147816998411,12.177456348763,30.3709157562617));
#79257=CARTESIAN_POINT('Ctrl Pts',(200.144815204499,12.2086746096786,30.325189637549));
#79258=CARTESIAN_POINT('Ctrl Pts',(200.141813983759,12.2398869096691,30.2794722499431));
#79259=CARTESIAN_POINT('Ctrl Pts',(200.138812763019,12.2685069268659,30.2319739897437));
#79260=CARTESIAN_POINT('Ctrl Pts',(200.13581154228,12.294338510907,30.1830227442648));
#79261=CARTESIAN_POINT('Ctrl Pts',(200.132807577633,12.3201937118279,30.1340267444388));
#79262=CARTESIAN_POINT('Ctrl Pts',(200.129803612986,12.3432551401478,30.0835755730157));
#79263=CARTESIAN_POINT('Ctrl Pts',(200.126799648339,12.3633728870516,30.0320212597751));
#79264=CARTESIAN_POINT('Ctrl Pts',(200.123794299159,12.3834999062642,29.9804431850506));
#79265=CARTESIAN_POINT('Ctrl Pts',(200.120788949979,12.4006803757923,29.9277614572397));
#79266=CARTESIAN_POINT('Ctrl Pts',(200.117783600799,12.4148139280457,29.8743444924237));
#79267=CARTESIAN_POINT('Ctrl Pts',(200.114772678927,12.4289736875466,29.8208284787914));
#79268=CARTESIAN_POINT('Ctrl Pts',(200.111761757055,12.4400751384979,29.766575022768));
#79269=CARTESIAN_POINT('Ctrl Pts',(200.108750835183,12.4480690658949,29.7119628042802));
#79270=CARTESIAN_POINT('Ctrl Pts',(200.106578615861,12.4538362575707,29.6725630053804));
#79271=CARTESIAN_POINT('Ctrl Pts',(200.104406396538,12.4579871180878,29.6329766711804));
#79272=CARTESIAN_POINT('Ctrl Pts',(200.102234177215,12.4605200161449,29.5933463038373));
#79273=CARTESIAN_POINT('Ctrl Pts',(200.099222387664,12.4640318879998,29.5383986634128));
#79274=CARTESIAN_POINT('Ctrl Pts',(200.096210598113,12.4644458728765,29.483138698796));
#79275=CARTESIAN_POINT('Ctrl Pts',(200.093198808562,12.4617251107476,29.4279448085845));
#79276=CARTESIAN_POINT('Ctrl Pts',(200.09019231761,12.4590091352167,29.3728480201968));
#79277=CARTESIAN_POINT('Ctrl Pts',(200.087185826657,12.4531693833186,29.3178175981223));
#79278=CARTESIAN_POINT('Ctrl Pts',(200.084179335705,12.4442209499736,29.2632340867916));
#79279=CARTESIAN_POINT('Ctrl Pts',(200.081175785817,12.4352812703308,29.2087039711545));
#79280=CARTESIAN_POINT('Ctrl Pts',(200.07817223593,12.4232390187041,29.1546204181236));
#79281=CARTESIAN_POINT('Ctrl Pts',(200.075168686042,12.4081611039551,29.1013591148564));
#79282=CARTESIAN_POINT('Ctrl Pts',(200.072166891965,12.3930920034294,29.0481289469969));
#79283=CARTESIAN_POINT('Ctrl Pts',(200.069165097888,12.3749909007801,28.9957205825852));
#79284=CARTESIAN_POINT('Ctrl Pts',(200.066163303811,12.3539753401218,28.9444974992477));
#79285=CARTESIAN_POINT('Ctrl Pts',(200.063162082907,12.3329637922471,28.8932841966224));
#79286=CARTESIAN_POINT('Ctrl Pts',(200.060160862003,12.3090390918353,28.8432562131816));
#79287=CARTESIAN_POINT('Ctrl Pts',(200.057159641099,12.2823671743628,28.7947577153085));
#79288=CARTESIAN_POINT('Ctrl Pts',(200.054155676289,12.2556708717342,28.7462148770373));
#79289=CARTESIAN_POINT('Ctrl Pts',(200.051151711479,12.2262225892105,28.6992047808735));
#79290=CARTESIAN_POINT('Ctrl Pts',(200.048147746668,12.1942338596529,28.6540462551306));
#79291=CARTESIAN_POINT('Ctrl Pts',(200.045142397325,12.1622303864312,28.6088669157405));
#79292=CARTESIAN_POINT('Ctrl Pts',(200.042137047982,12.1276844615012,28.5655412609229));
#79293=CARTESIAN_POINT('Ctrl Pts',(200.039131698639,12.0908485527022,28.5243557589636));
#79294=CARTESIAN_POINT('Ctrl Pts',(200.036120776606,12.0539443406716,28.4830938885102));
#79295=CARTESIAN_POINT('Ctrl Pts',(200.033109854574,12.0147420371894,28.4439804710278));
#79296=CARTESIAN_POINT('Ctrl Pts',(200.030098932542,11.9735308183608,28.4072649014048));
#79297=CARTESIAN_POINT('Ctrl Pts',(200.027926714521,11.9437991444042,28.3807765961281));
#79298=CARTESIAN_POINT('Ctrl Pts',(200.025754496501,11.9130226230988,28.3555355316041));
#79299=CARTESIAN_POINT('Ctrl Pts',(200.023582278481,11.8813193647311,28.3316214537446));
#79300=CARTESIAN_POINT('Ctrl Pts',(200.020570489526,11.8373626704676,28.2984644893445));
#79301=CARTESIAN_POINT('Ctrl Pts',(200.017558700571,11.7914411441689,28.2677228671092));
#79302=CARTESIAN_POINT('Ctrl Pts',(200.014546911616,11.7438505227137,28.239635509125));
#79303=CARTESIAN_POINT('Ctrl Pts',(200.011540421258,11.6963436267639,28.2115975648314));
#79304=CARTESIAN_POINT('Ctrl Pts',(200.008533930901,11.6471739138674,28.1862048834493));
#79305=CARTESIAN_POINT('Ctrl Pts',(200.005527440544,11.5966674909243,28.163654178263));
#79306=CARTESIAN_POINT('Ctrl Pts',(200.002523891251,11.5462104753034,28.1411255330423));
#79307=CARTESIAN_POINT('Ctrl Pts',(199.999520341958,11.4944198194221,28.1214335703311));
#79308=CARTESIAN_POINT('Ctrl Pts',(199.996516792664,11.4416460741353,28.1047290602894));
#79309=CARTESIAN_POINT('Ctrl Pts',(199.99351499918,11.3889031792108,28.0880343153342));
#79310=CARTESIAN_POINT('Ctrl Pts',(199.990513205695,11.3351788358903,28.0743237201462));
#79311=CARTESIAN_POINT('Ctrl Pts',(199.98751141221,11.2808412505503,28.0636990419869));
#79312=CARTESIAN_POINT('Ctrl Pts',(199.984510191896,11.2265140405622,28.0530763925297));
#79313=CARTESIAN_POINT('Ctrl Pts',(199.981508971581,11.1715743384589,28.0455385908318));
#79314=CARTESIAN_POINT('Ctrl Pts',(199.978507751266,11.1164008410242,28.0411363688786));
#79315=CARTESIAN_POINT('Ctrl Pts',(199.975503787035,11.061176900301,28.0367301221206));
#79316=CARTESIAN_POINT('Ctrl Pts',(199.972499822805,11.0057192640682,28.0354652239802));
#79317=CARTESIAN_POINT('Ctrl Pts',(199.969495858574,10.9504105494985,28.0373403894279));
#79318=CARTESIAN_POINT('Ctrl Pts',(199.966490509807,10.8950763429549,28.0392164191457));
#79319=CARTESIAN_POINT('Ctrl Pts',(199.963485161039,10.8398917209894,28.0442353495187));
#79320=CARTESIAN_POINT('Ctrl Pts',(199.960479812271,10.7852347923406,28.0523439097703));
#79321=CARTESIAN_POINT('Ctrl Pts',(199.9574688908,10.7304765154372,28.0604675054155));
#79322=CARTESIAN_POINT('Ctrl Pts',(199.954457969329,10.6762484039289,28.0716920673509));
#79323=CARTESIAN_POINT('Ctrl Pts',(199.951447047857,10.6229177969303,28.0859132763058));
#79324=CARTESIAN_POINT('Ctrl Pts',(199.949274825154,10.5844425472703,28.0961731363712));
#79325=CARTESIAN_POINT('Ctrl Pts',(199.947102602451,10.5464341864154,28.1079916346583));
#79326=CARTESIAN_POINT('Ctrl Pts',(199.944930379747,10.5090242803149,28.1213139977936));
#79327=CARTESIAN_POINT('Ctrl Pts',(199.941918590125,10.4571553965352,28.1397854717205));
#79328=CARTESIAN_POINT('Ctrl Pts',(199.938906800503,10.4062228765033,28.1612264023683));
#79329=CARTESIAN_POINT('Ctrl Pts',(199.935895010881,10.3565889221947,28.1855212306935));
#79330=CARTESIAN_POINT('Ctrl Pts',(199.932888519866,10.3070422883209,28.2097733174117));
#79331=CARTESIAN_POINT('Ctrl Pts',(199.92988202885,10.2587901562201,28.2368691074569));
#79332=CARTESIAN_POINT('Ctrl Pts',(199.926875537834,10.2121761831416,28.2666444618073));
#79333=CARTESIAN_POINT('Ctrl Pts',(199.923871987889,10.1656078097211,28.2963906887118));
#79334=CARTESIAN_POINT('Ctrl Pts',(199.920868437943,10.1206748629444,28.3288110044335));
#79335=CARTESIAN_POINT('Ctrl Pts',(199.917864887998,10.0776960770454,28.3636955849322));
#79336=CARTESIAN_POINT('Ctrl Pts',(199.914863093868,10.0347424156859,28.3985597726021));
#79337=CARTESIAN_POINT('Ctrl Pts',(199.911861299737,9.99374105948417,28.4358850378109));
#79338=CARTESIAN_POINT('Ctrl Pts',(199.908859505607,9.95497953035692,28.4754198576846));
#79339=CARTESIAN_POINT('Ctrl Pts',(199.905858284654,9.91622540255326,28.5149471285787));
#79340=CARTESIAN_POINT('Ctrl Pts',(199.902857063702,9.87971062131992,28.5566827397039));
#79341=CARTESIAN_POINT('Ctrl Pts',(199.89985584275,9.84568585776882,28.6003383352365));
#79342=CARTESIAN_POINT('Ctrl Pts',(199.896851877899,9.81162998671388,28.644033843364));
#79343=CARTESIAN_POINT('Ctrl Pts',(199.893847913048,9.7800690059787,28.6896524256977));
#79344=CARTESIAN_POINT('Ctrl Pts',(199.890843948197,9.75121230213354,28.7368738402745));
#79345=CARTESIAN_POINT('Ctrl Pts',(199.887838598818,9.72234229822248,28.7841170192194));
#79346=CARTESIAN_POINT('Ctrl Pts',(199.884833249439,9.69617930514412,28.8329640373152));
#79347=CARTESIAN_POINT('Ctrl Pts',(199.881827900059,9.67288681474544,28.8830698228134));
#79348=CARTESIAN_POINT('Ctrl Pts',(199.878816977998,9.64955113414744,28.9332685171773));
#79349=CARTESIAN_POINT('Ctrl Pts',(199.875806055937,9.62909678334026,28.9847301500446));
#79350=CARTESIAN_POINT('Ctrl Pts',(199.872795133876,9.61163869818922,29.0370905643279));
#79351=CARTESIAN_POINT('Ctrl Pts',(199.870622916255,9.5990436328168,29.0748657747888));
#79352=CARTESIAN_POINT('Ctrl Pts',(199.868450698634,9.58800703906827,29.1131084034907));
#79353=CARTESIAN_POINT('Ctrl Pts',(199.866278481013,9.57855554213467,29.1516784485509));
#79354=CARTESIAN_POINT('Ctrl Pts',(199.862361330468,9.56151169900859,29.2212316422924));
#79355=CARTESIAN_POINT('Ctrl Pts',(199.858444179922,9.54956641122312,29.2920793217693));
#79356=CARTESIAN_POINT('Ctrl Pts',(199.854527029377,9.54287258404038,29.3635744024794));
#79357=CARTESIAN_POINT('Ctrl Pts',(199.852069701546,9.53867337657027,29.408425078901));
#79358=CARTESIAN_POINT('Ctrl Pts',(199.849612373716,9.53653992342768,29.4535301700919));
#79359=CARTESIAN_POINT('Ctrl Pts',(199.847155045885,9.53650055522948,29.4987251837867));
#79360=CARTESIAN_POINT('',(199.347155045813,9.53650017837068,29.5007225586097));
#79361=CARTESIAN_POINT('Ctrl Pts',(199.847155045843,9.53650055522881,29.4987251845542));
#79362=CARTESIAN_POINT('Ctrl Pts',(199.844186143803,9.53645299126435,29.5533290378456));
#79363=CARTESIAN_POINT('Ctrl Pts',(199.841217241763,9.53946564116368,29.6080119926478));
#79364=CARTESIAN_POINT('Ctrl Pts',(199.838248339723,9.54553843940391,29.6624001808755));
#79365=CARTESIAN_POINT('Ctrl Pts',(199.835281504372,9.5516070102936,29.7167505088075));
#79366=CARTESIAN_POINT('Ctrl Pts',(199.832314669022,9.56073145143656,29.7708059399479));
#79367=CARTESIAN_POINT('Ctrl Pts',(199.829347833672,9.57285971481966,29.8241957069663));
#79368=CARTESIAN_POINT('Ctrl Pts',(199.82638182629,9.58498459351303,29.8775705742591));
#79369=CARTESIAN_POINT('Ctrl Pts',(199.823415818908,9.60011151178393,29.9302796184272));
#79370=CARTESIAN_POINT('Ctrl Pts',(199.820449811525,9.61813743050191,29.9819627465066));
#79371=CARTESIAN_POINT('Ctrl Pts',(199.817481326748,9.63617840559801,30.0336890435767));
#79372=CARTESIAN_POINT('Ctrl Pts',(199.81451284197,9.65712304052316,30.0843872002799));
#79373=CARTESIAN_POINT('Ctrl Pts',(199.811544357193,9.68081908982352,30.1337144279768));
#79374=CARTESIAN_POINT('Ctrl Pts',(199.808574612818,9.70452519390792,30.183062586362));
#79375=CARTESIAN_POINT('Ctrl Pts',(199.805604868444,9.73098477598868,30.231038182389));
#79376=CARTESIAN_POINT('Ctrl Pts',(199.802635124069,9.75999987188039,30.2773235698622));
#79377=CARTESIAN_POINT('Ctrl Pts',(199.799659959631,9.78906792305384,30.3236934325253));
#79378=CARTESIAN_POINT('Ctrl Pts',(199.796684795194,9.82070048633078,30.3683664856554));
#79379=CARTESIAN_POINT('Ctrl Pts',(199.793709630756,9.85465740638949,30.4110557574932));
#79380=CARTESIAN_POINT('Ctrl Pts',(199.79168194793,9.87780028304774,30.4401500496453));
#79381=CARTESIAN_POINT('Ctrl Pts',(199.789654265105,9.90202194565885,30.468323574742));
#79382=CARTESIAN_POINT('Ctrl Pts',(199.787626582279,9.92723678838578,30.4954955257595));
#79383=CARTESIAN_POINT('Ctrl Pts',(199.784614796865,9.9646892412928,30.5358549373527));
#79384=CARTESIAN_POINT('Ctrl Pts',(199.781603011451,10.0045000661863,30.5741814986321));
#79385=CARTESIAN_POINT('Ctrl Pts',(199.778591226037,10.0464200685972,30.6101880761501));
#79386=CARTESIAN_POINT('Ctrl Pts',(199.775584739212,10.0882663217627,30.6461313078243));
#79387=CARTESIAN_POINT('Ctrl Pts',(199.772578252388,10.1322139913949,30.6797623149588));
#79388=CARTESIAN_POINT('Ctrl Pts',(199.769571765564,10.1779765740526,30.7108301851183));
#79389=CARTESIAN_POINT('Ctrl Pts',(199.766568219797,10.2236943900567,30.7418676635364));
#79390=CARTESIAN_POINT('Ctrl Pts',(199.763564674029,10.2712231675746,30.770346677451));
#79391=CARTESIAN_POINT('Ctrl Pts',(199.760561128262,10.3202442725791,30.7960572522225));
#79392=CARTESIAN_POINT('Ctrl Pts',(199.757559338289,10.3692367211233,30.821752797262));
#79393=CARTESIAN_POINT('Ctrl Pts',(199.754557548316,10.4197193017533,30.8446828666115));
#79394=CARTESIAN_POINT('Ctrl Pts',(199.751555758343,10.4713473956468,30.8646826275404));
#79395=CARTESIAN_POINT('Ctrl Pts',(199.74855454152,10.5229656318795,30.8846785697953));
#79396=CARTESIAN_POINT('Ctrl Pts',(199.745553324697,10.5757284554008,30.9017451245872));
#79397=CARTESIAN_POINT('Ctrl Pts',(199.742552107874,10.6292719595987,30.9157658599007));
#79398=CARTESIAN_POINT('Ctrl Pts',(199.739548147077,10.682864417938,30.9297994141932));
#79399=CARTESIAN_POINT('Ctrl Pts',(199.73654418628,10.7372384715601,30.9407814521049));
#79400=CARTESIAN_POINT('Ctrl Pts',(199.733540225482,10.7920172216692,30.9486460623347));
#79401=CARTESIAN_POINT('Ctrl Pts',(199.73053488012,10.8468212200212,30.9565142974663));
#79402=CARTESIAN_POINT('Ctrl Pts',(199.727529534758,10.9020297603562,30.961262195475));
#79403=CARTESIAN_POINT('Ctrl Pts',(199.724524189396,10.9572612551116,30.9628758148542));
#79404=CARTESIAN_POINT('Ctrl Pts',(199.721513271244,11.0125951652202,30.9644924263559));
#79405=CARTESIAN_POINT('Ctrl Pts',(199.718502353092,11.0679515864211,30.9629631647149));
#79406=CARTESIAN_POINT('Ctrl Pts',(199.71549143494,11.1229505708737,30.9583262348054));
#79407=CARTESIAN_POINT('Ctrl Pts',(199.713319184475,11.1626300186545,30.9549808854315));
#79408=CARTESIAN_POINT('Ctrl Pts',(199.711146934009,11.2021234776193,30.950019095071));
#79409=CARTESIAN_POINT('Ctrl Pts',(199.708974683544,11.2412918033836,30.9434716885412));
#79410=CARTESIAN_POINT('Ctrl Pts',(199.705962890636,11.2955981035294,30.9343938069303));
#79411=CARTESIAN_POINT('Ctrl Pts',(199.702951097727,11.3495039340656,30.9222281897881));
#79412=CARTESIAN_POINT('Ctrl Pts',(199.699939304819,11.4026324297627,30.9070250091961));
#79413=CARTESIAN_POINT('Ctrl Pts',(199.69693281057,11.4556674562733,30.8918485756239));
#79414=CARTESIAN_POINT('Ctrl Pts',(199.693926316322,11.5079273589684,30.8736453282288));
#79415=CARTESIAN_POINT('Ctrl Pts',(199.690919822074,11.5590450000732,30.8525165203771));
#79416=CARTESIAN_POINT('Ctrl Pts',(199.687916268931,11.6101126353031,30.8314083817994));
#79417=CARTESIAN_POINT('Ctrl Pts',(199.684912715788,11.6600397375717,30.8073805529998));
#79418=CARTESIAN_POINT('Ctrl Pts',(199.681909162645,11.7084756840184,30.7805836384847));
#79419=CARTESIAN_POINT('Ctrl Pts',(199.678907365358,11.7568833151515,30.7538023892573));
#79420=CARTESIAN_POINT('Ctrl Pts',(199.675905568071,11.8038010578136,30.7242555179317));
#79421=CARTESIAN_POINT('Ctrl Pts',(199.672903770784,11.8489016955114,30.6921401601145));
#79422=CARTESIAN_POINT('Ctrl Pts',(199.669902546721,11.8939937207795,30.6600309350546));
#79423=CARTESIAN_POINT('Ctrl Pts',(199.666901322659,11.9372689009615,30.625354503514));
#79424=CARTESIAN_POINT('Ctrl Pts',(199.663900098596,11.9784298311313,30.5883507318656));
#79425=CARTESIAN_POINT('Ctrl Pts',(199.66089613073,12.0196283917791,30.5513131303303));
#79426=CARTESIAN_POINT('Ctrl Pts',(199.657892162864,12.0587084480754,30.5119442915319));
#79427=CARTESIAN_POINT('Ctrl Pts',(199.654888194997,12.0954076400463,30.4705227210778));
#79428=CARTESIAN_POINT('Ctrl Pts',(199.651882842651,12.1321237460789,30.4290820600944));
#79429=CARTESIAN_POINT('Ctrl Pts',(199.648877490305,12.1664564731692,30.3855871962501));
#79430=CARTESIAN_POINT('Ctrl Pts',(199.645872137959,12.1981842837386,30.3403491370864));
#79431=CARTESIAN_POINT('Ctrl Pts',(199.642861213045,12.2299709244697,30.2950271968642));
#79432=CARTESIAN_POINT('Ctrl Pts',(199.639850288132,12.2591427222622,30.24795605421));
#79433=CARTESIAN_POINT('Ctrl Pts',(199.636839363218,12.2855225904214,30.1994740306232));
#79434=CARTESIAN_POINT('Ctrl Pts',(199.634667170415,12.3045540048185,30.1644973023045));
#79435=CARTESIAN_POINT('Ctrl Pts',(199.632494977613,12.322133253818,30.1287868103729));
#79436=CARTESIAN_POINT('Ctrl Pts',(199.63032278481,12.3382095470459,30.0924757026201));
#79437=CARTESIAN_POINT('Ctrl Pts',(199.627310986406,12.3604997204729,30.0421294643636));
#79438=CARTESIAN_POINT('Ctrl Pts',(199.624299188002,12.3799909399452,29.9904192511729));
#79439=CARTESIAN_POINT('Ctrl Pts',(199.621287389598,12.396517810639,29.937687393659));
#79440=CARTESIAN_POINT('Ctrl Pts',(199.618280889694,12.4130156064681,29.8850483045616));
#79441=CARTESIAN_POINT('Ctrl Pts',(199.615274389791,12.4265592467518,29.8313916373946));
#79442=CARTESIAN_POINT('Ctrl Pts',(199.612267889887,12.4370313468767,29.7770796962855));
#79443=CARTESIAN_POINT('Ctrl Pts',(199.609264330996,12.4474932030038,29.7228208841));
#79444=CARTESIAN_POINT('Ctrl Pts',(199.606260772105,12.4548893720455,29.6679085832335));
#79445=CARTESIAN_POINT('Ctrl Pts',(199.603257213214,12.4591527681321,29.612718451251));
#79446=CARTESIAN_POINT('Ctrl Pts',(199.600255410097,12.4634136719876,29.5575605814743));
#79447=CARTESIAN_POINT('Ctrl Pts',(199.597253606981,12.4645453924085,29.5021257273295));
#79448=CARTESIAN_POINT('Ctrl Pts',(199.594251803864,12.4625325777978,29.4467955934154));
#79449=CARTESIAN_POINT('Ctrl Pts',(199.591250573902,12.4605201475071,29.3914760240481));
#79450=CARTESIAN_POINT('Ctrl Pts',(199.58824934394,12.4553643939643,29.3362616619538));
#79451=CARTESIAN_POINT('Ctrl Pts',(199.585248113977,12.4471020492454,29.2815328192389));
#79452=CARTESIAN_POINT('Ctrl Pts',(199.582244140153,12.4388321507116,29.226753940903));
#79453=CARTESIAN_POINT('Ctrl Pts',(199.579240166328,12.42745006613,29.1724619912569));
#79454=CARTESIAN_POINT('Ctrl Pts',(199.576236192504,12.4130440729133,29.1190292688346));
#79455=CARTESIAN_POINT('Ctrl Pts',(199.573230834157,12.3986314400218,29.065571919447));
#79456=CARTESIAN_POINT('Ctrl Pts',(199.570225475811,12.3811922865884,29.0129750881006));
#79457=CARTESIAN_POINT('Ctrl Pts',(199.567220117465,12.3608644878099,28.9615948590347));
#79458=CARTESIAN_POINT('Ctrl Pts',(199.564209186559,12.3404989970635,28.9101193603352));
#79459=CARTESIAN_POINT('Ctrl Pts',(199.561198255653,12.3172343842009,28.8598654495474));
#79460=CARTESIAN_POINT('Ctrl Pts',(199.558187324747,12.2912557854271,28.8111671127182));
#79461=CARTESIAN_POINT('Ctrl Pts',(199.556015178524,12.2725143008195,28.7760351512892));
#79462=CARTESIAN_POINT('Ctrl Pts',(199.5538430323,12.2523613224879,28.7417122946265));
#79463=CARTESIAN_POINT('Ctrl Pts',(199.551670886076,12.2308801030755,28.7083141899384));
#79464=CARTESIAN_POINT('Ctrl Pts',(199.548659132467,12.2010956717236,28.6620065973725));
#79465=CARTESIAN_POINT('Ctrl Pts',(199.545647378858,12.1686326388749,28.6172861704565));
#79466=CARTESIAN_POINT('Ctrl Pts',(199.542635625249,12.1336859088169,28.5744793302416));
#79467=CARTESIAN_POINT('Ctrl Pts',(199.539629170203,12.0988006603654,28.5317477998855));
#79468=CARTESIAN_POINT('Ctrl Pts',(199.536622715157,12.0614407174041,28.4909235803021));
#79469=CARTESIAN_POINT('Ctrl Pts',(199.533616260111,12.0218440733813,28.4523039850723));
#79470=CARTESIAN_POINT('Ctrl Pts',(199.53061274608,11.9822861641207,28.4137221688227));
#79471=CARTESIAN_POINT('Ctrl Pts',(199.527609232049,11.9404962642052,28.3773410709358));
#79472=CARTESIAN_POINT('Ctrl Pts',(199.524605718018,11.8967511863767,28.3434233446364));
#79473=CARTESIAN_POINT('Ctrl Pts',(199.521603959683,11.8530316796125,28.3095254448502));
#79474=CARTESIAN_POINT('Ctrl Pts',(199.518602201348,11.8073596764035,28.2780883848852));
#79475=CARTESIAN_POINT('Ctrl Pts',(199.515600443013,11.7600454964975,28.2493349396206));
#79476=CARTESIAN_POINT('Ctrl Pts',(199.512599257672,11.7127403482125,28.22058698299));
#79477=CARTESIAN_POINT('Ctrl Pts',(199.509598072331,11.6637940963546,28.1945218972784));
#79478=CARTESIAN_POINT('Ctrl Pts',(199.50659688699,11.6135445467326,28.1713181949109));
#79479=CARTESIAN_POINT('Ctrl Pts',(199.503592957185,11.5632490459227,28.1480932736929));
#79480=CARTESIAN_POINT('Ctrl Pts',(199.500589027381,11.5116483463261,28.1277351845344));
#79481=CARTESIAN_POINT('Ctrl Pts',(199.497585097577,11.4591019141554,28.1103749849622));
#79482=CARTESIAN_POINT('Ctrl Pts',(199.494579782981,11.4065312584276,28.093006782453));
#79483=CARTESIAN_POINT('Ctrl Pts',(199.491574468385,11.3530145112847,28.0786393613286));
#79484=CARTESIAN_POINT('Ctrl Pts',(199.48856915379,11.2989248790498,28.067353439719));
#79485=CARTESIAN_POINT('Ctrl Pts',(199.48555826566,11.2447349343855,28.0560465876987));
#79486=CARTESIAN_POINT('Ctrl Pts',(199.48254737753,11.1899705051224,28.0478327288488));
#79487=CARTESIAN_POINT('Ctrl Pts',(199.4795364894,11.1350123385002,28.0427409569837));
#79488=CARTESIAN_POINT('Ctrl Pts',(199.477363988714,11.0953573763999,28.0390669985396));
#79489=CARTESIAN_POINT('Ctrl Pts',(199.475191488028,11.0556016858806,28.0370173999341));
#79490=CARTESIAN_POINT('Ctrl Pts',(199.473018987342,11.0158877126441,28.0365862408099));
#79491=CARTESIAN_POINT('Ctrl Pts',(199.47000715515,10.9608305042163,28.0359885061631));
#79492=CARTESIAN_POINT('Ctrl Pts',(199.466995322958,10.9056254374112,28.0385009286239));
#79493=CARTESIAN_POINT('Ctrl Pts',(199.463983490766,10.8506523401595,28.0441402792507));
#79494=CARTESIAN_POINT('Ctrl Pts',(199.46097695768,10.7957759642054,28.0497697078368));
#79495=CARTESIAN_POINT('Ctrl Pts',(199.457970424595,10.7411312683149,28.0585150927121));
#79496=CARTESIAN_POINT('Ctrl Pts',(199.45496389151,10.6870974719425,28.0703412092617));
#79497=CARTESIAN_POINT('Ctrl Pts',(199.451960299834,10.6331165389569,28.0821557558567));
#79498=CARTESIAN_POINT('Ctrl Pts',(199.448956708158,10.5797458341841,28.0970449509043));
#79499=CARTESIAN_POINT('Ctrl Pts',(199.445953116483,10.5273569830918,28.114922085741));
#79500=CARTESIAN_POINT('Ctrl Pts',(199.442951281033,10.4749987642145,28.1327887676622));
#79501=CARTESIAN_POINT('Ctrl Pts',(199.439949445583,10.423621759186,28.1536397562874));
#79502=CARTESIAN_POINT('Ctrl Pts',(199.436947610133,10.3735827201601,28.1773384251752));
#79503=CARTESIAN_POINT('Ctrl Pts',(199.433946348344,10.3235532437556,28.2010325651711));
#79504=CARTESIAN_POINT('Ctrl Pts',(199.430945086555,10.2748617018364,28.2275730788476));
#79505=CARTESIAN_POINT('Ctrl Pts',(199.427943824765,10.2278430004879,28.2567760386381));
#79506=CARTESIAN_POINT('Ctrl Pts',(199.424939820138,10.1807813289851,28.2860056868664));
#79507=CARTESIAN_POINT('Ctrl Pts',(199.421935815511,10.1353960010385,28.3179023631074));
#79508=CARTESIAN_POINT('Ctrl Pts',(199.418931810884,10.0919942062385,28.352237947789));
#79509=CARTESIAN_POINT('Ctrl Pts',(199.41592642226,10.0485724154928,28.386589351459));
#79510=CARTESIAN_POINT('Ctrl Pts',(199.412921033637,10.0071363745303,28.4233815526671));
#79511=CARTESIAN_POINT('Ctrl Pts',(199.409915645013,9.96795879150149,28.4623472671645));
#79512=CARTESIAN_POINT('Ctrl Pts',(199.406904685046,9.92870858166622,28.5013852157097));
#79513=CARTESIAN_POINT('Ctrl Pts',(199.403893725079,9.89172554559009,28.5426043324622));
#79514=CARTESIAN_POINT('Ctrl Pts',(199.400882765112,9.85724342692036,28.5857026388077));
#79515=CARTESIAN_POINT('Ctrl Pts',(199.398710872944,9.83237048131507,28.6167906888106));
#79516=CARTESIAN_POINT('Ctrl Pts',(199.396538980776,9.80879796000743,28.6488557914288));
#79517=CARTESIAN_POINT('Ctrl Pts',(199.394367088608,9.78659921254147,28.6817758381745));
#79518=CARTESIAN_POINT('Ctrl Pts',(199.391312151604,9.75537492983388,28.7280804708081));
#79519=CARTESIAN_POINT('Ctrl Pts',(199.3882572146,9.72674340609812,28.7762658439025));
#79520=CARTESIAN_POINT('Ctrl Pts',(199.385202277597,9.70093225921005,28.8260153897611));
#79521=CARTESIAN_POINT('Ctrl Pts',(199.382031674951,9.67414385390876,28.8776485466989));
#79522=CARTESIAN_POINT('Ctrl Pts',(199.378861072304,9.65039409250268,28.9309663124073));
#79523=CARTESIAN_POINT('Ctrl Pts',(199.375690469658,9.62988870897934,28.9855806183495));
#79524=CARTESIAN_POINT('Ctrl Pts',(199.372645582071,9.61019636820771,29.0380294556217));
#79525=CARTESIAN_POINT('Ctrl Pts',(199.369600694484,9.59349615832397,29.0916734209036));
#79526=CARTESIAN_POINT('Ctrl Pts',(199.366555806897,9.57992289330038,29.1461451412971));
#79527=CARTESIAN_POINT('Ctrl Pts',(199.36351361467,9.56636164344493,29.2005686428665));
#79528=CARTESIAN_POINT('Ctrl Pts',(199.360471422443,9.55592196783507,29.2558179546714));
#79529=CARTESIAN_POINT('Ctrl Pts',(199.357429230216,9.54868887481389,29.3115105628662));
#79530=CARTESIAN_POINT('Ctrl Pts',(199.354388673487,9.54145967034044,29.3671732304305));
#79531=CARTESIAN_POINT('Ctrl Pts',(199.351348116758,9.53743369000977,29.4232782185999));
#79532=CARTESIAN_POINT('Ctrl Pts',(199.348307560029,9.53664449786614,29.4794348747984));
#79533=CARTESIAN_POINT('Ctrl Pts',(199.347923388634,9.53654478420382,29.4865302138721));
#79534=CARTESIAN_POINT('Ctrl Pts',(199.347539217238,9.53649667484675,29.4936263721534));
#79535=CARTESIAN_POINT('Ctrl Pts',(199.347155045843,9.5365001783704,29.5007225580503));
#79536=CARTESIAN_POINT('Ctrl Pts',(199.347155045813,9.53650017837068,29.5007225586097));
#79537=CARTESIAN_POINT('Ctrl Pts',(199.343841136659,9.53653040021501,29.5619351207308));
#79538=CARTESIAN_POINT('Ctrl Pts',(199.340527227506,9.54040521676902,29.6230182051036));
#79539=CARTESIAN_POINT('Ctrl Pts',(199.337213318352,9.54805131113806,29.6835136368559));
#79540=CARTESIAN_POINT('Ctrl Pts',(199.333886785213,9.55572653249469,29.7442395195555));
#79541=CARTESIAN_POINT('Ctrl Pts',(199.330560252073,9.56720167272118,29.8043729560867));
#79542=CARTESIAN_POINT('Ctrl Pts',(199.327233718933,9.58235272736732,29.8634672755519));
#79543=CARTESIAN_POINT('Ctrl Pts',(199.323891681091,9.59757439985442,29.9228370288632));
#79544=CARTESIAN_POINT('Ctrl Pts',(199.320549643249,9.61650617573339,29.9811576601772));
#79545=CARTESIAN_POINT('Ctrl Pts',(199.317207605408,9.63897437045939,30.0379976633161));
#79546=CARTESIAN_POINT('Ctrl Pts',(199.316710133563,9.6423188251934,30.0464584595615));
#79547=CARTESIAN_POINT('Ctrl Pts',(199.316212661718,9.64574155335958,30.0548864924784));
#79548=CARTESIAN_POINT('Ctrl Pts',(199.315715189873,9.64924189529193,30.0632803853903));
#79549=CARTESIAN_POINT('Ctrl Pts',(199.312703713051,9.67043143337053,30.1140933393597));
#79550=CARTESIAN_POINT('Ctrl Pts',(199.309692236228,9.69453614823446,30.1638143929741));
#79551=CARTESIAN_POINT('Ctrl Pts',(199.306680759406,9.72142152962381,30.2120880177973));
#79552=CARTESIAN_POINT('Ctrl Pts',(199.303674581285,9.74825960611454,30.2602767050519));
#79553=CARTESIAN_POINT('Ctrl Pts',(199.300668403164,9.77786838474692,30.3070225605282));
#79554=CARTESIAN_POINT('Ctrl Pts',(199.297662225042,9.81006582268166,30.3519911405934));
#79555=CARTESIAN_POINT('Ctrl Pts',(199.2946589878,9.84223176256306,30.3969157288747));
#79556=CARTESIAN_POINT('Ctrl Pts',(199.291655750558,9.87698103919725,30.4400660593064));
#79557=CARTESIAN_POINT('Ctrl Pts',(199.288652513315,9.91408730586176,30.4811349910738));
#79558=CARTESIAN_POINT('Ctrl Pts',(199.285651031134,9.95117188799834,30.5221799225718));
#79559=CARTESIAN_POINT('Ctrl Pts',(199.282649548953,9.99061037690318,30.5611454757929));
#79560=CARTESIAN_POINT('Ctrl Pts',(199.279648066772,10.0321364360397,30.5977578838515));
#79561=CARTESIAN_POINT('Ctrl Pts',(199.276647156453,10.073654583366,30.63436331628));
#79562=CARTESIAN_POINT('Ctrl Pts',(199.273646246134,10.117259115408,30.6686161454159));
#79563=CARTESIAN_POINT('Ctrl Pts',(199.270645335815,10.1626488643213,30.7002813526743));
#79564=CARTESIAN_POINT('Ctrl Pts',(199.267641677108,10.2080801834855,30.7319755605471));
#79565=CARTESIAN_POINT('Ctrl Pts',(199.264638018402,10.2552995521394,30.7610771098658));
#79566=CARTESIAN_POINT('Ctrl Pts',(199.261634359696,10.3039761461935,30.7873938965726));
#79567=CARTESIAN_POINT('Ctrl Pts',(199.25862931441,10.3526752108257,30.8137228318987));
#79568=CARTESIAN_POINT('Ctrl Pts',(199.255624269125,10.4028323634365,30.8372642176464));
#79569=CARTESIAN_POINT('Ctrl Pts',(199.25261922384,10.4540944166606,30.8578730957195));
#79570=CARTESIAN_POINT('Ctrl Pts',(199.249608598822,10.5054516526525,30.8785202401111));
#79571=CARTESIAN_POINT('Ctrl Pts',(199.246597973805,10.5579173862867,30.8962238314625));
#79572=CARTESIAN_POINT('Ctrl Pts',(199.243587348787,10.6111219443893,30.9108884108477));
#79573=CARTESIAN_POINT('Ctrl Pts',(199.241412662904,10.6495535659721,30.9214811793191));
#79574=CARTESIAN_POINT('Ctrl Pts',(199.239237977022,10.6883703561137,30.930489336424));
#79575=CARTESIAN_POINT('Ctrl Pts',(199.237063291139,10.7274305992426,30.9378936580188));
#79576=CARTESIAN_POINT('Ctrl Pts',(199.234051030188,10.7815348016252,30.9481497363732));
#79577=CARTESIAN_POINT('Ctrl Pts',(199.231038769237,10.8363306405577,30.9553690988392));
#79578=CARTESIAN_POINT('Ctrl Pts',(199.228026508286,10.8914470393717,30.9594685692878));
#79579=CARTESIAN_POINT('Ctrl Pts',(199.225019550016,10.9464664131636,30.9635608231689));
#79580=CARTESIAN_POINT('Ctrl Pts',(199.222012591746,11.0018047052847,30.9645440460637));
#79581=CARTESIAN_POINT('Ctrl Pts',(199.219005633476,11.0570823156062,30.9623863577198));
#79582=CARTESIAN_POINT('Ctrl Pts',(199.21600161914,11.1123058068991,30.9602307818406));
#79583=CARTESIAN_POINT('Ctrl Pts',(199.212997604805,11.1674682097885,30.9549404072662));
#79584=CARTESIAN_POINT('Ctrl Pts',(199.209993590469,11.2221883647312,30.9465353713539));
#79585=CARTESIAN_POINT('Ctrl Pts',(199.20699133562,11.2768764694288,30.9381352583711));
#79586=CARTESIAN_POINT('Ctrl Pts',(199.203989080772,11.3311223195393,30.9266241801385));
#79587=CARTESIAN_POINT('Ctrl Pts',(199.200986825923,11.3845506351572,30.9120740274505));
#79588=CARTESIAN_POINT('Ctrl Pts',(199.197985148735,11.4379686706961,30.8975266743401));
#79589=CARTESIAN_POINT('Ctrl Pts',(199.194983471546,11.4905689757804,30.8799415467321));
#79590=CARTESIAN_POINT('Ctrl Pts',(199.191981794358,11.5419894718377,30.8594409374508));
#79591=CARTESIAN_POINT('Ctrl Pts',(199.188977383739,11.5934567931637,30.838921659611));
#79592=CARTESIAN_POINT('Ctrl Pts',(199.185972973121,11.6437416684417,30.8154817920101));
#79593=CARTESIAN_POINT('Ctrl Pts',(199.182968562502,11.6925015450675,30.7892919995405));
#79594=CARTESIAN_POINT('Ctrl Pts',(199.179962772536,11.7412838077147,30.7630901831427));
#79595=CARTESIAN_POINT('Ctrl Pts',(199.17695698257,11.7885392257408,30.7341362010396));
#79596=CARTESIAN_POINT('Ctrl Pts',(199.173951192604,11.8339523114518,30.70264533102));
#79597=CARTESIAN_POINT('Ctrl Pts',(199.170939843705,11.8794493845107,30.6710962215169));
#79598=CARTESIAN_POINT('Ctrl Pts',(199.167928494806,11.9230969029341,30.6370011776122));
#79599=CARTESIAN_POINT('Ctrl Pts',(199.164917145906,11.9646116428316,30.6006164765775));
#79600=CARTESIAN_POINT('Ctrl Pts',(199.162748561406,11.9945079532505,30.5744144982121));
#79601=CARTESIAN_POINT('Ctrl Pts',(199.160579976905,12.0232989123031,30.5470259635572));
#79602=CARTESIAN_POINT('Ctrl Pts',(199.158411392405,12.0508912880956,30.5185576815305));
#79603=CARTESIAN_POINT('Ctrl Pts',(199.155399333181,12.0892157665761,30.4790166115585));
#79604=CARTESIAN_POINT('Ctrl Pts',(199.152387273957,12.1253847074543,30.4372277818558));
#79605=CARTESIAN_POINT('Ctrl Pts',(199.149375214733,12.1591245791634,30.3934553486208));
#79606=CARTESIAN_POINT('Ctrl Pts',(199.146368444345,12.1928052074713,30.3497597748313));
#79607=CARTESIAN_POINT('Ctrl Pts',(199.143361673956,12.2240649119281,30.3040879241949));
#79608=CARTESIAN_POINT('Ctrl Pts',(199.140354903568,12.2526683148564,30.2567392833432));
#79609=CARTESIAN_POINT('Ctrl Pts',(199.137351068508,12.2812437940074,30.2094368661141));
#79610=CARTESIAN_POINT('Ctrl Pts',(199.134347233448,12.3071678376621,30.1604613508079));
#79611=CARTESIAN_POINT('Ctrl Pts',(199.131343398389,12.3302476565136,30.1101421329003));
#79612=CARTESIAN_POINT('Ctrl Pts',(199.128341313988,12.3533140242571,30.0598522414463));
#79613=CARTESIAN_POINT('Ctrl Pts',(199.125339229588,12.3735392336328,30.0082206780741));
#79614=CARTESIAN_POINT('Ctrl Pts',(199.122337145188,12.3907769542751,29.955600387903));
#79615=CARTESIAN_POINT('Ctrl Pts',(199.11933562939,12.4080114100561,29.9029900641277));
#79616=CARTESIAN_POINT('Ctrl Pts',(199.116334113591,12.4222593370221,29.8493918863434));
#79617=CARTESIAN_POINT('Ctrl Pts',(199.113332597792,12.4334237614922,29.7951754901572));
#79618=CARTESIAN_POINT('Ctrl Pts',(199.110328333512,12.4445984091983,29.7409094481506));
#79619=CARTESIAN_POINT('Ctrl Pts',(199.107324069233,12.4526838073393,29.6860245743851));
#79620=CARTESIAN_POINT('Ctrl Pts',(199.104319804954,12.4576341211716,29.6309007975384));
#79621=CARTESIAN_POINT('Ctrl Pts',(199.101314153152,12.46258672131,29.5757515617357));
#79622=CARTESIAN_POINT('Ctrl Pts',(199.098308501351,12.4644013335964,29.5203637307685));
#79623=CARTESIAN_POINT('Ctrl Pts',(199.09530284955,12.4630842685681,29.4651191590033));
#79624=CARTESIAN_POINT('Ctrl Pts',(199.092291624031,12.4617647611579,29.4097721410137));
#79625=CARTESIAN_POINT('Ctrl Pts',(199.089280398512,12.4573020187898,29.3545694395871));
#79626=CARTESIAN_POINT('Ctrl Pts',(199.086269172992,12.4497543379427,29.2998885070358));
#79627=CARTESIAN_POINT('Ctrl Pts',(199.084099279885,12.4443154691035,29.2604853544417));
#79628=CARTESIAN_POINT('Ctrl Pts',(199.081929386778,12.4372757958333,29.2213530221574));
#79629=CARTESIAN_POINT('Ctrl Pts',(199.079759493671,12.4286733336564,29.1826283634301));
#79630=CARTESIAN_POINT('Ctrl Pts',(199.07675034364,12.4167436679778,29.1289260369756));
#79631=CARTESIAN_POINT('Ctrl Pts',(199.073741193609,12.4017568779544,29.0757847809708));
#79632=CARTESIAN_POINT('Ctrl Pts',(199.070732043578,12.383782542528,29.0235777870472));
#79633=CARTESIAN_POINT('Ctrl Pts',(199.067728196713,12.3658398841116,28.9714627999454));
#79634=CARTESIAN_POINT('Ctrl Pts',(199.064724349847,12.3449202993446,28.9202793031738));
#79635=CARTESIAN_POINT('Ctrl Pts',(199.061720502982,12.3211438748843,28.8703881260208));
#79636=CARTESIAN_POINT('Ctrl Pts',(199.058719597923,12.2973907357786,28.82054580961));
#79637=CARTESIAN_POINT('Ctrl Pts',(199.055718692864,12.270786525552,28.7719937804295));
#79638=CARTESIAN_POINT('Ctrl Pts',(199.052717787805,12.2414997540638,28.7250738030886));
#79639=CARTESIAN_POINT('Ctrl Pts',(199.049718634572,12.2122300791931,28.6781812160289));
#79640=CARTESIAN_POINT('Ctrl Pts',(199.046719481339,12.1802812262359,28.632919239829));
#79641=CARTESIAN_POINT('Ctrl Pts',(199.043720328106,12.1458669461172,28.5896038270094));
#79642=CARTESIAN_POINT('Ctrl Pts',(199.040721739337,12.111459143039,28.546296566494));
#79643=CARTESIAN_POINT('Ctrl Pts',(199.037723150568,12.0745871630082,28.5049355551979));
#79644=CARTESIAN_POINT('Ctrl Pts',(199.0347245618,12.0355058586884,28.4658047251017));
#79645=CARTESIAN_POINT('Ctrl Pts',(199.031723194895,11.9963883462823,28.4266376410345));
#79646=CARTESIAN_POINT('Ctrl Pts',(199.028721827991,11.955057794877,28.3897052403928));
#79647=CARTESIAN_POINT('Ctrl Pts',(199.025720461087,11.9118057930955,28.3552544187998));
#79648=CARTESIAN_POINT('Ctrl Pts',(199.022717694468,11.8685336203466,28.3207875307504));
#79649=CARTESIAN_POINT('Ctrl Pts',(199.019714927849,11.8233386433526,28.2888048340456));
#79650=CARTESIAN_POINT('Ctrl Pts',(199.01671216123,11.7765427345572,28.259510729024));
#79651=CARTESIAN_POINT('Ctrl Pts',(199.0137037656,11.7296591017816,28.2301617090419));
#79652=CARTESIAN_POINT('Ctrl Pts',(199.010695369971,11.6811690068258,28.2035116029031));
#79653=CARTESIAN_POINT('Ctrl Pts',(199.007686974342,11.6314192312139,28.1797189676234));
#79654=CARTESIAN_POINT('Ctrl Pts',(199.005493847874,11.5951515446659,28.1623740886193));
#79655=CARTESIAN_POINT('Ctrl Pts',(199.003300721405,11.5582149209316,28.1465468160399));
#79656=CARTESIAN_POINT('Ctrl Pts',(199.001107594937,11.5207491537022,28.1322819848673));
#79657=CARTESIAN_POINT('Ctrl Pts',(198.998090930476,11.4692146662257,28.1126605859803));
#79658=CARTESIAN_POINT('Ctrl Pts',(198.995074266014,11.4164644752731,28.0959158357281));
#79659=CARTESIAN_POINT('Ctrl Pts',(198.992057601553,11.3628503020118,28.082194686027));
#79660=CARTESIAN_POINT('Ctrl Pts',(198.989046266859,11.3093308529307,28.0684977785101));
#79661=CARTESIAN_POINT('Ctrl Pts',(198.986034932165,11.2549509564839,28.0578139977815));
#79662=CARTESIAN_POINT('Ctrl Pts',(198.983023597471,11.2000796617887,28.0502412687145));
#79663=CARTESIAN_POINT('Ctrl Pts',(198.980015226992,11.1452623797891,28.0426759938822));
#79664=CARTESIAN_POINT('Ctrl Pts',(198.977006856512,11.0899551760505,28.0382157745756));
#79665=CARTESIAN_POINT('Ctrl Pts',(198.973998486033,11.0345377234283,28.0369075915512));
#79666=CARTESIAN_POINT('Ctrl Pts',(198.970991903168,10.9791532006022,28.0356001858669));
#79667=CARTESIAN_POINT('Ctrl Pts',(198.967985320303,10.9236590831148,28.0374411157049));
#79668=CARTESIAN_POINT('Ctrl Pts',(198.964978737438,10.8684383194882,28.042425379536));
#79669=CARTESIAN_POINT('Ctrl Pts',(198.961972768234,10.8132288267504,28.0474086260489));
#79670=CARTESIAN_POINT('Ctrl Pts',(198.958966799031,10.7582931001436,28.0555338849726));
#79671=CARTESIAN_POINT('Ctrl Pts',(198.955960829828,10.7040099414027,28.0667442184971));
#79672=CARTESIAN_POINT('Ctrl Pts',(198.952952216565,10.6496790350379,28.0779644126635));
#79673=CARTESIAN_POINT('Ctrl Pts',(198.949943603302,10.5960023590066,28.0922749963719));
#79674=CARTESIAN_POINT('Ctrl Pts',(198.94693499004,10.5433479918902,28.1095679831472));
#79675=CARTESIAN_POINT('Ctrl Pts',(198.943925041331,10.4906702528656,28.126868645831));
#79676=CARTESIAN_POINT('Ctrl Pts',(198.940915092623,10.4390162176512,28.1471541590495));
#79677=CARTESIAN_POINT('Ctrl Pts',(198.937905143915,10.3887351995767,28.1702678488645));
#79678=CARTESIAN_POINT('Ctrl Pts',(198.9348897579,10.3383633516001,28.1934232922928));
#79679=CARTESIAN_POINT('Ctrl Pts',(198.931874371884,10.2893699407518,28.2194168713064));
#79680=CARTESIAN_POINT('Ctrl Pts',(198.928858985869,10.2420797583762,28.2480458645234));
#79681=CARTESIAN_POINT('Ctrl Pts',(198.92672455598,10.2086055768981,28.2683107919637));
#79682=CARTESIAN_POINT('Ctrl Pts',(198.924590126091,10.1759842445242,28.2898952236279));
#79683=CARTESIAN_POINT('Ctrl Pts',(198.922455696203,10.1443211833688,28.3127148561662));
#79684=CARTESIAN_POINT('Ctrl Pts',(198.919318172452,10.0977777916554,28.3462587731857));
#79685=CARTESIAN_POINT('Ctrl Pts',(198.916180648701,10.0531030287581,28.3826208168073));
#79686=CARTESIAN_POINT('Ctrl Pts',(198.91304312495,10.0106574334974,28.4215596742953));
#79687=CARTESIAN_POINT('Ctrl Pts',(198.910057117073,9.9702616016631,28.4586181141462));
#79688=CARTESIAN_POINT('Ctrl Pts',(198.907071109196,9.93188506305593,28.4980098223084));
#79689=CARTESIAN_POINT('Ctrl Pts',(198.904085101318,9.89580812800508,28.5394831808759));
#79690=CARTESIAN_POINT('Ctrl Pts',(198.901101865289,9.8597646824164,28.5809180405944));
#79691=CARTESIAN_POINT('Ctrl Pts',(198.89811862926,9.82601696303526,28.6244303220827));
#79692=CARTESIAN_POINT('Ctrl Pts',(198.895135393231,9.79480843547741,28.6697316441032));
#79693=CARTESIAN_POINT('Ctrl Pts',(198.892153710288,9.76361615522021,28.7150093820505));
#79694=CARTESIAN_POINT('Ctrl Pts',(198.889172027346,9.73496075035578,28.7620738746278));
#79695=CARTESIAN_POINT('Ctrl Pts',(198.886190344403,9.70904387744193,28.8106056718903));
#79696=CARTESIAN_POINT('Ctrl Pts',(198.883208998249,9.68312993190989,28.8591319873532));
#79697=CARTESIAN_POINT('Ctrl Pts',(198.880227652096,9.65995415457463,28.9091248054983));
#79698=CARTESIAN_POINT('Ctrl Pts',(198.877246305942,9.63967233018285,28.960239978574));
#79699=CARTESIAN_POINT('Ctrl Pts',(198.874262118805,9.61937117883709,29.011403860315));
#79700=CARTESIAN_POINT('Ctrl Pts',(198.871277931667,9.6019696806173,29.0636917325209));
#79701=CARTESIAN_POINT('Ctrl Pts',(198.86829374453,9.58757487353748,29.1167409333919));
#79702=CARTESIAN_POINT('Ctrl Pts',(198.865307895739,9.57317205115243,29.1698196730774));
#79703=CARTESIAN_POINT('Ctrl Pts',(198.862322046949,9.56177936146926,29.2236600609534));
#79704=CARTESIAN_POINT('Ctrl Pts',(198.859336198159,9.55345273827624,29.2778890601535));
#79705=CARTESIAN_POINT('Ctrl Pts',(198.856345198788,9.54511175168336,29.3322116042134));
#79706=CARTESIAN_POINT('Ctrl Pts',(198.853354199418,9.53984743173593,29.3869235644018));
#79707=CARTESIAN_POINT('Ctrl Pts',(198.850363200047,9.53766374727779,29.4416481879084));
#79708=CARTESIAN_POINT('Ctrl Pts',(198.849293842093,9.53688302483176,29.461213625471));
#79709=CARTESIAN_POINT('Ctrl Pts',(198.848224484139,9.5364955976742,29.4807807041731));
#79710=CARTESIAN_POINT('Ctrl Pts',(198.847155126185,9.5365000377376,29.500332352169));
#79711=CARTESIAN_POINT('Origin',(197.762132885264,11.,29.5));
#79712=CARTESIAN_POINT('',(204.512132885225,9.82225001771146,29.4997957468552));
#79713=CARTESIAN_POINT('Ctrl Pts',(204.456095751509,10.1027690874833,30.2629362700282));
#79714=CARTESIAN_POINT('Ctrl Pts',(204.459251171507,10.0724807910944,30.2273165244804));
#79715=CARTESIAN_POINT('Ctrl Pts',(204.462406591505,10.0442847328763,30.18985243697));
#79716=CARTESIAN_POINT('Ctrl Pts',(204.465562011503,10.0184068810581,30.1508225651788));
#79717=CARTESIAN_POINT('Ctrl Pts',(204.468715935768,9.99254129587267,30.1118111943477));
#79718=CARTESIAN_POINT('Ctrl Pts',(204.471869860032,9.96899205078237,30.0712359781232));
#79719=CARTESIAN_POINT('Ctrl Pts',(204.475023784296,9.94794254402139,30.0294054890345));
#79720=CARTESIAN_POINT('Ctrl Pts',(204.47817997384,9.92687791862971,29.9875449555498));
#79721=CARTESIAN_POINT('Ctrl Pts',(204.481336163384,9.90831687996344,29.9444278478773));
#79722=CARTESIAN_POINT('Ctrl Pts',(204.484492352928,9.89239647383176,29.9003866772505));
#79723=CARTESIAN_POINT('Ctrl Pts',(204.487649506968,9.87647120260323,29.8563320481379));
#79724=CARTESIAN_POINT('Ctrl Pts',(204.490806661008,9.86318833913874,29.8113533321652));
#79725=CARTESIAN_POINT('Ctrl Pts',(204.493963815047,9.85263516109169,29.7657987752735));
#79726=CARTESIAN_POINT('Ctrl Pts',(204.497127144096,9.84206134231471,29.7201551192213));
#79727=CARTESIAN_POINT('Ctrl Pts',(204.500290473144,9.83422797565444,29.6739339282284));
#79728=CARTESIAN_POINT('Ctrl Pts',(204.503453802192,9.82917094541982,29.6274926956766));
#79729=CARTESIAN_POINT('Ctrl Pts',(204.50634682987,9.82454603027125,29.5850197916237));
#79730=CARTESIAN_POINT('Ctrl Pts',(204.509239857548,9.82224263537602,29.5423632453761));
#79731=CARTESIAN_POINT('Ctrl Pts',(204.512132885225,9.82225001771146,29.4997957468552));
#79732=CARTESIAN_POINT('',(204.899997647687,10.8098243290602,30.6622944018977));
#79733=CARTESIAN_POINT('Ctrl Pts',(204.512132885264,9.82225001771156,29.4997957462862));
#79734=CARTESIAN_POINT('Ctrl Pts',(204.512893439603,9.82225195847519,29.4886050840047));
#79735=CARTESIAN_POINT('Ctrl Pts',(204.513653993942,9.8224133915092,29.4774159819222));
#79736=CARTESIAN_POINT('Ctrl Pts',(204.514414548282,9.82273420589625,29.4662314860668));
#79737=CARTESIAN_POINT('Ctrl Pts',(204.517691710729,9.82411656716551,29.418038466954));
#79738=CARTESIAN_POINT('Ctrl Pts',(204.520968873176,9.82846618208739,29.3698219095396));
#79739=CARTESIAN_POINT('Ctrl Pts',(204.524246035624,9.83578244468732,29.3219759948721));
#79740=CARTESIAN_POINT('Ctrl Pts',(204.527420481918,9.84286939355581,29.2756297154456));
#79741=CARTESIAN_POINT('Ctrl Pts',(204.530594928212,9.85273966328401,29.2296317836103));
#79742=CARTESIAN_POINT('Ctrl Pts',(204.533769374506,9.86534000748018,29.1843391632227));
#79743=CARTESIAN_POINT('Ctrl Pts',(204.53694069231,9.87792793374334,29.1390911797687));
#79744=CARTESIAN_POINT('Ctrl Pts',(204.540112010113,9.89324046023478,29.0945476658318));
#79745=CARTESIAN_POINT('Ctrl Pts',(204.543283327916,9.91117340460796,29.0510548945951));
#79746=CARTESIAN_POINT('Ctrl Pts',(204.546452910818,9.92909653858145,29.0075859165215));
#79747=CARTESIAN_POINT('Ctrl Pts',(204.549622493719,9.94963703863887,28.965167056149));
#79748=CARTESIAN_POINT('Ctrl Pts',(204.552792076621,9.97264193779918,28.9241263380472));
#79749=CARTESIAN_POINT('Ctrl Pts',(204.555961315207,9.99564433790623,28.883090078254));
#79750=CARTESIAN_POINT('Ctrl Pts',(204.559130553792,10.0211103315968,28.8434321476796));
#79751=CARTESIAN_POINT('Ctrl Pts',(204.562299792378,10.048841461537,28.8054551870406));
#79752=CARTESIAN_POINT('Ctrl Pts',(204.565472205846,10.0766003719902,28.7674401818121));
#79753=CARTESIAN_POINT('Ctrl Pts',(204.568644619314,10.1066286158871,28.7311099554934));
#79754=CARTESIAN_POINT('Ctrl Pts',(204.571817032781,10.1386861062732,28.6967357601803));
#79755=CARTESIAN_POINT('Ctrl Pts',(204.57499138483,10.1707631861689,28.6623405596787));
#79756=CARTESIAN_POINT('Ctrl Pts',(204.578165736878,10.2048715767345,28.6299041524169));
#79757=CARTESIAN_POINT('Ctrl Pts',(204.581340088926,10.2407354097751,28.5996598728643));
#79758=CARTESIAN_POINT('Ctrl Pts',(204.584520042633,10.2766625303599,28.5693622223802));
#79759=CARTESIAN_POINT('Ctrl Pts',(204.58769999634,10.314350824734,28.541264745237));
#79760=CARTESIAN_POINT('Ctrl Pts',(204.590879950047,10.3534941684928,28.5155583956744));
#79761=CARTESIAN_POINT('Ctrl Pts',(204.59160878237,10.3624656620405,28.5096666059832));
#79762=CARTESIAN_POINT('Ctrl Pts',(204.592337614693,10.3715134882872,28.5039002332347));
#79763=CARTESIAN_POINT('Ctrl Pts',(204.593066447016,10.3806337904139,28.498261231197));
#79764=CARTESIAN_POINT('Ctrl Pts',(204.596343609463,10.4216428273245,28.4729057068416));
#79765=CARTESIAN_POINT('Ctrl Pts',(204.599620771911,10.4643037186516,28.4500154946675));
#79766=CARTESIAN_POINT('Ctrl Pts',(204.602897934358,10.5082868708975,28.4298069047278));
#79767=CARTESIAN_POINT('Ctrl Pts',(204.606072182813,10.5508888033101,28.4102329329044));
#79768=CARTESIAN_POINT('Ctrl Pts',(204.609246431269,10.5947306225305,28.3931748907485));
#79769=CARTESIAN_POINT('Ctrl Pts',(204.612420679724,10.6394849311947,28.3787846113862));
#79770=CARTESIAN_POINT('Ctrl Pts',(204.615591809407,10.6841952677083,28.3644084708086));
#79771=CARTESIAN_POINT('Ctrl Pts',(204.618762939089,10.7298157913554,28.3526950744201));
#79772=CARTESIAN_POINT('Ctrl Pts',(204.621934068771,10.7760000228538,28.3437478334124));
#79773=CARTESIAN_POINT('Ctrl Pts',(204.625103473532,10.8221591326404,28.3348054592175));
#79774=CARTESIAN_POINT('Ctrl Pts',(204.628272878292,10.8688807971651,28.3286263652757));
#79775=CARTESIAN_POINT('Ctrl Pts',(204.631442283052,10.9158069516336,28.3252631813437));
#79776=CARTESIAN_POINT('Ctrl Pts',(204.634611353751,10.9627281599921,28.321900351898));
#79777=CARTESIAN_POINT('Ctrl Pts',(204.637780424449,11.0098532603664,28.3213528806569));
#79778=CARTESIAN_POINT('Ctrl Pts',(204.640949495148,11.0568203743606,28.3236214437701));
#79779=CARTESIAN_POINT('Ctrl Pts',(204.644121756859,11.10383478065,28.325892291153));
#79780=CARTESIAN_POINT('Ctrl Pts',(204.647294018569,11.1506903263654,28.3309848015154));
#79781=CARTESIAN_POINT('Ctrl Pts',(204.65046628028,11.1970284568235,28.3388476199474));
#79782=CARTESIAN_POINT('Ctrl Pts',(204.653640489855,11.2433950402878,28.3467152663865));
#79783=CARTESIAN_POINT('Ctrl Pts',(204.65681469943,11.2892430339211,28.357356479953));
#79784=CARTESIAN_POINT('Ctrl Pts',(204.659988909005,11.3342258791852,28.3706691697368));
#79785=CARTESIAN_POINT('Ctrl Pts',(204.663168734926,11.3792883156843,28.3840054145763));
#79786=CARTESIAN_POINT('Ctrl Pts',(204.666348560848,11.4234820289682,28.400022371368));
#79787=CARTESIAN_POINT('Ctrl Pts',(204.66952838677,11.4664792212056,28.4185693740774));
#79788=CARTESIAN_POINT('Ctrl Pts',(204.670258373096,11.4763500013037,28.4228271726846));
#79789=CARTESIAN_POINT('Ctrl Pts',(204.670988359423,11.4861578265088,28.4272181176327));
#79790=CARTESIAN_POINT('Ctrl Pts',(204.67171834575,11.4958989262837,28.4317400515742));
#79791=CARTESIAN_POINT('Ctrl Pts',(204.674995508197,11.5396301102882,28.4520405853768));
#79792=CARTESIAN_POINT('Ctrl Pts',(204.678272670645,11.5822124998671,28.4750772168618));
#79793=CARTESIAN_POINT('Ctrl Pts',(204.681549833092,11.6232835343469,28.5006938915867));
#79794=CARTESIAN_POINT('Ctrl Pts',(204.684720990222,11.6630260573188,28.5254819519951));
#79795=CARTESIAN_POINT('Ctrl Pts',(204.687892147353,11.701352999871,28.5526853558338));
#79796=CARTESIAN_POINT('Ctrl Pts',(204.691063304483,11.7379578236565,28.5821147604389));
#79797=CARTESIAN_POINT('Ctrl Pts',(204.694231337706,11.774526588025,28.6115151741334));
#79798=CARTESIAN_POINT('Ctrl Pts',(204.697399370929,11.8093761583506,28.6431369004431));
#79799=CARTESIAN_POINT('Ctrl Pts',(204.700567404152,11.8422299025174,28.6767480010315));
#79800=CARTESIAN_POINT('Ctrl Pts',(204.703733713565,11.8750657700944,28.7103408129325));
#79801=CARTESIAN_POINT('Ctrl Pts',(204.706900022977,11.905907573397,28.7459204564798));
#79802=CARTESIAN_POINT('Ctrl Pts',(204.71006633239,11.9345146968104,28.7832173663199));
#79803=CARTESIAN_POINT('Ctrl Pts',(204.713232315092,11.9631188684441,28.8205104277387));
#79804=CARTESIAN_POINT('Ctrl Pts',(204.716398297794,11.9894884804504,28.8595199597774));
#79805=CARTESIAN_POINT('Ctrl Pts',(204.719564280496,12.0134242008582,28.8999446262095));
#79806=CARTESIAN_POINT('Ctrl Pts',(204.722733487946,12.0373843012709,28.9404104676531));
#79807=CARTESIAN_POINT('Ctrl Pts',(204.725902695396,12.0589052809648,28.9822938374839));
#79808=CARTESIAN_POINT('Ctrl Pts',(204.729071902847,12.0778330889414,29.0252675544236));
#79809=CARTESIAN_POINT('Ctrl Pts',(204.732243074755,12.0967726294682,29.0682679089586));
#79810=CARTESIAN_POINT('Ctrl Pts',(204.735414246663,12.1131156063047,29.1123594320846));
#79811=CARTESIAN_POINT('Ctrl Pts',(204.738585418572,12.1267569467799,29.1571970750076));
#79812=CARTESIAN_POINT('Ctrl Pts',(204.741762260819,12.1404226791918,29.2021148916462));
#79813=CARTESIAN_POINT('Ctrl Pts',(204.744939103066,12.1513770134583,29.247780946518));
#79814=CARTESIAN_POINT('Ctrl Pts',(204.748115945314,12.1595657696491,29.2938391687104));
#79815=CARTESIAN_POINT('Ctrl Pts',(204.748867378371,12.1615026936814,29.3047335310979));
#79816=CARTESIAN_POINT('Ctrl Pts',(204.749618811427,12.1632851163349,29.3156498153152));
#79817=CARTESIAN_POINT('Ctrl Pts',(204.750370244484,12.1649127461391,29.3265832868996));
#79818=CARTESIAN_POINT('Ctrl Pts',(204.753647406931,12.1720111925336,29.3742665265072));
#79819=CARTESIAN_POINT('Ctrl Pts',(204.756924569379,12.1761928797529,29.4224921053704));
#79820=CARTESIAN_POINT('Ctrl Pts',(204.760201731826,12.1773897634831,29.4708725671355));
#79821=CARTESIAN_POINT('Ctrl Pts',(204.763380803022,12.1785508223725,29.5178049163603));
#79822=CARTESIAN_POINT('Ctrl Pts',(204.766559874218,12.1769032410329,29.564882406677));
#79823=CARTESIAN_POINT('Ctrl Pts',(204.769738945413,12.1724369784728,29.6117434293802));
#79824=CARTESIAN_POINT('Ctrl Pts',(204.772914862409,12.1679751472337,29.6585579576738));
#79825=CARTESIAN_POINT('Ctrl Pts',(204.776090779405,12.1607002235794,29.7051558935741));
#79826=CARTESIAN_POINT('Ctrl Pts',(204.779266696401,12.1506541863793,29.7511772399477));
#79827=CARTESIAN_POINT('Ctrl Pts',(204.782440843553,12.1406137475358,29.7971729399991));
#79828=CARTESIAN_POINT('Ctrl Pts',(204.785614990705,12.1278053729575,29.8425921459696));
#79829=CARTESIAN_POINT('Ctrl Pts',(204.788789137858,12.1123222703681,29.8870842664629));
#79830=CARTESIAN_POINT('Ctrl Pts',(204.79196289648,12.0968410629802,29.9315709409205));
#79831=CARTESIAN_POINT('Ctrl Pts',(204.795136655102,12.0786859618688,29.9751302321802));
#79832=CARTESIAN_POINT('Ctrl Pts',(204.798310413724,12.0579994206949,30.0174285344946));
#79833=CARTESIAN_POINT('Ctrl Pts',(204.801487248844,12.0372928269251,30.0597678388671));
#79834=CARTESIAN_POINT('Ctrl Pts',(204.804664083965,12.0140501425046,30.1008432169051));
#79835=CARTESIAN_POINT('Ctrl Pts',(204.807840919085,11.9884603266246,30.1403446300152));
#79836=CARTESIAN_POINT('Ctrl Pts',(204.811019639365,11.9628553255382,30.1798694835873));
#79837=CARTESIAN_POINT('Ctrl Pts',(204.814198359645,11.9349007495811,30.217818066111));
#79838=CARTESIAN_POINT('Ctrl Pts',(204.817377079925,11.9048274810867,30.253911328984));
#79839=CARTESIAN_POINT('Ctrl Pts',(204.820561282099,11.874702349435,30.2900668368558));
#79840=CARTESIAN_POINT('Ctrl Pts',(204.823745484273,11.8424516184588,30.324360240831));
#79841=CARTESIAN_POINT('Ctrl Pts',(204.826929686447,11.8083434499435,30.3565488482471));
#79842=CARTESIAN_POINT('Ctrl Pts',(204.827627172037,11.8008722044781,30.3635996222307));
#79843=CARTESIAN_POINT('Ctrl Pts',(204.828324657628,11.793311960662,30.3705495616509));
#79844=CARTESIAN_POINT('Ctrl Pts',(204.829022143218,11.7856657360398,30.3773963834625));
#79845=CARTESIAN_POINT('Ctrl Pts',(204.832160484023,11.7512615002151,30.4082037013083));
#79846=CARTESIAN_POINT('Ctrl Pts',(204.835298824828,11.7149584985154,30.4370593463094));
#79847=CARTESIAN_POINT('Ctrl Pts',(204.838437165633,11.6770096964571,30.4637182852904));
#79848=CARTESIAN_POINT('Ctrl Pts',(204.8415710348,11.6391149654251,30.49033923951));
#79849=CARTESIAN_POINT('Ctrl Pts',(204.844704903967,11.599579532835,30.5147693478104));
#79850=CARTESIAN_POINT('Ctrl Pts',(204.847838773134,11.5586905173501,30.5368027624978));
#79851=CARTESIAN_POINT('Ctrl Pts',(204.850969639116,11.5178406857839,30.5588150625773));
#79852=CARTESIAN_POINT('Ctrl Pts',(204.854100505098,11.4756403384177,30.5784349409332));
#79853=CARTESIAN_POINT('Ctrl Pts',(204.85723137108,11.4324043118212,30.5955006041159));
#79854=CARTESIAN_POINT('Ctrl Pts',(204.860360696891,11.3891895543849,30.6125578721627));
#79855=CARTESIAN_POINT('Ctrl Pts',(204.863490022701,11.3449406583823,30.6270632035716));
#79856=CARTESIAN_POINT('Ctrl Pts',(204.866619348512,11.2999930468601,30.6389026448014));
#79857=CARTESIAN_POINT('Ctrl Pts',(204.869750597747,11.2550178085163,30.6507493630838));
#79858=CARTESIAN_POINT('Ctrl Pts',(204.872881846982,11.2093435496543,30.6599267660785));
#79859=CARTESIAN_POINT('Ctrl Pts',(204.876013096216,11.1633193090463,30.6663712384111));
#79860=CARTESIAN_POINT('Ctrl Pts',(204.879145355631,11.1172802204449,30.6728177898108));
#79861=CARTESIAN_POINT('Ctrl Pts',(204.882277615046,11.0708914961412,30.6765296033856));
#79862=CARTESIAN_POINT('Ctrl Pts',(204.885409874461,11.0245070441812,30.6774949967136));
#79863=CARTESIAN_POINT('Ctrl Pts',(204.888547402122,10.9780445767542,30.6784620137669));
#79864=CARTESIAN_POINT('Ctrl Pts',(204.891684929782,10.9315869687223,30.676673411482));
#79865=CARTESIAN_POINT('Ctrl Pts',(204.894822457443,10.8854858481198,30.6721696001514));
#79866=CARTESIAN_POINT('Ctrl Pts',(204.896547520857,10.8601387069477,30.6696933318934));
#79867=CARTESIAN_POINT('Ctrl Pts',(204.898272584272,10.8348992087756,30.6663971766041));
#79868=CARTESIAN_POINT('Ctrl Pts',(204.899997647687,10.8098243290602,30.6622944018976));
#79869=CARTESIAN_POINT('',(204.9,12.0381913065552,30.0561059912401));
#79870=CARTESIAN_POINT('Origin',(204.9,11.,29.5));
#79871=CARTESIAN_POINT('Ctrl Pts',(204.9,12.0381913065552,30.0561059912401));
#79872=CARTESIAN_POINT('Ctrl Pts',(204.8997621394,12.0398535320846,30.0530027912723));
#79873=CARTESIAN_POINT('Ctrl Pts',(204.89952497894,12.0415018578031,30.0498921132293));
#79874=CARTESIAN_POINT('Ctrl Pts',(204.899013325775,12.0450378088497,30.0431462212962));
#79875=CARTESIAN_POINT('Ctrl Pts',(204.898739072365,12.0469204737467,30.0395084450192));
#79876=CARTESIAN_POINT('Ctrl Pts',(204.897680308448,12.0541376476317,30.0253830292433));
#79877=CARTESIAN_POINT('Ctrl Pts',(204.89690203245,12.0593340221635,30.0148251714119));
#79878=CARTESIAN_POINT('Ctrl Pts',(204.892716259105,12.0866302329651,29.9572015369054));
#79879=CARTESIAN_POINT('Ctrl Pts',(204.889419901625,12.1057547581559,29.9087857804606));
#79880=CARTESIAN_POINT('Ctrl Pts',(204.88277133655,12.1378588951479,29.8085562301249));
#79881=CARTESIAN_POINT('Ctrl Pts',(204.879426409703,12.1506424663593,29.7568101653783));
#79882=CARTESIAN_POINT('Ctrl Pts',(204.873957668299,12.1654413373207,29.6728239710727));
#79883=CARTESIAN_POINT('Ctrl Pts',(204.871880972903,12.1697110786283,29.6410581390914));
#79884=CARTESIAN_POINT('Ctrl Pts',(204.86888439387,12.1739260763192,29.5957771724359));
#79885=CARTESIAN_POINT('Ctrl Pts',(204.867993052736,12.1749425694157,29.5823749751506));
#79886=CARTESIAN_POINT('Ctrl Pts',(204.866414377093,12.1763264255328,29.5587805592554));
#79887=CARTESIAN_POINT('Ctrl Pts',(204.865729800394,12.1767911863115,29.5485953429596));
#79888=CARTESIAN_POINT('Ctrl Pts',(204.864283413661,12.1774897790295,29.5271836312266));
#79889=CARTESIAN_POINT('Ctrl Pts',(204.863520879776,12.1776954105801,29.5159573038996));
#79890=CARTESIAN_POINT('Ctrl Pts',(204.861460576082,12.1778165078225,29.4858051968804));
#79891=CARTESIAN_POINT('Ctrl Pts',(204.860154549293,12.1774363518464,29.4668822054782));
#79892=CARTESIAN_POINT('Ctrl Pts',(204.851760518394,12.1721170338875,29.3465745301024));
#79893=CARTESIAN_POINT('Ctrl Pts',(204.84429566794,12.1545442070436,29.2461938481589));
#79894=CARTESIAN_POINT('Ctrl Pts',(204.832481771872,12.1068316636469,29.0932147548902));
#79895=CARTESIAN_POINT('Ctrl Pts',(204.828171512584,12.0851503279611,29.0384798070805));
#79896=CARTESIAN_POINT('Ctrl Pts',(204.823333120496,12.0550535108067,28.9764932034397));
#79897=CARTESIAN_POINT('Ctrl Pts',(204.822628894145,12.0505205545771,28.9674552991932));
#79898=CARTESIAN_POINT('Ctrl Pts',(204.821530312826,12.0431997640778,28.9533162876739));
#79899=CARTESIAN_POINT('Ctrl Pts',(204.821131560455,12.0404897145043,28.9481757646331));
#79900=CARTESIAN_POINT('Ctrl Pts',(204.820380238465,12.0352809514194,28.9384704004453));
#79901=CARTESIAN_POINT('Ctrl Pts',(204.820027264506,12.0327899591039,28.9339019150734));
#79902=CARTESIAN_POINT('Ctrl Pts',(204.819251361133,12.0272177924107,28.9238417617422));
#79903=CARTESIAN_POINT('Ctrl Pts',(204.818829303563,12.0241227628582,28.9183581173867));
#79904=CARTESIAN_POINT('Ctrl Pts',(204.817372035183,12.0132196290819,28.8993972727712));
#79905=CARTESIAN_POINT('Ctrl Pts',(204.816349865883,12.005187907466,28.8860496927542));
#79906=CARTESIAN_POINT('Ctrl Pts',(204.810677945495,11.9586168467305,28.8120204159697));
#79907=CARTESIAN_POINT('Ctrl Pts',(204.806276193001,11.9148462150769,28.7548014717858));
#79908=CARTESIAN_POINT('Ctrl Pts',(204.800859524225,11.8555976668415,28.6905007113916));
#79909=CARTESIAN_POINT('Ctrl Pts',(204.799895492085,11.8448443379115,28.6792841537973));
#79910=CARTESIAN_POINT('Ctrl Pts',(204.796717948592,11.8088265218339,28.643172966142));
#79911=CARTESIAN_POINT('Ctrl Pts',(204.794488948545,11.7826606131208,28.6192077368393));
#79912=CARTESIAN_POINT('Ctrl Pts',(204.790623897005,11.7363554295078,28.5804916860132));
#79913=CARTESIAN_POINT('Ctrl Pts',(204.789010268092,11.7167557547728,28.5651332147385));
#79914=CARTESIAN_POINT('Ctrl Pts',(204.786622134294,11.6874922607355,28.5436635249152));
#79915=CARTESIAN_POINT('Ctrl Pts',(204.785866986079,11.6782021358176,28.5370530077902));
#79916=CARTESIAN_POINT('Ctrl Pts',(204.784516542602,11.6615351404257,28.5255542079479));
#79917=CARTESIAN_POINT('Ctrl Pts',(204.783923370422,11.6541963053092,28.5206121655161));
#79918=CARTESIAN_POINT('Ctrl Pts',(204.782661341268,11.6385496556531,28.510329890232));
#79919=CARTESIAN_POINT('Ctrl Pts',(204.781991751255,11.630228998063,28.5050105586854));
#79920=CARTESIAN_POINT('Ctrl Pts',(204.780170726628,11.6075561671157,28.4909144920433));
#79921=CARTESIAN_POINT('Ctrl Pts',(204.779011906754,11.5930817216433,28.4823399007452));
#79922=CARTESIAN_POINT('Ctrl Pts',(204.770989069588,11.4926125388997,28.4256939284209));
#79923=CARTESIAN_POINT('Ctrl Pts',(204.763732780374,11.401079393115,28.3882769545885));
#79924=CARTESIAN_POINT('Ctrl Pts',(204.753631994265,11.2688033510141,28.3526891134676));
#79925=CARTESIAN_POINT('Ctrl Pts',(204.750804328036,11.2311523543663,28.3445146195401));
#79926=CARTESIAN_POINT('Ctrl Pts',(204.746960200983,11.1784255428744,28.3357480122263));
#79927=CARTESIAN_POINT('Ctrl Pts',(204.745894692865,11.1636384986637,28.3335777553877));
#79928=CARTESIAN_POINT('Ctrl Pts',(204.744046256935,11.1376194936769,28.3302635875255));
#79929=CARTESIAN_POINT('Ctrl Pts',(204.743258128614,11.1264050946354,28.3289986437637));
#79930=CARTESIAN_POINT('Ctrl Pts',(204.742075044553,11.1093614911839,28.3273239002478));
#79931=CARTESIAN_POINT('Ctrl Pts',(204.741673878754,11.1035449080758,28.3267959993782));
#79932=CARTESIAN_POINT('Ctrl Pts',(204.740926438267,11.0926327594941,28.3258874247159));
#79933=CARTESIAN_POINT('Ctrl Pts',(204.740579582805,11.0875382366932,28.3254966039862));
#79934=CARTESIAN_POINT('Ctrl Pts',(204.73977870613,11.0757085508936,28.3246665027824));
#79935=CARTESIAN_POINT('Ctrl Pts',(204.739326029258,11.0689717577804,28.3242519332794));
#79936=CARTESIAN_POINT('Ctrl Pts',(204.737878475276,11.0472819280288,28.3231042529416));
#79937=CARTESIAN_POINT('Ctrl Pts',(204.736894886709,11.0323177233119,28.3225982866763));
#79938=CARTESIAN_POINT('Ctrl Pts',(204.731117051202,10.9433771928577,28.3212881356391));
#79939=CARTESIAN_POINT('Ctrl Pts',(204.726587413168,10.8694606630325,28.3271701914354));
#79940=CARTESIAN_POINT('Ctrl Pts',(204.718423111919,10.7396533226863,28.3499327253727));
#79941=CARTESIAN_POINT('Ctrl Pts',(204.714821888093,10.6835456352904,28.3640902866266));
#79942=CARTESIAN_POINT('Ctrl Pts',(204.709666519717,10.6075550195903,28.3893340893997));
#79943=CARTESIAN_POINT('Ctrl Pts',(204.708215569518,10.5866082330783,28.396959214733));
#79944=CARTESIAN_POINT('Ctrl Pts',(204.70600285836,10.5554215912255,28.4093250019287));
#79945=CARTESIAN_POINT('Ctrl Pts',(204.705255329852,10.5450121928987,28.413626218097));
#79946=CARTESIAN_POINT('Ctrl Pts',(204.703946108039,10.5270108615761,28.4213685589823));
#79947=CARTESIAN_POINT('Ctrl Pts',(204.703386678647,10.5193906882608,28.4247422661992));
#79948=CARTESIAN_POINT('Ctrl Pts',(204.702114415478,10.5022269844102,28.4325601151705));
#79949=CARTESIAN_POINT('Ctrl Pts',(204.701400026632,10.4927060586697,28.4370518697298));
#79950=CARTESIAN_POINT('Ctrl Pts',(204.699449334287,10.467031355635,28.4495881197688));
#79951=CARTESIAN_POINT('Ctrl Pts',(204.698204932061,10.4510007458687,28.4578769495896));
#79952=CARTESIAN_POINT('Ctrl Pts',(204.691579123177,10.367502300047,28.503512184149));
#79953=CARTESIAN_POINT('Ctrl Pts',(204.685988565283,10.3036426338576,28.5470444743933));
#79954=CARTESIAN_POINT('Ctrl Pts',(204.677061702671,10.2099690235038,28.625372822217));
#79955=CARTESIAN_POINT('Ctrl Pts',(204.673766637479,10.1771167262118,28.6562079076123));
#79956=CARTESIAN_POINT('Ctrl Pts',(204.668803075765,10.1294807006603,28.7063538972275));
#79957=CARTESIAN_POINT('Ctrl Pts',(204.66709033462,10.1133930330931,28.7243671937004));
#79958=CARTESIAN_POINT('Ctrl Pts',(204.664846260019,10.0926593639401,28.74907143223));
#79959=CARTESIAN_POINT('Ctrl Pts',(204.664286092104,10.0875133527247,28.7553330467909));
#79960=CARTESIAN_POINT('Ctrl Pts',(204.663357978279,10.0790305112331,28.7658748706159));
#79961=CARTESIAN_POINT('Ctrl Pts',(204.662987703017,10.0756579503402,28.7701258437393));
#79962=CARTESIAN_POINT('Ctrl Pts',(204.662228769661,10.0687673346919,28.7789355507026));
#79963=CARTESIAN_POINT('Ctrl Pts',(204.661840366852,10.0652531093118,28.7834970545875));
#79964=CARTESIAN_POINT('Ctrl Pts',(204.660794245967,10.0558262370379,28.7959206483484));
#79965=CARTESIAN_POINT('Ctrl Pts',(204.660140676092,10.0499782613084,28.8038315294323));
#79966=CARTESIAN_POINT('Ctrl Pts',(204.656251258742,10.0154831567366,28.8517392778778));
#79967=CARTESIAN_POINT('Ctrl Pts',(204.653148647334,9.98926276363873,28.8934303479486));
#79968=CARTESIAN_POINT('Ctrl Pts',(204.645799026573,9.93286816337074,28.9969661573862));
#79969=CARTESIAN_POINT('Ctrl Pts',(204.641593877423,9.90535244248988,29.060045484077));
#79970=CARTESIAN_POINT('Ctrl Pts',(204.634885854393,9.87156267080785,29.1606934057659));
#79971=CARTESIAN_POINT('Ctrl Pts',(204.632483470342,9.86133807472025,29.1967700871807));
#79972=CARTESIAN_POINT('Ctrl Pts',(204.629143052692,9.84979343198479,29.2464212002093));
#79973=CARTESIAN_POINT('Ctrl Pts',(204.628251747704,9.8469621351811,29.2596231813895));
#79974=CARTESIAN_POINT('Ctrl Pts',(204.626721994398,9.84252851621573,29.2821815627156));
#79975=CARTESIAN_POINT('Ctrl Pts',(204.626087168365,9.8408111635584,29.2915141729892));
#79976=CARTESIAN_POINT('Ctrl Pts',(204.62479374824,9.83756041306616,29.3104634964701));
#79977=CARTESIAN_POINT('Ctrl Pts',(204.624135018228,9.83603314421863,29.320080494722));
#79978=CARTESIAN_POINT('Ctrl Pts',(204.622466227357,9.83248665838815,29.3443514920207));
#79979=CARTESIAN_POINT('Ctrl Pts',(204.621451449481,9.83062399535249,29.3590262912858));
#79980=CARTESIAN_POINT('Ctrl Pts',(204.617293943785,9.82418039852081,29.4187816436883));
#79981=CARTESIAN_POINT('Ctrl Pts',(204.614082568928,9.82192689548017,29.4640689578767));
#79982=CARTESIAN_POINT('Ctrl Pts',(204.605180762538,9.82290861423555,29.5874750785639));
#79983=CARTESIAN_POINT('Ctrl Pts',(204.599389406086,9.83129804255859,29.6653197939489));
#79984=CARTESIAN_POINT('Ctrl Pts',(204.591428354726,9.85385487288358,29.7728677207805));
#79985=CARTESIAN_POINT('Ctrl Pts',(204.589153131017,9.86163712014357,29.8037034215908));
#79986=CARTESIAN_POINT('Ctrl Pts',(204.586321260908,9.8731481269769,29.8426031463734));
#79987=CARTESIAN_POINT('Ctrl Pts',(204.585713078908,9.87573204446398,29.8509895086234));
#79988=CARTESIAN_POINT('Ctrl Pts',(204.584730963057,9.88009160156128,29.8645965354617));
#79989=CARTESIAN_POINT('Ctrl Pts',(204.584354015249,9.88181054208747,29.8698348197347));
#79990=CARTESIAN_POINT('Ctrl Pts',(204.583651927284,9.88509935238766,29.8796245315236));
#79991=CARTESIAN_POINT('Ctrl Pts',(204.583326298668,9.88666044773974,29.8841787106893));
#79992=CARTESIAN_POINT('Ctrl Pts',(204.582459780755,9.89090916277573,29.896330057781));
#79993=CARTESIAN_POINT('Ctrl Pts',(204.581921709043,9.89364696839344,29.9039096164536));
#79994=CARTESIAN_POINT('Ctrl Pts',(204.579883315049,9.90439061225302,29.9327240656868));
#79995=CARTESIAN_POINT('Ctrl Pts',(204.57841037789,9.91293228610771,29.9537554258736));
#79996=CARTESIAN_POINT('Ctrl Pts',(204.572669531453,9.9490803079368,30.0358680904623));
#79997=CARTESIAN_POINT('Ctrl Pts',(204.568566189962,9.98127216169274,30.0947955784569));
#79998=CARTESIAN_POINT('Ctrl Pts',(204.561501206555,10.0442084259457,30.1897506761016));
#79999=CARTESIAN_POINT('Ctrl Pts',(204.558575493033,10.0724146180511,30.2272387055263));
#80000=CARTESIAN_POINT('Ctrl Pts',(204.55557810053,10.1027691095676,30.2629362959998));
#80001=CARTESIAN_POINT('Ctrl Pts',(198.520303559452,10.4906978680325,30.5595938614862));
#80002=CARTESIAN_POINT('Ctrl Pts',(198.54655243945,10.1411874905847,30.3915989467844));
#80003=CARTESIAN_POINT('Ctrl Pts',(198.599050199445,9.6273193758111,29.6852027538047));
#80004=CARTESIAN_POINT('Ctrl Pts',(198.677796839438,10.0915926961985,28.4524239122179));
#80005=CARTESIAN_POINT('Ctrl Pts',(198.756543479431,11.3767175053669,28.166546434716));
#80006=CARTESIAN_POINT('Ctrl Pts',(198.835290119423,12.3213447234544,29.0822494362045));
#80007=CARTESIAN_POINT('Ctrl Pts',(198.914036759416,12.0746318004869,30.3752124421159));
#80008=CARTESIAN_POINT('Ctrl Pts',(198.992783399409,10.8585526214878,30.8785952513234));
#80009=CARTESIAN_POINT('Ctrl Pts',(199.071530039402,9.77012615756758,30.1387612927136));
#80010=CARTESIAN_POINT('Ctrl Pts',(199.150276679395,9.79086261747825,28.822782934047));
#80011=CARTESIAN_POINT('Ctrl Pts',(199.229023319388,10.9021199481224,28.1176026645591));
#80012=CARTESIAN_POINT('Ctrl Pts',(199.307769959381,12.1016443134302,28.6591711062653));
#80013=CARTESIAN_POINT('Ctrl Pts',(199.386516599373,12.3076180711695,29.9590757800039));
#80014=CARTESIAN_POINT('Ctrl Pts',(199.465263239366,11.3342701062169,30.8449444178606));
#80015=CARTESIAN_POINT('Ctrl Pts',(199.544009879359,10.0594504089439,30.5178309587577));
#80016=CARTESIAN_POINT('Ctrl Pts',(199.622756519352,9.63289662650049,29.2727515562712));
#80017=CARTESIAN_POINT('Ctrl Pts',(199.701503159345,10.4393114539152,28.232624181157));
#80018=CARTESIAN_POINT('Ctrl Pts',(199.780249799338,11.7514020703729,28.3355223410407));
#80019=CARTESIAN_POINT('Ctrl Pts',(199.858996439331,12.3858154013911,29.4886440980506));
#80020=CARTESIAN_POINT('Ctrl Pts',(199.937743079323,11.7703842663141,30.6520075205645));
#80021=CARTESIAN_POINT('Ctrl Pts',(200.016489719316,10.4601560671557,30.7763940594563));
#80022=CARTESIAN_POINT('Ctrl Pts',(200.095236359309,9.63680435061106,29.7496214849068));
#80023=CARTESIAN_POINT('Ctrl Pts',(200.173982999302,10.0428966880961,28.4977193452295));
#80024=CARTESIAN_POINT('Ctrl Pts',(200.252729639295,11.3121849809262,28.1497578732641));
#80025=CARTESIAN_POINT('Ctrl Pts',(200.331476279288,12.2999187025004,29.0195578811959));
#80026=CARTESIAN_POINT('Ctrl Pts',(200.41022291928,12.1152768251165,30.3226608448567));
#80027=CARTESIAN_POINT('Ctrl Pts',(200.488969559273,10.9247848643951,30.8838193328497));
#80028=CARTESIAN_POINT('Ctrl Pts',(200.567716199266,9.80212821472357,30.1969336041217));
#80029=CARTESIAN_POINT('Ctrl Pts',(200.646462839259,9.75981270382478,28.8814947592023));
#80030=CARTESIAN_POINT('Ctrl Pts',(200.725209479252,10.8360020047419,28.1238757613965));
#80031=CARTESIAN_POINT('Ctrl Pts',(200.803956119245,12.0600984382385,28.6073608994928));
#80032=CARTESIAN_POINT('Ctrl Pts',(200.882702759238,12.3281092805904,29.8959027675046));
#80033=CARTESIAN_POINT('Ctrl Pts',(200.96144939923,11.3983198990878,30.8273863493732));
#80034=CARTESIAN_POINT('Ctrl Pts',(201.040196039223,10.1092922596587,30.5617217073256));
#80035=CARTESIAN_POINT('Ctrl Pts',(201.118942679216,9.62357948773663,29.3385074740712));
#80036=CARTESIAN_POINT('Ctrl Pts',(201.197689319209,10.3792380561133,28.2609407312269));
#80037=CARTESIAN_POINT('Ctrl Pts',(201.276435959202,11.6947517555518,28.3008614505954));
#80038=CARTESIAN_POINT('Ctrl Pts',(201.355182599195,12.3836801125892,29.4222657827231));
#80039=CARTESIAN_POINT('Ctrl Pts',(201.433929239188,11.8246898135138,30.613777344893));
#80040=CARTESIAN_POINT('Ctrl Pts',(201.51267587918,10.5219251446065,30.8007911804555));
#80041=CARTESIAN_POINT('Ctrl Pts',(201.591422519173,9.65032843542909,29.814642543689));
#80042=CARTESIAN_POINT('Ctrl Pts',(201.670169159166,9.99597862438151,28.544722898939));
#80043=CARTESIAN_POINT('Ctrl Pts',(201.748915799159,11.2471394110297,28.136352181087));
#80044=CARTESIAN_POINT('Ctrl Pts',(201.827662439152,12.2754091704247,28.9578333185203));
#80045=CARTESIAN_POINT('Ctrl Pts',(201.906409079145,12.153408080749,30.2682857943327));
#80046=CARTESIAN_POINT('Ctrl Pts',(201.985155719137,10.9911669464399,30.8858337705782));
#80047=CARTESIAN_POINT('Ctrl Pts',(202.06390235913,9.83689219990197,30.2535207414938));
#80048=CARTESIAN_POINT('Ctrl Pts',(202.142648999123,9.73160551758984,28.9416195745714));
#80049=CARTESIAN_POINT('Ctrl Pts',(202.221395639116,10.7702632509767,28.1333126587772));
#80050=CARTESIAN_POINT('Ctrl Pts',(202.300142279109,12.0161168329507,28.5575988941514));
#80051=CARTESIAN_POINT('Ctrl Pts',(202.378888919102,12.345551120398,29.8318214051353));
#80052=CARTESIAN_POINT('Ctrl Pts',(202.457635559095,11.461454671499,30.8067795715665));
#80053=CARTESIAN_POINT('Ctrl Pts',(202.536382199087,10.1611797372155,30.6031744328302));
#80054=CARTESIAN_POINT('Ctrl Pts',(202.61512883908,9.61742319582523,29.4046341619453));
#80055=CARTESIAN_POINT('Ctrl Pts',(202.693875479073,10.3205902545797,28.2921027939644));
#80056=CARTESIAN_POINT('Ctrl Pts',(202.772622119066,11.6365059455802,28.2689543291454));
#80057=CARTESIAN_POINT('Ctrl Pts',(202.851368759059,12.3783672456924,29.3560659924908));
#80058=CARTESIAN_POINT('Ctrl Pts',(202.930115399052,11.8771014781942,30.5729894032756));
#80059=CARTESIAN_POINT('Ctrl Pts',(203.008862039045,10.5847921103831,30.8222010704512));
#80060=CARTESIAN_POINT('Ctrl Pts',(203.087608679037,9.66695200530575,29.8789410329763));
#80061=CARTESIAN_POINT('Ctrl Pts',(203.16635531903,9.9513662702466,28.5939202220822));
#80062=CARTESIAN_POINT('Ctrl Pts',(203.245101959023,11.1815262916617,28.1260780713519));
#80063=CARTESIAN_POINT('Ctrl Pts',(203.323848599016,12.2479706941989,28.8973538263122));
#80064=CARTESIAN_POINT('Ctrl Pts',(203.402595239009,12.1888905644702,30.2121463982623));
#80065=CARTESIAN_POINT('Ctrl Pts',(203.481341879002,11.057569313348,30.8846656706159));
#80066=CARTESIAN_POINT('Ctrl Pts',(203.560088518995,9.87432723218788,30.3083774508533));
#80067=CARTESIAN_POINT('Ctrl Pts',(203.638835158987,9.70631116638201,29.0030266693794));
#80068=CARTESIAN_POINT('Ctrl Pts',(203.71758179898,10.7050520820644,28.1458881738925));
#80069=CARTESIAN_POINT('Ctrl Pts',(203.796328438973,11.9698017408791,28.5100009735364));
#80070=CARTESIAN_POINT('Ctrl Pts',(203.875075078966,12.3599029382575,29.7669782619617));
#80071=CARTESIAN_POINT('Ctrl Pts',(203.953821718959,11.5235297221299,30.7831713140073));
#80072=CARTESIAN_POINT('Ctrl Pts',(204.032568358952,10.2149935501509,30.6420947708184));
#80073=CARTESIAN_POINT('Ctrl Pts',(204.111314998944,9.61444194280345,29.4709777328597));
#80074=CARTESIAN_POINT('Ctrl Pts',(204.190061638937,10.2635027270343,28.3260431590116));
#80075=CARTESIAN_POINT('Ctrl Pts',(204.26880827893,11.5767983600888,28.2398651595848));
#80076=CARTESIAN_POINT('Ctrl Pts',(204.347554918923,12.3698891101204,29.2902156265541));
#80077=CARTESIAN_POINT('Ctrl Pts',(204.426301558916,11.9274986610999,30.5296982380858));
#80078=CARTESIAN_POINT('Ctrl Pts',(204.505048198909,10.648613086735,30.8406556465544));
#80079=CARTESIAN_POINT('Ctrl Pts',(204.583794838902,9.68663581581289,29.9422012341082));
#80080=CARTESIAN_POINT('Ctrl Pts',(204.662541478895,9.90916386048687,28.6455463696896));
#80081=CARTESIAN_POINT('Ctrl Pts',(204.741288118887,11.1154852624214,28.1182320587536));
#80082=CARTESIAN_POINT('Ctrl Pts',(204.82004122376,12.2177166671994,28.8398027453881));
#80083=CARTESIAN_POINT('Ctrl Pts',(204.872545448635,12.2194357483118,29.7134875651393));
#80084=CARTESIAN_POINT('Ctrl Pts',(204.898800793512,12.0361954097,30.0553619354564));
#80085=CARTESIAN_POINT('Ctrl Pts',(198.576061721773,10.448859910947,30.6466369734669));
#80086=CARTESIAN_POINT('Ctrl Pts',(198.602310601771,10.0706380884556,30.4648416766526));
#80087=CARTESIAN_POINT('Ctrl Pts',(198.654808361766,9.51455693198427,29.7004167189139));
#80088=CARTESIAN_POINT('Ctrl Pts',(198.733555001759,10.0169691998355,28.3663680317231));
#80089=CARTESIAN_POINT('Ctrl Pts',(198.812301641752,11.4076639511671,28.0570064003472));
#80090=CARTESIAN_POINT('Ctrl Pts',(198.891048281745,12.4298900453077,29.0479322223869));
#80091=CARTESIAN_POINT('Ctrl Pts',(198.969794921737,12.1629102433391,30.4471090596551));
#80092=CARTESIAN_POINT('Ctrl Pts',(199.048541561731,10.8469330562424,30.9918435676819));
#80093=CARTESIAN_POINT('Ctrl Pts',(199.127288201723,9.6690949507249,30.1912340115086));
#80094=CARTESIAN_POINT('Ctrl Pts',(199.206034841716,9.69153486142714,28.7671511650745));
#80095=CARTESIAN_POINT('Ctrl Pts',(199.284781481709,10.8940793349912,28.0040420160462));
#80096=CARTESIAN_POINT('Ctrl Pts',(199.363528121702,12.1921417698824,28.5900990153309));
#80097=CARTESIAN_POINT('Ctrl Pts',(199.442274761695,12.4150357812317,29.9967877619047));
#80098=CARTESIAN_POINT('Ctrl Pts',(199.521021401688,11.3617295992783,30.9554283983997));
#80099=CARTESIAN_POINT('Ctrl Pts',(199.59976804168,9.98218650023936,30.6014433477502));
#80100=CARTESIAN_POINT('Ctrl Pts',(199.678514681673,9.52059234053389,29.2540836378792));
#80101=CARTESIAN_POINT('Ctrl Pts',(199.757261321666,10.3932522253021,28.1285122762744));
#80102=CARTESIAN_POINT('Ctrl Pts',(199.836007961659,11.8131279607647,28.2398632749097));
#80103=CARTESIAN_POINT('Ctrl Pts',(199.914754601652,12.4996568358807,29.4877112377529));
#80104=CARTESIAN_POINT('Ctrl Pts',(199.993501241645,11.8336694988909,30.7466421945276));
#80105=CARTESIAN_POINT('Ctrl Pts',(200.072247881638,10.4158091738726,30.8812467913257));
#80106=CARTESIAN_POINT('Ctrl Pts',(200.15099452163,9.52482107487274,29.7701272953434));
#80107=CARTESIAN_POINT('Ctrl Pts',(200.229741161623,9.96427293065161,28.4153843766718));
#80108=CARTESIAN_POINT('Ctrl Pts',(200.308487801616,11.3378302335473,28.038838698559));
#80109=CARTESIAN_POINT('Ctrl Pts',(200.387234441609,12.406703927765,28.9800907054531));
#80110=CARTESIAN_POINT('Ctrl Pts',(200.465981081602,12.2068941599339,30.3902404738483));
#80111=CARTESIAN_POINT('Ctrl Pts',(200.544727721595,10.9186061201527,30.9974967950628));
#80112=CARTESIAN_POINT('Ctrl Pts',(200.623474361587,9.70372590065377,30.254185039744));
#80113=CARTESIAN_POINT('Ctrl Pts',(200.70222100158,9.65793427132171,28.8306860268263));
#80114=CARTESIAN_POINT('Ctrl Pts',(200.780967641573,10.8225299600418,28.0108304328474));
#80115=CARTESIAN_POINT('Ctrl Pts',(200.859714281566,12.1471829999977,28.5340327234736));
#80116=CARTESIAN_POINT('Ctrl Pts',(200.938460921559,12.4372102947006,29.9284252368941));
#80117=CARTESIAN_POINT('Ctrl Pts',(201.017207561552,11.4310409300796,30.9364279764058));
#80118=CARTESIAN_POINT('Ctrl Pts',(201.095954201545,10.036122740277,30.648939616774));
#80119=CARTESIAN_POINT('Ctrl Pts',(201.174700841537,9.51050982101215,29.3252412477091));
#80120=CARTESIAN_POINT('Ctrl Pts',(201.25344748153,10.3282439409536,28.1591549634882));
#80121=CARTESIAN_POINT('Ctrl Pts',(201.332194121523,11.7518239575108,28.2023550748697));
#80122=CARTESIAN_POINT('Ctrl Pts',(201.410940761516,12.4973461381895,29.4158801019212));
#80123=CARTESIAN_POINT('Ctrl Pts',(201.489687401509,11.892436117448,30.7052715009815));
#80124=CARTESIAN_POINT('Ctrl Pts',(201.568434041502,10.4826524339143,30.9076480777059));
#80125=CARTESIAN_POINT('Ctrl Pts',(201.647180681494,9.5394561310469,29.8404896792376));
#80126=CARTESIAN_POINT('Ctrl Pts',(201.725927321488,9.91350065975225,28.4662491603656));
#80127=CARTESIAN_POINT('Ctrl Pts',(201.80467396148,11.2674413250092,28.0243317606992));
#80128=CARTESIAN_POINT('Ctrl Pts',(201.883420601473,12.380180996006,28.9132956169691));
#80129=CARTESIAN_POINT('Ctrl Pts',(201.962167241466,12.2481578073955,30.3313986424342));
#80130=CARTESIAN_POINT('Ctrl Pts',(202.040913881459,10.9904413321285,30.9996767140528));
#80131=CARTESIAN_POINT('Ctrl Pts',(202.119660521452,9.74134566441371,30.3154206756722));
#80132=CARTESIAN_POINT('Ctrl Pts',(202.198407161445,9.62740993192143,28.8957499525728));
#80133=CARTESIAN_POINT('Ctrl Pts',(202.277153801437,10.7513909242313,28.0210425488711));
#80134=CARTESIAN_POINT('Ctrl Pts',(202.35590044143,12.0995884105907,28.4801828879167));
#80135=CARTESIAN_POINT('Ctrl Pts',(202.434647081423,12.4560849401055,29.8590797432351));
#80136=CARTESIAN_POINT('Ctrl Pts',(202.513393721416,11.49936207367,30.9141284008834));
#80137=CARTESIAN_POINT('Ctrl Pts',(202.592140361409,10.0922726505296,30.6937975849468));
#80138=CARTESIAN_POINT('Ctrl Pts',(202.670887001402,9.50384780438328,29.3968000854914));
#80139=CARTESIAN_POINT('Ctrl Pts',(202.749633641394,10.2647783622114,28.1928769154577));
#80140=CARTESIAN_POINT('Ctrl Pts',(202.828380281387,11.68879339298,28.1678268593889));
#80141=CARTESIAN_POINT('Ctrl Pts',(202.90712692138,12.4915968319313,29.3442421565958));
#80142=CARTESIAN_POINT('Ctrl Pts',(202.985873561373,11.9491532755479,30.661132927109));
#80143=CARTESIAN_POINT('Ctrl Pts',(203.064620201366,10.5506837711931,30.9308167391706));
#80144=CARTESIAN_POINT('Ctrl Pts',(203.143366841359,9.55744528759493,29.9100701362738));
#80145=CARTESIAN_POINT('Ctrl Pts',(203.222113481352,9.86522350698284,28.5194879264268));
#80146=CARTESIAN_POINT('Ctrl Pts',(203.300860121344,11.1964382441623,28.0132136573202));
#80147=CARTESIAN_POINT('Ctrl Pts',(203.379606761337,12.3504885143112,28.8478478785262));
#80148=CARTESIAN_POINT('Ctrl Pts',(203.45835340133,12.2865550926423,30.2706475286895));
#80149=CARTESIAN_POINT('Ctrl Pts',(203.537100041323,11.0622984953209,30.9984126574607));
#80150=CARTESIAN_POINT('Ctrl Pts',(203.615846681316,9.78185589543917,30.3747837330477));
#80151=CARTESIAN_POINT('Ctrl Pts',(203.694593321309,9.60003771000796,28.9622014939599));
#80152=CARTESIAN_POINT('Ctrl Pts',(203.773339961301,10.6808228131128,28.0346511126009));
#80153=CARTESIAN_POINT('Ctrl Pts',(203.852086601294,12.0494686440188,28.4286749114918));
#80154=CARTESIAN_POINT('Ctrl Pts',(203.930833241287,12.4716157256189,29.788909890293));
#80155=CARTESIAN_POINT('Ctrl Pts',(204.00957988128,11.5665364418599,30.888580781196));
#80156=CARTESIAN_POINT('Ctrl Pts',(204.088326521273,10.150507140024,30.7359151360001));
#80157=CARTESIAN_POINT('Ctrl Pts',(204.167073161266,9.50062164852651,29.4685936227394));
#80158=CARTESIAN_POINT('Ctrl Pts',(204.245819801259,10.2030012302491,28.2296054006543));
#80159=CARTESIAN_POINT('Ctrl Pts',(204.324566441252,11.6241809715519,28.1363480838334));
#80160=CARTESIAN_POINT('Ctrl Pts',(204.403313081244,12.4824222377153,29.2729823399399));
#80161=CARTESIAN_POINT('Ctrl Pts',(204.482059721237,12.0036904669934,30.6142854958097));
#80162=CARTESIAN_POINT('Ctrl Pts',(204.56080636123,10.6197474887435,30.9507873147457));
#80163=CARTESIAN_POINT('Ctrl Pts',(204.639553001223,9.57874607625232,29.9785270122555));
#80164=CARTESIAN_POINT('Ctrl Pts',(204.718299641216,9.81955426977905,28.5753550390969));
#80165=CARTESIAN_POINT('Ctrl Pts',(204.797046281209,11.1249721016664,28.0047231134747));
#80166=CARTESIAN_POINT('Ctrl Pts',(204.875799386081,12.3177491910527,28.7855691133793));
#80167=CARTESIAN_POINT('Ctrl Pts',(204.928303610957,12.319609490584,29.7310250601308));
#80168=CARTESIAN_POINT('Ctrl Pts',(204.954558955833,12.121316394597,30.1009835956933));
#80169=CARTESIAN_POINT('Ctrl Pts',(198.631819884095,10.4070219538616,30.7336800854477));
#80170=CARTESIAN_POINT('Ctrl Pts',(198.658068764092,10.0000886863265,30.5380844065209));
#80171=CARTESIAN_POINT('Ctrl Pts',(198.710566524088,9.40179448815744,29.7156306840231));
#80172=CARTESIAN_POINT('Ctrl Pts',(198.78931316408,9.94234570347243,28.2803121512281));
#80173=CARTESIAN_POINT('Ctrl Pts',(198.868059804073,11.4386103969674,27.9474663659784));
#80174=CARTESIAN_POINT('Ctrl Pts',(198.946806444066,12.5384353671611,29.0136150085693));
#80175=CARTESIAN_POINT('Ctrl Pts',(199.025553084059,12.2511886861915,30.5190056771942));
#80176=CARTESIAN_POINT('Ctrl Pts',(199.104299724052,10.8353134909969,31.1050918840403));
#80177=CARTESIAN_POINT('Ctrl Pts',(199.183046364045,9.56806374388221,30.2437067303035));
#80178=CARTESIAN_POINT('Ctrl Pts',(199.261793004038,9.59220710537601,28.7115193961018));
#80179=CARTESIAN_POINT('Ctrl Pts',(199.34053964403,10.8860387218602,27.8904813675333));
#80180=CARTESIAN_POINT('Ctrl Pts',(199.419286284023,12.2826392263346,28.5210269243967));
#80181=CARTESIAN_POINT('Ctrl Pts',(199.498032924016,12.522453491294,30.0344997438053));
#80182=CARTESIAN_POINT('Ctrl Pts',(199.576779564009,11.3891890923396,31.0659123789388));
#80183=CARTESIAN_POINT('Ctrl Pts',(199.655526204002,9.90492259153486,30.6850557367427));
#80184=CARTESIAN_POINT('Ctrl Pts',(199.734272843994,9.40828805456728,29.2354157194871));
#80185=CARTESIAN_POINT('Ctrl Pts',(199.813019483988,10.3471929966891,28.0244003713917));
#80186=CARTESIAN_POINT('Ctrl Pts',(199.89176612398,11.8748538511566,28.1442042087787));
#80187=CARTESIAN_POINT('Ctrl Pts',(199.970512763973,12.6134982703702,29.4867783774552));
#80188=CARTESIAN_POINT('Ctrl Pts',(200.049259403966,11.8969547314676,30.8412768684909));
#80189=CARTESIAN_POINT('Ctrl Pts',(200.128006043959,10.3714622805895,30.986099523195));
#80190=CARTESIAN_POINT('Ctrl Pts',(200.206752683952,9.41283779913442,29.7906331057803));
#80191=CARTESIAN_POINT('Ctrl Pts',(200.285499323945,9.88564917320709,28.3330494081142));
#80192=CARTESIAN_POINT('Ctrl Pts',(200.364245963937,11.3634754861682,27.9279195238539));
#80193=CARTESIAN_POINT('Ctrl Pts',(200.44299260393,12.5134891530294,28.9406235297101));
#80194=CARTESIAN_POINT('Ctrl Pts',(200.521739243923,12.2985114947512,30.4578201028399));
#80195=CARTESIAN_POINT('Ctrl Pts',(200.600485883916,10.9124273759101,31.1111742572759));
#80196=CARTESIAN_POINT('Ctrl Pts',(200.679232523909,9.60532358658397,30.3114364753665));
#80197=CARTESIAN_POINT('Ctrl Pts',(200.757979163902,9.55605583881862,28.7798772944504));
#80198=CARTESIAN_POINT('Ctrl Pts',(200.836725803895,10.8090579153417,27.8977851042985));
#80199=CARTESIAN_POINT('Ctrl Pts',(200.915472443887,12.2342675617569,28.4607045474545));
#80200=CARTESIAN_POINT('Ctrl Pts',(200.99421908388,12.5463113088109,29.9609477062835));
#80201=CARTESIAN_POINT('Ctrl Pts',(201.072965723873,11.4637619610715,31.0454696034384));
#80202=CARTESIAN_POINT('Ctrl Pts',(201.151712363866,9.96295322089544,30.7361575262224));
#80203=CARTESIAN_POINT('Ctrl Pts',(201.230459003859,9.39744015428766,29.3119750213469));
#80204=CARTESIAN_POINT('Ctrl Pts',(201.309205643852,10.2772498257939,28.0573691957494));
#80205=CARTESIAN_POINT('Ctrl Pts',(201.387952283845,11.8088961594698,28.1038486991439));
#80206=CARTESIAN_POINT('Ctrl Pts',(201.466698923837,12.6110121637899,29.4094944211192));
#80207=CARTESIAN_POINT('Ctrl Pts',(201.54544556383,11.9601824213823,30.7967656570699));
#80208=CARTESIAN_POINT('Ctrl Pts',(201.624192203823,10.4433797232223,31.0145049749563));
#80209=CARTESIAN_POINT('Ctrl Pts',(201.702938843816,9.42858382666472,29.8663368147861));
#80210=CARTESIAN_POINT('Ctrl Pts',(201.781685483809,9.83102269512299,28.3877754217921));
#80211=CARTESIAN_POINT('Ctrl Pts',(201.860432123801,11.2877432389887,27.9123113403115));
#80212=CARTESIAN_POINT('Ctrl Pts',(201.939178763795,12.4849528215873,28.868757915418));
#80213=CARTESIAN_POINT('Ctrl Pts',(202.017925403787,12.342907534042,30.3945114905358));
#80214=CARTESIAN_POINT('Ctrl Pts',(202.09667204378,10.9897157178171,31.1135196575275));
#80215=CARTESIAN_POINT('Ctrl Pts',(202.175418683773,9.64579912892547,30.3773206098504));
#80216=CARTESIAN_POINT('Ctrl Pts',(202.254165323766,9.52321434625301,28.8498803305741));
#80217=CARTESIAN_POINT('Ctrl Pts',(202.332911963759,10.732518597486,27.9087724389652));
#80218=CARTESIAN_POINT('Ctrl Pts',(202.411658603752,12.1830599882308,28.4027668816818));
#80219=CARTESIAN_POINT('Ctrl Pts',(202.490405243744,12.5666187598128,29.8863380813349));
#80220=CARTESIAN_POINT('Ctrl Pts',(202.569151883737,11.5372694758411,31.0214772302005));
#80221=CARTESIAN_POINT('Ctrl Pts',(202.64789852373,10.0233655638437,30.7844207370633));
#80222=CARTESIAN_POINT('Ctrl Pts',(202.726645163723,9.39027241294133,29.3889660090376));
#80223=CARTESIAN_POINT('Ctrl Pts',(202.805391803716,10.208966469843,28.093651036951));
#80224=CARTESIAN_POINT('Ctrl Pts',(202.884138443709,11.7410808403797,28.0666993896324));
#80225=CARTESIAN_POINT('Ctrl Pts',(202.962885083701,12.6048264181704,29.3324183207009));
#80226=CARTESIAN_POINT('Ctrl Pts',(203.041631723694,12.0212050729015,30.7492764509423));
#80227=CARTESIAN_POINT('Ctrl Pts',(203.120378363687,10.5165754320031,31.0394324078902));
#80228=CARTESIAN_POINT('Ctrl Pts',(203.19912500368,9.4479385698841,29.9411992395711));
#80229=CARTESIAN_POINT('Ctrl Pts',(203.277871643673,9.7790807437191,28.4450556307714));
#80230=CARTESIAN_POINT('Ctrl Pts',(203.356618283666,11.2113501966631,27.9003492432886));
#80231=CARTESIAN_POINT('Ctrl Pts',(203.435364923658,12.4530063344234,28.7983419307402));
#80232=CARTESIAN_POINT('Ctrl Pts',(203.514111563651,12.3842196208143,30.3291486591167));
#80233=CARTESIAN_POINT('Ctrl Pts',(203.592858203644,11.0670276772939,31.1121596443056));
#80234=CARTESIAN_POINT('Ctrl Pts',(203.671604843637,9.68938455869046,30.4411900152422));
#80235=CARTESIAN_POINT('Ctrl Pts',(203.75035148363,9.49376425363389,28.9213763185404));
#80236=CARTESIAN_POINT('Ctrl Pts',(203.829098123623,10.6565935441613,27.9234140513093));
#80237=CARTESIAN_POINT('Ctrl Pts',(203.907844763616,12.1291355471585,28.3473488494473));
#80238=CARTESIAN_POINT('Ctrl Pts',(203.986591403609,12.5833285129804,29.8108415186245));
#80239=CARTESIAN_POINT('Ctrl Pts',(204.065338043601,11.60954316159,30.9939902483847));
#80240=CARTESIAN_POINT('Ctrl Pts',(204.144084683594,10.086020729897,30.8297355011819));
#80241=CARTESIAN_POINT('Ctrl Pts',(204.222831323587,9.38680135424956,29.466209512619));
#80242=CARTESIAN_POINT('Ctrl Pts',(204.30157796358,10.1424997334639,28.1331676422972));
#80243=CARTESIAN_POINT('Ctrl Pts',(204.380324603573,11.6715635830151,28.0328310080821));
#80244=CARTESIAN_POINT('Ctrl Pts',(204.459071243566,12.5949553653103,29.2557490533256));
#80245=CARTESIAN_POINT('Ctrl Pts',(204.537817883559,12.0798822728867,30.6988727535335));
#80246=CARTESIAN_POINT('Ctrl Pts',(204.616564523551,10.590881890752,31.0609189829369));
#80247=CARTESIAN_POINT('Ctrl Pts',(204.695311163544,9.47085633669177,30.0148527904026));
#80248=CARTESIAN_POINT('Ctrl Pts',(204.774057803537,9.72994467907122,28.5051637085043));
#80249=CARTESIAN_POINT('Ctrl Pts',(204.85280444353,11.1344589409116,27.8912141681958));
#80250=CARTESIAN_POINT('Ctrl Pts',(204.931557548403,12.417781714906,28.7313354813706));
#80251=CARTESIAN_POINT('Ctrl Pts',(204.984061773278,12.4197832328561,29.7485625551224));
#80252=CARTESIAN_POINT('Ctrl Pts',(205.010317118156,12.2064373794939,30.1466052559301));
#80253=CARTESIAN_POINT('Ctrl Pts',(198.687578046416,10.3651839967761,30.8207231974284));
#80254=CARTESIAN_POINT('Ctrl Pts',(198.713826926414,9.92953928419742,30.6113271363891));
#80255=CARTESIAN_POINT('Ctrl Pts',(198.766324686409,9.2890320443306,29.7308446491323));
#80256=CARTESIAN_POINT('Ctrl Pts',(198.845071326402,9.86772220710937,28.1942562707332));
#80257=CARTESIAN_POINT('Ctrl Pts',(198.923817966395,11.4695568427676,27.8379263316095));
#80258=CARTESIAN_POINT('Ctrl Pts',(199.002564606388,12.6469806890144,28.9792977947516));
#80259=CARTESIAN_POINT('Ctrl Pts',(199.08131124638,12.3394671290437,30.5909022947333));
#80260=CARTESIAN_POINT('Ctrl Pts',(199.160057886373,10.8236939257515,31.2183402003988));
#80261=CARTESIAN_POINT('Ctrl Pts',(199.238804526366,9.46703253703953,30.2961794490986));
#80262=CARTESIAN_POINT('Ctrl Pts',(199.317551166359,9.49287934932489,28.6558876271292));
#80263=CARTESIAN_POINT('Ctrl Pts',(199.396297806352,10.8779981087292,27.7769207190204));
#80264=CARTESIAN_POINT('Ctrl Pts',(199.475044446344,12.3731366827867,28.4519548334623));
#80265=CARTESIAN_POINT('Ctrl Pts',(199.553791086337,12.6298712013562,30.0722117257062));
#80266=CARTESIAN_POINT('Ctrl Pts',(199.63253772633,11.4166485854008,31.1763963594777));
#80267=CARTESIAN_POINT('Ctrl Pts',(199.711284366323,9.82765868283031,30.7686681257351));
#80268=CARTESIAN_POINT('Ctrl Pts',(199.790031006316,9.29598376860071,29.2167478010951));
#80269=CARTESIAN_POINT('Ctrl Pts',(199.868777646309,10.301133768076,27.9202884665091));
#80270=CARTESIAN_POINT('Ctrl Pts',(199.947524286302,11.9365797415486,28.0485451426477));
#80271=CARTESIAN_POINT('Ctrl Pts',(200.026270926294,12.7273397048599,29.4858455171576));
#80272=CARTESIAN_POINT('Ctrl Pts',(200.105017566287,11.9602399640443,30.9359115424541));
#80273=CARTESIAN_POINT('Ctrl Pts',(200.18376420628,10.3271153873065,31.0909522550645));
#80274=CARTESIAN_POINT('Ctrl Pts',(200.262510846273,9.30085452339609,29.811138916217));
#80275=CARTESIAN_POINT('Ctrl Pts',(200.341257486266,9.80702541576257,28.2507144395565));
#80276=CARTESIAN_POINT('Ctrl Pts',(200.420004126259,11.3891207387892,27.8170003491488));
#80277=CARTESIAN_POINT('Ctrl Pts',(200.498750766252,12.6202743782939,28.9011563539673));
#80278=CARTESIAN_POINT('Ctrl Pts',(200.577497406244,12.3901288295685,30.5253997318316));
#80279=CARTESIAN_POINT('Ctrl Pts',(200.656244046237,10.9062486316675,31.2248517194891));
#80280=CARTESIAN_POINT('Ctrl Pts',(200.73499068623,9.50692127251416,30.3686879109888));
#80281=CARTESIAN_POINT('Ctrl Pts',(200.813737326223,9.45417740631555,28.7290685620745));
#80282=CARTESIAN_POINT('Ctrl Pts',(200.892483966216,10.7955858706416,27.7847397757495));
#80283=CARTESIAN_POINT('Ctrl Pts',(200.971230606209,12.3213521235159,28.3873763714354));
#80284=CARTESIAN_POINT('Ctrl Pts',(201.049977246202,12.6554123229211,29.993470175673));
#80285=CARTESIAN_POINT('Ctrl Pts',(201.128723886194,11.4964829920634,31.1545112304711));
#80286=CARTESIAN_POINT('Ctrl Pts',(201.207470526187,9.88978370151384,30.8233754356706));
#80287=CARTESIAN_POINT('Ctrl Pts',(201.28621716618,9.28437048756318,29.2987087949847));
#80288=CARTESIAN_POINT('Ctrl Pts',(201.364963806173,10.2262557106342,27.9555834280108));
#80289=CARTESIAN_POINT('Ctrl Pts',(201.443710446166,11.8659683614289,28.0053423234181));
#80290=CARTESIAN_POINT('Ctrl Pts',(201.522457086159,12.7246781893901,29.4031087403172));
#80291=CARTESIAN_POINT('Ctrl Pts',(201.601203726151,12.0279287253164,30.8882598131583));
#80292=CARTESIAN_POINT('Ctrl Pts',(201.679950366144,10.4041070125303,31.1213618722067));
#80293=CARTESIAN_POINT('Ctrl Pts',(201.758697006137,9.31771152228255,29.8921839503347));
#80294=CARTESIAN_POINT('Ctrl Pts',(201.83744364613,9.74854473049371,28.3093016832186));
#80295=CARTESIAN_POINT('Ctrl Pts',(201.916190286123,11.3080451529682,27.8002909199237));
#80296=CARTESIAN_POINT('Ctrl Pts',(201.994936926116,12.5897246471684,28.8242202138668));
#80297=CARTESIAN_POINT('Ctrl Pts',(202.073683566109,12.4376572606885,30.4576243386374));
#80298=CARTESIAN_POINT('Ctrl Pts',(202.152430206102,10.9889901035058,31.227362601002));
#80299=CARTESIAN_POINT('Ctrl Pts',(202.231176846094,9.55025259343721,30.4392205440286));
#80300=CARTESIAN_POINT('Ctrl Pts',(202.309923486087,9.4190187605846,28.8040107085755));
#80301=CARTESIAN_POINT('Ctrl Pts',(202.38867012608,10.7136462707406,27.7965023290593));
#80302=CARTESIAN_POINT('Ctrl Pts',(202.467416766073,12.266531565871,28.325350875447));
#80303=CARTESIAN_POINT('Ctrl Pts',(202.546163406066,12.6771525795203,29.9135964194346));
#80304=CARTESIAN_POINT('Ctrl Pts',(202.624910046059,11.5751768780122,31.1288260595174));
#80305=CARTESIAN_POINT('Ctrl Pts',(202.703656686051,9.95445847715783,30.8750438891797));
#80306=CARTESIAN_POINT('Ctrl Pts',(202.782403326044,9.27669702149938,29.3811319325837));
#80307=CARTESIAN_POINT('Ctrl Pts',(202.861149966037,10.1531545774746,27.9944251584444));
#80308=CARTESIAN_POINT('Ctrl Pts',(202.93989660603,11.7933682877795,27.9655719198759));
#80309=CARTESIAN_POINT('Ctrl Pts',(203.018643246023,12.7180560044093,29.320594484806));
#80310=CARTESIAN_POINT('Ctrl Pts',(203.097389886016,12.0932568702551,30.8374199747755));
#80311=CARTESIAN_POINT('Ctrl Pts',(203.176136526008,10.4824670928131,31.1480480766096));
#80312=CARTESIAN_POINT('Ctrl Pts',(203.254883166001,9.33843185217328,29.9723283428685));
#80313=CARTESIAN_POINT('Ctrl Pts',(203.333629805994,9.69293798045533,28.3706233351159));
#80314=CARTESIAN_POINT('Ctrl Pts',(203.412376445987,11.2262621491638,27.787484829257));
#80315=CARTESIAN_POINT('Ctrl Pts',(203.49112308598,12.5555241545356,28.7488359829542));
#80316=CARTESIAN_POINT('Ctrl Pts',(203.569869725973,12.4818841489864,30.3876497895438));
#80317=CARTESIAN_POINT('Ctrl Pts',(203.648616365966,11.0717568592669,31.2259066311503));
#80318=CARTESIAN_POINT('Ctrl Pts',(203.727363005958,9.59691322194175,30.5075962974366));
#80319=CARTESIAN_POINT('Ctrl Pts',(203.806109645951,9.38749079725985,28.8805511431208));
#80320=CARTESIAN_POINT('Ctrl Pts',(203.884856285944,10.6323642752097,27.8121769900177));
#80321=CARTESIAN_POINT('Ctrl Pts',(203.963602925937,12.2088024502983,28.2660227874026));
#80322=CARTESIAN_POINT('Ctrl Pts',(204.04234956593,12.6950413003419,29.8327731469559));
#80323=CARTESIAN_POINT('Ctrl Pts',(204.121096205923,11.65254988132,31.0993997155733));
#80324=CARTESIAN_POINT('Ctrl Pts',(204.199842845915,10.0215343197701,30.9235558663637));
#80325=CARTESIAN_POINT('Ctrl Pts',(204.278589485908,9.27298105997262,29.4638254024987));
#80326=CARTESIAN_POINT('Ctrl Pts',(204.357336125901,10.0819982366787,28.0367298839401));
#80327=CARTESIAN_POINT('Ctrl Pts',(204.436082765894,11.7189461944783,27.9293139323307));
#80328=CARTESIAN_POINT('Ctrl Pts',(204.514829405887,12.7074884929052,29.2385157667114));
#80329=CARTESIAN_POINT('Ctrl Pts',(204.59357604588,12.1560740787801,30.7834600112573));
#80330=CARTESIAN_POINT('Ctrl Pts',(204.672322685873,10.5620162927605,31.1710506511282));
#80331=CARTESIAN_POINT('Ctrl Pts',(204.751069325865,9.36296659713122,30.0511785685499));
#80332=CARTESIAN_POINT('Ctrl Pts',(204.829815965859,9.6403350883634,28.4349723779117));
#80333=CARTESIAN_POINT('Ctrl Pts',(204.908562605851,11.1439457801568,27.7777052229169));
#80334=CARTESIAN_POINT('Ctrl Pts',(204.987315710724,12.5178142387592,28.6771018493619));
#80335=CARTESIAN_POINT('Ctrl Pts',(205.039819935599,12.5199569751282,29.7661000501139));
#80336=CARTESIAN_POINT('Ctrl Pts',(205.066075280477,12.2915583643908,30.1922269161671));
#80337=CARTESIAN_POINT('',(198.742834887867,9.59283488786683,29.4999999776455));
#80338=CARTESIAN_POINT('Ctrl Pts',(198.972408128224,11.1995478642895,30.6605616167741));
#80339=CARTESIAN_POINT('Ctrl Pts',(198.966501983882,11.348264713408,30.6409839384106));
#80340=CARTESIAN_POINT('Ctrl Pts',(198.960346934242,11.492521083178,30.5932335246781));
#80341=CARTESIAN_POINT('Ctrl Pts',(198.947518383083,11.7438279441065,30.4546727204742));
#80342=CARTESIAN_POINT('Ctrl Pts',(198.939902859204,11.8722401983294,30.3575442180324));
#80343=CARTESIAN_POINT('Ctrl Pts',(198.926658933748,12.0778877277915,30.098241261682));
#80344=CARTESIAN_POINT('Ctrl Pts',(198.921294598489,12.1489157369381,29.9614237661834));
#80345=CARTESIAN_POINT('Ctrl Pts',(198.909498712764,12.2370951872888,29.6741489463717));
#80346=CARTESIAN_POINT('Ctrl Pts',(198.903140038498,12.2553418433651,29.5254782198062));
#80347=CARTESIAN_POINT('Ctrl Pts',(198.889569860502,12.2386848362927,29.2166280406198));
#80348=CARTESIAN_POINT('Ctrl Pts',(198.883054686962,12.1992248449925,29.0604998586629));
#80349=CARTESIAN_POINT('Ctrl Pts',(198.871725362742,12.0655442778753,28.7779974846995));
#80350=CARTESIAN_POINT('Ctrl Pts',(198.866407482465,11.977007093434,28.6539718304304));
#80351=CARTESIAN_POINT('Ctrl Pts',(198.853705589642,11.7478211253242,28.4273791893381));
#80352=CARTESIAN_POINT('Ctrl Pts',(198.846169447702,11.6028745119117,28.3312951172536));
#80353=CARTESIAN_POINT('Ctrl Pts',(198.830658409164,11.2500215328413,28.1877695053229));
#80354=CARTESIAN_POINT('Ctrl Pts',(198.82510348869,11.0734739644163,28.1710043522631));
#80355=CARTESIAN_POINT('Ctrl Pts',(198.814498133308,10.7702425966382,28.1727599220091));
#80356=CARTESIAN_POINT('Ctrl Pts',(198.807850967611,10.5957549738643,28.2082078386801));
#80357=CARTESIAN_POINT('Ctrl Pts',(198.79593624953,10.325286655316,28.3201894396842));
#80358=CARTESIAN_POINT('Ctrl Pts',(198.788786367281,10.175500812056,28.3975680811577));
#80359=CARTESIAN_POINT('Ctrl Pts',(198.775759760057,9.90188201278484,28.6562922654616));
#80360=CARTESIAN_POINT('Ctrl Pts',(198.770524087712,9.80098972541154,28.7967707471683));
#80361=CARTESIAN_POINT('Ctrl Pts',(198.758042229528,9.64857140583055,29.1186526630969));
#80362=CARTESIAN_POINT('Ctrl Pts',(198.750674473101,9.6026374392904,29.3007603239914));
#80363=CARTESIAN_POINT('Ctrl Pts',(198.743211014123,9.59323546930708,29.4904190941088));
#80364=CARTESIAN_POINT('Ctrl Pts',(198.743022763441,9.59302276351726,29.4952102169629));
#80365=CARTESIAN_POINT('Ctrl Pts',(198.742834886993,9.59283488699264,29.4999999775771));
#80366=CARTESIAN_POINT('',(204.9,11.0092027577153,28.0365289346043));
#80367=CARTESIAN_POINT('Ctrl Pts',(204.9,11.0092027577153,28.0365289346043));
#80368=CARTESIAN_POINT('Ctrl Pts',(204.9,11.0467246940174,28.0401107183363));
#80369=CARTESIAN_POINT('Ctrl Pts',(204.9,11.0840390001416,28.0452338732584));
#80370=CARTESIAN_POINT('Ctrl Pts',(204.9,11.1210654556941,28.0519424056269));
#80371=CARTESIAN_POINT('Ctrl Pts',(204.9,11.1772434868872,28.0621208614103));
#80372=CARTESIAN_POINT('Ctrl Pts',(204.9,11.2327603402564,28.0759472193249));
#80373=CARTESIAN_POINT('Ctrl Pts',(204.9,11.2873508399968,28.0932167979845));
#80374=CARTESIAN_POINT('Ctrl Pts',(204.9,11.3055295981515,28.0989676061907));
#80375=CARTESIAN_POINT('Ctrl Pts',(204.9,11.3236054164889,28.1051005740255));
#80376=CARTESIAN_POINT('Ctrl Pts',(204.9,11.3415677738497,28.1116090823259));
#80377=CARTESIAN_POINT('Ctrl Pts',(204.9,11.3560653465849,28.1168621552154));
#80378=CARTESIAN_POINT('Ctrl Pts',(204.9,11.3704917883079,28.1223611732078));
#80379=CARTESIAN_POINT('Ctrl Pts',(204.9,11.3848184296621,28.1280931162888));
#80380=CARTESIAN_POINT('Ctrl Pts',(204.9,11.4382112265666,28.1494550297496));
#80381=CARTESIAN_POINT('Ctrl Pts',(204.9,11.4902868729584,28.1740712692501));
#80382=CARTESIAN_POINT('Ctrl Pts',(204.9,11.540775841265,28.2017251394184));
#80383=CARTESIAN_POINT('Ctrl Pts',(204.9,11.5747780701796,28.2203488755607));
#80384=CARTESIAN_POINT('Ctrl Pts',(204.9,11.6080601401866,28.2403513100541));
#80385=CARTESIAN_POINT('Ctrl Pts',(204.9,11.6405303154535,28.2616756760846));
#80386=CARTESIAN_POINT('Ctrl Pts',(204.9,11.6552489720069,28.2713419626765));
#80387=CARTESIAN_POINT('Ctrl Pts',(204.9,11.6698006835649,28.2812799668365));
#80388=CARTESIAN_POINT('Ctrl Pts',(204.9,11.6841762722072,28.2914847959323));
#80389=CARTESIAN_POINT('Ctrl Pts',(204.9,11.6930458914565,28.2977810910501));
#80390=CARTESIAN_POINT('Ctrl Pts',(204.9,11.7018484634984,28.3041791027851));
#80391=CARTESIAN_POINT('Ctrl Pts',(204.9,11.7105703291338,28.3106688265015));
#80392=CARTESIAN_POINT('Ctrl Pts',(204.9,11.7554995199851,28.3440995221365));
#80393=CARTESIAN_POINT('Ctrl Pts',(204.9,11.7983690353811,28.3800162233986));
#80394=CARTESIAN_POINT('Ctrl Pts',(204.9,11.8389289333709,28.4182226735728));
#80395=CARTESIAN_POINT('Ctrl Pts',(204.9,11.878830470216,28.4558089633541));
#80396=CARTESIAN_POINT('Ctrl Pts',(204.9,11.916497391643,28.495612127975));
#80397=CARTESIAN_POINT('Ctrl Pts',(204.9,11.9516504462208,28.5374721453969));
#80398=CARTESIAN_POINT('Ctrl Pts',(204.9,11.9727877167464,28.562642262847));
#80399=CARTESIAN_POINT('Ctrl Pts',(204.9,11.9930152525099,28.5885564984141));
#80400=CARTESIAN_POINT('Ctrl Pts',(204.9,12.0122635537669,28.6151829584833));
#80401=CARTESIAN_POINT('Ctrl Pts',(204.9,12.0215425059034,28.6280186703339));
#80402=CARTESIAN_POINT('Ctrl Pts',(204.9,12.0305937901605,28.6410199186625));
#80403=CARTESIAN_POINT('Ctrl Pts',(204.9,12.0394090002104,28.6541832358476));
#80404=CARTESIAN_POINT('Ctrl Pts',(204.9,12.0452465725742,28.6629001939441));
#80405=CARTESIAN_POINT('Ctrl Pts',(204.9,12.0509813985653,28.6716894675584));
#80406=CARTESIAN_POINT('Ctrl Pts',(204.9,12.0566084820447,28.6805461942609));
#80407=CARTESIAN_POINT('Ctrl Pts',(204.9,12.0849733998086,28.7251910490057));
#80408=CARTESIAN_POINT('Ctrl Pts',(204.9,12.1104810950123,28.7713524632294));
#80409=CARTESIAN_POINT('Ctrl Pts',(204.9,12.1328881532658,28.8188760625729));
#80410=CARTESIAN_POINT('Ctrl Pts',(204.9,12.1410969885954,28.8362863534227));
#80411=CARTESIAN_POINT('Ctrl Pts',(204.9,12.1488892176525,28.8538796496196));
#80412=CARTESIAN_POINT('Ctrl Pts',(204.9,12.1562511770789,28.8716488877078));
#80413=CARTESIAN_POINT('Ctrl Pts',(204.9,12.176836651322,28.9213351426566));
#80414=CARTESIAN_POINT('Ctrl Pts',(204.9,12.1940617705563,28.9723971863));
#80415=CARTESIAN_POINT('Ctrl Pts',(204.9,12.2079432696189,29.0245060000646));
#80416=CARTESIAN_POINT('Ctrl Pts',(204.9,12.2140838020104,29.0475565263344));
#80417=CARTESIAN_POINT('Ctrl Pts',(204.9,12.2195693705896,29.0708118633043));
#80418=CARTESIAN_POINT('Ctrl Pts',(204.9,12.2243982001874,29.0942430113211));
#80419=CARTESIAN_POINT('Ctrl Pts',(204.9,12.2278988728214,29.1112294832984));
#80420=CARTESIAN_POINT('Ctrl Pts',(204.9,12.2310543513456,29.1283083458108));
#80421=CARTESIAN_POINT('Ctrl Pts',(204.9,12.2338633353961,29.1454683109099));
#80422=CARTESIAN_POINT('Ctrl Pts',(204.9,12.2354876524558,29.1553911953245));
#80423=CARTESIAN_POINT('Ctrl Pts',(204.9,12.2369946081418,29.1653322684556));
#80424=CARTESIAN_POINT('Ctrl Pts',(204.9,12.2383840776953,29.1752855278806));
#80425=CARTESIAN_POINT('Ctrl Pts',(204.9,12.2456448442699,29.227296954227));
#80426=CARTESIAN_POINT('Ctrl Pts',(204.9,12.2497072803007,29.2796751085222));
#80427=CARTESIAN_POINT('Ctrl Pts',(204.9,12.2506115813095,29.332111511891));
#80428=CARTESIAN_POINT('Ctrl Pts',(204.9,12.2515113959996,29.384287773545));
#80429=CARTESIAN_POINT('Ctrl Pts',(204.9,12.2492840172522,29.4365228621948));
#80430=CARTESIAN_POINT('Ctrl Pts',(204.9,12.2439194548097,29.4885008047487));
#80431=CARTESIAN_POINT('Ctrl Pts',(204.9,12.2412354063128,29.5145068993889));
#80432=CARTESIAN_POINT('Ctrl Pts',(204.9,12.2377652801437,29.540448325675));
#80433=CARTESIAN_POINT('Ctrl Pts',(204.9,12.2335034987925,29.5662830099219));
#80434=CARTESIAN_POINT('Ctrl Pts',(204.9,12.2303627085674,29.5853223075921));
#80435=CARTESIAN_POINT('Ctrl Pts',(204.9,12.226791895369,29.6043035962146));
#80436=CARTESIAN_POINT('Ctrl Pts',(204.9,12.2227878760177,29.6232092328652));
#80437=CARTESIAN_POINT('Ctrl Pts',(204.9,12.2208506527614,29.6323561514443));
#80438=CARTESIAN_POINT('Ctrl Pts',(204.9,12.2188121268174,29.6414843522619));
#80439=CARTESIAN_POINT('Ctrl Pts',(204.9,12.2166751428225,29.6505793804909));
#80440=CARTESIAN_POINT('Ctrl Pts',(204.9,12.2051403348265,29.6996716547401));
#80441=CARTESIAN_POINT('Ctrl Pts',(204.9,12.1907203877244,29.7478975714839));
#80442=CARTESIAN_POINT('Ctrl Pts',(204.9,12.1734205317272,29.7949731113051));
#80443=CARTESIAN_POINT('Ctrl Pts',(204.9,12.1564678597905,29.8411039104843));
#80444=CARTESIAN_POINT('Ctrl Pts',(204.9,12.1367492989439,29.8861308946856));
#80445=CARTESIAN_POINT('Ctrl Pts',(204.9,12.1142291617453,29.9297582081839));
#80446=CARTESIAN_POINT('Ctrl Pts',(204.9,12.0917090245467,29.9733855216821));
#80447=CARTESIAN_POINT('Ctrl Pts',(204.9,12.0663870507824,30.0156140542582));
#80448=CARTESIAN_POINT('Ctrl Pts',(204.9,12.0381913065553,30.05610599124));
#80449=CARTESIAN_POINT('Ctrl Pts',(204.9,10.9852095428848,28.0365747397361));
#80450=CARTESIAN_POINT('Ctrl Pts',(204.9,10.9932072811616,28.0365594713589));
#80451=CARTESIAN_POINT('Ctrl Pts',(204.9,11.0012050194384,28.0365442029816));
#80452=CARTESIAN_POINT('Ctrl Pts',(204.9,11.0092027577153,28.0365289346043));
#80453=CARTESIAN_POINT('Ctrl Pts',(198.742834886993,9.59283488699264,29.4999999775771));
#80454=CARTESIAN_POINT('Ctrl Pts',(198.737090843768,9.58709084143462,29.6464397908325));
#80455=CARTESIAN_POINT('Ctrl Pts',(198.732013616724,9.60462181747414,29.7916213325757));
#80456=CARTESIAN_POINT('Ctrl Pts',(198.721768578781,9.69219000241292,30.0997116657855));
#80457=CARTESIAN_POINT('Ctrl Pts',(198.716403767351,9.77035013284231,30.2572004764847));
#80458=CARTESIAN_POINT('Ctrl Pts',(198.706589374933,9.9379839780765,30.4834339409197));
#80459=CARTESIAN_POINT('Ctrl Pts',(198.702622193431,10.0115439287722,30.562750641684));
#80460=CARTESIAN_POINT('Ctrl Pts',(198.694468921762,10.1766052708443,30.7053066795134));
#80461=CARTESIAN_POINT('Ctrl Pts',(198.690304067705,10.2681818274306,30.7678059282328));
#80462=CARTESIAN_POINT('Ctrl Pts',(198.6865,10.3659929054241,30.8190402776365));
#80463=CARTESIAN_POINT('Origin',(204.9,11.,29.5));
#80464=CARTESIAN_POINT('',(204.9,11.,30.9635));
#80465=CARTESIAN_POINT('Origin',(204.9,11.,29.5));
#80466=CARTESIAN_POINT('Ctrl Pts',(204.9,10.8095183674143,30.6639494701171));
#80467=CARTESIAN_POINT('Ctrl Pts',(204.9,10.7712696975013,30.6624764558929));
#80468=CARTESIAN_POINT('Ctrl Pts',(204.9,10.7332004594639,30.6590457335319));
#80469=CARTESIAN_POINT('Ctrl Pts',(204.9,10.6954537511157,30.6536225274562));
#80470=CARTESIAN_POINT('Ctrl Pts',(204.9,10.6475314468811,30.6467373567259));
#80471=CARTESIAN_POINT('Ctrl Pts',(204.9,10.6001284968355,30.6366429213737));
#80472=CARTESIAN_POINT('Ctrl Pts',(204.9,10.5534379360125,30.6235714344056));
#80473=CARTESIAN_POINT('Ctrl Pts',(204.9,10.5362710773309,30.6187654015461));
#80474=CARTESIAN_POINT('Ctrl Pts',(204.9,10.5192004912383,30.613556412169));
#80475=CARTESIAN_POINT('Ctrl Pts',(204.9,10.5022357871601,30.6079542951409));
#80476=CARTESIAN_POINT('Ctrl Pts',(204.9,10.4916312146694,30.6044524329303));
#80477=CARTESIAN_POINT('Ctrl Pts',(204.9,10.4810727536708,30.6007984267483));
#80478=CARTESIAN_POINT('Ctrl Pts',(204.9,10.4705700758602,30.5969978312444));
#80479=CARTESIAN_POINT('Ctrl Pts',(204.9,10.4230152151206,30.5797891923453));
#80480=CARTESIAN_POINT('Ctrl Pts',(204.9,10.3765580062203,30.5595645005949));
#80481=CARTESIAN_POINT('Ctrl Pts',(204.9,10.3314093737795,30.5365807286222));
#80482=CARTESIAN_POINT('Ctrl Pts',(204.9,10.2991899201142,30.5201788015628));
#80483=CARTESIAN_POINT('Ctrl Pts',(204.9,10.2676367064342,30.5023705311667));
#80484=CARTESIAN_POINT('Ctrl Pts',(204.9,10.2368280860054,30.4832333089675));
#80485=CARTESIAN_POINT('Ctrl Pts',(204.9,10.2257215662505,30.4763343328546));
#80486=CARTESIAN_POINT('Ctrl Pts',(204.9,10.214711842786,30.4692625282535));
#80487=CARTESIAN_POINT('Ctrl Pts',(204.9,10.2038027069567,30.4620211376777));
#80488=CARTESIAN_POINT('Ctrl Pts',(204.9,10.1950670831385,30.4562225056889));
#80489=CARTESIAN_POINT('Ctrl Pts',(204.9,10.1864036448346,30.4503202091041));
#80490=CARTESIAN_POINT('Ctrl Pts',(204.9,10.1778157661554,30.4443176664685));
#80491=CARTESIAN_POINT('Ctrl Pts',(204.9,10.1342875508468,30.4138933931408));
#80492=CARTESIAN_POINT('Ctrl Pts',(204.9,10.0926859169683,30.3808888745858));
#80493=CARTESIAN_POINT('Ctrl Pts',(204.9,10.0532360341447,30.3455716202146));
#80494=CARTESIAN_POINT('Ctrl Pts',(204.9,10.0139891823114,30.3104361280342));
#80495=CARTESIAN_POINT('Ctrl Pts',(204.9,9.97687099749904,30.2730109976963));
#80496=CARTESIAN_POINT('Ctrl Pts',(204.9,9.9421187286471,30.2335108505032));
#80497=CARTESIAN_POINT('Ctrl Pts',(204.9,9.92163451139171,30.2102280657109));
#80498=CARTESIAN_POINT('Ctrl Pts',(204.9,9.90197265915035,30.1862234739019));
#80499=CARTESIAN_POINT('Ctrl Pts',(204.9,9.88318645150572,30.161534408886));
#80500=CARTESIAN_POINT('Ctrl Pts',(204.9,9.87352309519722,30.1488347072387));
#80501=CARTESIAN_POINT('Ctrl Pts',(204.9,9.86409149497076,30.1359538257004));
#80502=CARTESIAN_POINT('Ctrl Pts',(204.9,9.85489938332372,30.1228964121846));
#80503=CARTESIAN_POINT('Ctrl Pts',(204.9,9.84937935931052,30.1150552067114));
#80504=CARTESIAN_POINT('Ctrl Pts',(204.9,9.84394660300455,30.1071514450078));
#80505=CARTESIAN_POINT('Ctrl Pts',(204.9,9.83860949535559,30.099196663335));
#80506=CARTESIAN_POINT('Ctrl Pts',(204.9,9.80807359169367,30.0536839132112));
#80507=CARTESIAN_POINT('Ctrl Pts',(204.9,9.78060307134752,30.0064153274634));
#80508=CARTESIAN_POINT('Ctrl Pts',(204.9,9.7564418151761,29.9576382608005));
#80509=CARTESIAN_POINT('Ctrl Pts',(204.9,9.75084518682776,29.9463397127408));
#80510=CARTESIAN_POINT('Ctrl Pts',(204.9,9.74542623557677,29.9349600394241));
#80511=CARTESIAN_POINT('Ctrl Pts',(204.9,9.74018822887327,29.9235019929462));
#80512=CARTESIAN_POINT('Ctrl Pts',(204.9,9.71832767946602,29.8756824300249));
#80513=CARTESIAN_POINT('Ctrl Pts',(204.9,9.6996152796779,29.8265001396101));
#80514=CARTESIAN_POINT('Ctrl Pts',(204.9,9.68396802411589,29.7762398165101));
#80515=CARTESIAN_POINT('Ctrl Pts',(204.9,9.67642580370168,29.7520135594897));
#80516=CARTESIAN_POINT('Ctrl Pts',(204.9,9.66959638476633,29.7275363893671));
#80517=CARTESIAN_POINT('Ctrl Pts',(204.9,9.66347414088689,29.7028381764364));
#80518=CARTESIAN_POINT('Ctrl Pts',(204.9,9.65957072765371,29.6870911181538));
#80519=CARTESIAN_POINT('Ctrl Pts',(204.9,9.65595483418736,29.6712541813871));
#80520=CARTESIAN_POINT('Ctrl Pts',(204.9,9.65262551776375,29.655334919862));
#80521=CARTESIAN_POINT('Ctrl Pts',(204.9,9.65064506445563,29.6458653020369));
#80522=CARTESIAN_POINT('Ctrl Pts',(204.9,9.64876639256952,29.6363678821321));
#80523=CARTESIAN_POINT('Ctrl Pts',(204.9,9.64699127757553,29.6268563749219));
#80524=CARTESIAN_POINT('Ctrl Pts',(204.9,9.63682229938692,29.5723684630463));
#80525=CARTESIAN_POINT('Ctrl Pts',(204.9,9.63002532774624,29.5173152919441));
#80526=CARTESIAN_POINT('Ctrl Pts',(204.9,9.62648601813751,29.4620248108003));
#80527=CARTESIAN_POINT('Ctrl Pts',(204.9,9.62294670852878,29.4067343296565));
#80528=CARTESIAN_POINT('Ctrl Pts',(204.9,9.6226650108644,29.3512055186983));
#80529=CARTESIAN_POINT('Ctrl Pts',(204.9,9.62557417374219,29.2957426309545));
#80530=CARTESIAN_POINT('Ctrl Pts',(204.9,9.62722255400633,29.2643164326324));
#80531=CARTESIAN_POINT('Ctrl Pts',(204.9,9.62989624266107,29.2329110520043));
#80532=CARTESIAN_POINT('Ctrl Pts',(204.9,9.63358997720682,29.2015803757213));
#80533=CARTESIAN_POINT('Ctrl Pts',(204.9,9.63609588323508,29.1803249959438));
#80534=CARTESIAN_POINT('Ctrl Pts',(204.9,9.639071373389,29.1591039819646));
#80535=CARTESIAN_POINT('Ctrl Pts',(204.9,9.6425161244344,29.1379341571094));
#80536=CARTESIAN_POINT('Ctrl Pts',(204.9,9.64495055563062,29.1229732843592));
#80537=CARTESIAN_POINT('Ctrl Pts',(204.9,9.64762080578892,29.1080315224471));
#80538=CARTESIAN_POINT('Ctrl Pts',(204.9,9.65051964564107,29.093150364109));
#80539=CARTESIAN_POINT('Ctrl Pts',(204.9,9.66165233100661,29.0360008622038));
#80540=CARTESIAN_POINT('Ctrl Pts',(204.9,9.67616209913347,28.9796679258513));
#80541=CARTESIAN_POINT('Ctrl Pts',(204.9,9.69396309947139,28.9244837740775));
#80542=CARTESIAN_POINT('Ctrl Pts',(204.9,9.71191078973324,28.868844874881));
#80543=CARTESIAN_POINT('Ctrl Pts',(204.9,9.73320408854728,28.8143725695034));
#80544=CARTESIAN_POINT('Ctrl Pts',(204.9,9.75780799601074,28.7614030799068));
#80545=CARTESIAN_POINT('Ctrl Pts',(204.9,9.78241190347419,28.7084335903102));
#80546=CARTESIAN_POINT('Ctrl Pts',(204.9,9.81032638815783,28.6569656545721));
#80547=CARTESIAN_POINT('Ctrl Pts',(204.9,9.84157002494772,28.6073497615898));
#80548=CARTESIAN_POINT('Ctrl Pts',(204.9,9.84353590847449,28.6042278757691));
#80549=CARTESIAN_POINT('Ctrl Pts',(204.9,9.8455149900329,28.6011133307502));
#80550=CARTESIAN_POINT('Ctrl Pts',(204.9,9.84750728139497,28.5980062175589));
#80551=CARTESIAN_POINT('Origin',(204.9,11.,29.5));
#80552=CARTESIAN_POINT('Ctrl Pts',(198.685427081353,11.6348121556185,30.820715192556));
#80553=CARTESIAN_POINT('Ctrl Pts',(198.711644380931,11.1996942109557,31.0298580584491));
#80554=CARTESIAN_POINT('Ctrl Pts',(198.764078980087,10.1136086674488,30.9807436605481));
#80555=CARTESIAN_POINT('Ctrl Pts',(198.842730878821,9.27393396051783,29.5726451812295));
#80556=CARTESIAN_POINT('Ctrl Pts',(198.921382777556,9.99078494028664,28.0992649491572));
#80557=CARTESIAN_POINT('Ctrl Pts',(199.00003467629,11.614247459966,27.8863179216116));
#80558=CARTESIAN_POINT('Ctrl Pts',(199.078686575024,12.6857081782859,29.1255487079913));
#80559=CARTESIAN_POINT('Ctrl Pts',(199.157338473758,12.2398448395701,30.7017293637303));
#80560=CARTESIAN_POINT('Ctrl Pts',(199.235990372492,10.6784277100622,31.1964884698741));
#80561=CARTESIAN_POINT('Ctrl Pts',(199.314642271227,9.40630700003317,30.1645830946929));
#80562=CARTESIAN_POINT('Ctrl Pts',(199.393294169961,9.56838264010626,28.5346249407398));
#80563=CARTESIAN_POINT('Ctrl Pts',(199.471946068695,11.0187431449501,27.7734015618396));
#80564=CARTESIAN_POINT('Ctrl Pts',(199.550597967429,12.4522462845997,28.5659350063268));
#80565=CARTESIAN_POINT('Ctrl Pts',(199.629249866163,12.5788764490999,30.1990281642664));
#80566=CARTESIAN_POINT('Ctrl Pts',(199.707901764897,11.2846866311837,31.203069843307));
#80567=CARTESIAN_POINT('Ctrl Pts',(199.786553663632,9.73430782530876,30.6745283379686));
#80568=CARTESIAN_POINT('Ctrl Pts',(199.865205562366,9.3229189215623,29.0890352988328));
#80569=CARTESIAN_POINT('Ctrl Pts',(199.9438574611,10.4207257607197,27.8733671106996));
#80570=CARTESIAN_POINT('Ctrl Pts',(200.022509359834,12.0398184039788,28.12149687136));
#80571=CARTESIAN_POINT('Ctrl Pts',(200.101161258568,12.7231841573457,29.6101339730259));
#80572=CARTESIAN_POINT('Ctrl Pts',(200.179813157302,11.8558660427577,30.999662122572));
#80573=CARTESIAN_POINT('Ctrl Pts',(200.258465056036,10.2183587950959,31.0396526191242));
#80574=CARTESIAN_POINT('Ctrl Pts',(200.337116954771,9.28424615241247,29.6941182368515));
#80575=CARTESIAN_POINT('Ctrl Pts',(200.415768853505,9.89413090757163,28.1738979263852));
#80576=CARTESIAN_POINT('Ctrl Pts',(200.494420752239,11.4991811460846,27.8470295399369));
#80577=CARTESIAN_POINT('Ctrl Pts',(200.573072650973,12.6550210305185,29.0076601310952));
#80578=CARTESIAN_POINT('Ctrl Pts',(200.651724549707,12.3215166406444,30.6113446481208));
#80579=CARTESIAN_POINT('Ctrl Pts',(200.730376448442,10.7987867324307,31.2149362609849));
#80580=CARTESIAN_POINT('Ctrl Pts',(200.809028347176,9.45712753126317,30.2752662145761));
#80581=CARTESIAN_POINT('Ctrl Pts',(200.88768024591,9.50389073404023,28.6379383881611));
#80582=CARTESIAN_POINT('Ctrl Pts',(200.966332144644,10.8969943931969,27.7763750398514));
#80583=CARTESIAN_POINT('Ctrl Pts',(201.044984043378,12.3827922283826,28.4658922631549));
#80584=CARTESIAN_POINT('Ctrl Pts',(201.123635942113,12.6242229827909,30.0859973212029));
#80585=CARTESIAN_POINT('Ctrl Pts',(201.202287840846,11.4040244554083,31.1787666299141));
#80586=CARTESIAN_POINT('Ctrl Pts',(201.280939739581,9.82024655447976,30.7608231303653));
#80587=CARTESIAN_POINT('Ctrl Pts',(201.359591638315,9.29812225624811,29.2082718669661));
#80588=CARTESIAN_POINT('Ctrl Pts',(201.438243537049,10.3075083298367,27.9182451375021));
#80589=CARTESIAN_POINT('Ctrl Pts',(201.516895435783,11.9400638285778,28.0516308631841));
#80590=CARTESIAN_POINT('Ctrl Pts',(201.595547334518,12.7266610856501,29.4883959669684));
#80591=CARTESIAN_POINT('Ctrl Pts',(201.674199233252,11.9594455785568,30.9356034759184));
#80592=CARTESIAN_POINT('Ctrl Pts',(201.752851131986,10.3288303001514,31.0909193544258));
#80593=CARTESIAN_POINT('Ctrl Pts',(201.83150303072,9.30219692370285,29.8145757021723));
#80594=CARTESIAN_POINT('Ctrl Pts',(201.910154929454,9.80340714836079,28.2551471148416));
#80595=CARTESIAN_POINT('Ctrl Pts',(201.988806828188,11.3814246641764,27.8159547559999));
#80596=CARTESIAN_POINT('Ctrl Pts',(202.067458726923,12.6162002336191,28.8922254010485));
#80597=CARTESIAN_POINT('Ctrl Pts',(202.146110625657,12.3965661488944,30.5154290472719));
#80598=CARTESIAN_POINT('Ctrl Pts',(202.224762524391,10.9201699084762,31.2248537082224));
#80599=CARTESIAN_POINT('Ctrl Pts',(202.303414423125,9.51561232603495,30.3820920539613));
#80600=CARTESIAN_POINT('Ctrl Pts',(202.382066321859,9.4468470041279,28.7455406374798));
#80601=CARTESIAN_POINT('Ctrl Pts',(202.460718220593,10.7757554757318,27.7879230298789));
#80602=CARTESIAN_POINT('Ctrl Pts',(202.539370119328,12.3064603548631,28.3709940215176));
#80603=CARTESIAN_POINT('Ctrl Pts',(202.618022018062,12.6614887841502,29.9700512508477));
#80604=CARTESIAN_POINT('Ctrl Pts',(202.696673916796,11.5213526430484,31.1461119584899));
#80605=CARTESIAN_POINT('Ctrl Pts',(202.77532581553,9.91205414106004,30.8408456161187));
#80606=CARTESIAN_POINT('Ctrl Pts',(202.853977714264,9.28179210220836,29.3289597174551));
#80607=CARTESIAN_POINT('Ctrl Pts',(202.932629612999,10.1977358505203,27.9709920232824));
#80608=CARTESIAN_POINT('Ctrl Pts',(203.011281511733,11.8356326711549,27.9889701535476));
#80609=CARTESIAN_POINT('Ctrl Pts',(203.089933410467,12.7215482713383,29.36671568772));
#80610=CARTESIAN_POINT('Ctrl Pts',(203.168585309201,12.0582521005643,30.8644030382864));
#80611=CARTESIAN_POINT('Ctrl Pts',(203.247237207935,10.4426407158838,31.1342716370908));
#80612=CARTESIAN_POINT('Ctrl Pts',(203.32588910667,9.3285938687821,29.9334682287171));
#80613=CARTESIAN_POINT('Ctrl Pts',(203.404541005403,9.71863615894957,28.342589151653));
#80614=CARTESIAN_POINT('Ctrl Pts',(203.483192904138,11.2617706826824,27.7932577107749));
#80615=CARTESIAN_POINT('Ctrl Pts',(203.561844802872,12.5693392211027,28.7798141920086));
#80616=CARTESIAN_POINT('Ctrl Pts',(203.640496701606,12.4646680616967,30.4144619565041));
#80617=CARTESIAN_POINT('Ctrl Pts',(203.71914860034,11.041950231981,31.2261903450361));
#80618=CARTESIAN_POINT('Ctrl Pts',(203.797800499075,9.5814815785967,30.4845298298707));
#80619=CARTESIAN_POINT('Ctrl Pts',(203.876452397809,9.39752989638986,28.8568958589839));
#80620=CARTESIAN_POINT('Ctrl Pts',(203.955104296543,10.65563202014,27.8079887971982));
#80621=CARTESIAN_POINT('Ctrl Pts',(204.033756195277,12.2236293586242,28.2817110867069));
#80622=CARTESIAN_POINT('Ctrl Pts',(204.112408094011,12.6904886275653,29.8517693451864));
#80623=CARTESIAN_POINT('Ctrl Pts',(204.191059992745,11.6360881356371,31.10526295475));
#80624=CARTESIAN_POINT('Ctrl Pts',(204.26971189148,10.0092721109943,30.9142087249912));
#80625=CARTESIAN_POINT('Ctrl Pts',(204.348363790214,9.27401355747157,29.4504755991501));
#80626=CARTESIAN_POINT('Ctrl Pts',(204.427015688948,10.0919463015996,28.0313927786227));
#80627=CARTESIAN_POINT('Ctrl Pts',(204.505667587682,11.7270613398761,27.9337281077398));
#80628=CARTESIAN_POINT('Ctrl Pts',(204.584319486416,12.7078361411144,29.2459025633933));
#80629=CARTESIAN_POINT('Ctrl Pts',(204.662971385151,12.1518672632886,30.7859920400904));
#80630=CARTESIAN_POINT('Ctrl Pts',(204.741623283884,10.5590803622657,31.1703805458846));
#80631=CARTESIAN_POINT('Ctrl Pts',(204.820275182619,9.36368173991768,30.048410370431));
#80632=CARTESIAN_POINT('Ctrl Pts',(204.872709781775,9.54849896857087,28.9770389950952));
#80633=CARTESIAN_POINT('Ctrl Pts',(204.898927081353,9.8460438482599,28.5968608675124));
#80634=CARTESIAN_POINT('Ctrl Pts',(198.741050723552,11.5930751352726,30.7338820776337));
#80635=CARTESIAN_POINT('Ctrl Pts',(198.76726802313,11.1865649076305,30.9292744191052));
#80636=CARTESIAN_POINT('Ctrl Pts',(198.819702622287,10.1718862740663,30.8833891474997));
#80637=CARTESIAN_POINT('Ctrl Pts',(198.898354521021,9.38741769388793,29.5678689755753));
#80638=CARTESIAN_POINT('Ctrl Pts',(198.977006419755,10.0571378434374,28.1913591329231));
#80639=CARTESIAN_POINT('Ctrl Pts',(199.055658318489,11.5738625074928,27.9924127421684));
#80640=CARTESIAN_POINT('Ctrl Pts',(199.134310217223,12.5748778548401,29.1501677721583));
#80641=CARTESIAN_POINT('Ctrl Pts',(199.212962115957,12.1583287110005,30.6227192148848));
#80642=CARTESIAN_POINT('Ctrl Pts',(199.291614014691,10.6995701363518,31.0849493741634));
#80643=CARTESIAN_POINT('Ctrl Pts',(199.370265913426,9.5110875978464,30.1208887232174));
#80644=CARTESIAN_POINT('Ctrl Pts',(199.44891781216,9.66250724428823,28.5980954936162));
#80645=CARTESIAN_POINT('Ctrl Pts',(199.527569710894,11.0175108386447,27.8869202988471));
#80646=CARTESIAN_POINT('Ctrl Pts',(199.606221609628,12.3567653896749,28.6273470150609));
#80647=CARTESIAN_POINT('Ctrl Pts',(199.684873508362,12.4750699956528,30.1530691314153));
#80648=CARTESIAN_POINT('Ctrl Pts',(199.763525407097,11.2659693277849,31.0910980417724));
#80649=CARTESIAN_POINT('Ctrl Pts',(199.842177305831,9.81752333966091,30.5973065760587));
#80650=CARTESIAN_POINT('Ctrl Pts',(199.920829204565,9.43318203872702,29.1160550115813));
#80651=CARTESIAN_POINT('Ctrl Pts',(199.999481103299,10.4588113274449,27.9803134087427));
#80652=CARTESIAN_POINT('Ctrl Pts',(200.078133002033,11.9714534215208,28.2121293720419));
#80653=CARTESIAN_POINT('Ctrl Pts',(200.156784900767,12.6098898991963,29.6028929902686));
#80654=CARTESIAN_POINT('Ctrl Pts',(200.235436799502,11.7995953835968,30.9010637766396));
#80655=CARTESIAN_POINT('Ctrl Pts',(200.314088698236,10.2697493908549,30.9384250164052));
#80656=CARTESIAN_POINT('Ctrl Pts',(200.39274059697,9.39705188968703,29.6813555373201));
#80657=CARTESIAN_POINT('Ctrl Pts',(200.471392495704,9.96683852730155,28.2610852127933));
#80658=CARTESIAN_POINT('Ctrl Pts',(200.550044394438,11.4663614631815,27.9557074553049));
#80659=CARTESIAN_POINT('Ctrl Pts',(200.628696293173,12.5462082962121,29.0400300202722));
#80660=CARTESIAN_POINT('Ctrl Pts',(200.707348191907,12.2346308328824,30.5382770268103));
#80661=CARTESIAN_POINT('Ctrl Pts',(200.786000090641,10.8120159092322,31.1021842776096));
#80662=CARTESIAN_POINT('Ctrl Pts',(200.864651989375,9.55856682956415,30.2242947555627));
#80663=CARTESIAN_POINT('Ctrl Pts',(200.943303888109,9.60225549016605,28.6946163876517));
#80664=CARTESIAN_POINT('Ctrl Pts',(201.021955786844,10.9037667069733,27.8896982794803));
#80665=CARTESIAN_POINT('Ctrl Pts',(201.100607685578,12.2918777320872,28.533881786151));
#80666=CARTESIAN_POINT('Ctrl Pts',(201.179259584312,12.5174351289682,30.04746973174));
#80667=CARTESIAN_POINT('Ctrl Pts',(201.257911483046,11.377461043277,31.0683926927285));
#80668=CARTESIAN_POINT('Ctrl Pts',(201.33656338178,9.89781185174615,30.6779277412664));
#80669=CARTESIAN_POINT('Ctrl Pts',(201.415215280514,9.4100156807653,29.2274521282705));
#80670=CARTESIAN_POINT('Ctrl Pts',(201.493867179248,10.3530376075469,28.0222408381107));
#80671=CARTESIAN_POINT('Ctrl Pts',(201.572519077983,11.8782574142038,28.1468568471176));
#80672=CARTESIAN_POINT('Ctrl Pts',(201.651170976717,12.6131382297557,29.4891588977951));
#80673=CARTESIAN_POINT('Ctrl Pts',(201.729822875451,11.8963648714868,30.8412167964057));
#80674=CARTESIAN_POINT('Ctrl Pts',(201.808474774185,10.3729577214212,30.9863211155975));
#80675=CARTESIAN_POINT('Ctrl Pts',(201.887126672919,9.41382245089489,29.7938932808203));
#80676=CARTESIAN_POINT('Ctrl Pts',(201.965778571654,9.88207958673907,28.3369925075861));
#80677=CARTESIAN_POINT('Ctrl Pts',(202.044430470388,11.3563471214289,27.9266757464382));
#80678=CARTESIAN_POINT('Ctrl Pts',(202.123082369122,12.5099398518091,28.9321847820681));
#80679=CARTESIAN_POINT('Ctrl Pts',(202.201734267856,12.3047460580928,30.448667592831));
#80680=CARTESIAN_POINT('Ctrl Pts',(202.28038616659,10.9254185007166,31.1114496820445));
#80681=CARTESIAN_POINT('Ctrl Pts',(202.359038065324,9.61320642218011,30.3240971121862));
#80682=CARTESIAN_POINT('Ctrl Pts',(202.437689964059,9.54896221666022,28.7951441075536));
#80683=CARTESIAN_POINT('Ctrl Pts',(202.516341862793,10.7904988894945,27.9004870233427));
#80684=CARTESIAN_POINT('Ctrl Pts',(202.594993761527,12.2205644533283,28.4452228230262));
#80685=CARTESIAN_POINT('Ctrl Pts',(202.673645660261,12.5522508141855,29.9391467723392));
#80686=CARTESIAN_POINT('Ctrl Pts',(202.752297558995,11.487075249842,31.0378849693009));
#80687=CARTESIAN_POINT('Ctrl Pts',(202.83094945773,9.98358336123639,30.7526889854281));
#80688=CARTESIAN_POINT('Ctrl Pts',(202.909601356464,9.39475918602047,29.3402051097958));
#80689=CARTESIAN_POINT('Ctrl Pts',(202.988253255198,10.2504823438464,28.0715197722685));
#80690=CARTESIAN_POINT('Ctrl Pts',(203.066905153932,11.7806922962912,28.0883158936796));
#80691=CARTESIAN_POINT('Ctrl Pts',(203.145557052666,12.6083615678522,29.375478736764));
#80692=CARTESIAN_POINT('Ctrl Pts',(203.224208951401,11.988675157115,30.7746975768125));
#80693=CARTESIAN_POINT('Ctrl Pts',(203.302860850135,10.4792854391697,31.0268231139892));
#80694=CARTESIAN_POINT('Ctrl Pts',(203.381512748869,9.43848387496357,29.904968975637));
#80695=CARTESIAN_POINT('Ctrl Pts',(203.460164647603,9.80288203898061,28.4186854892838));
#80696=CARTESIAN_POINT('Ctrl Pts',(203.538816546337,11.2445600350721,27.905470964759));
#80697=CARTESIAN_POINT('Ctrl Pts',(203.617468445071,12.4661598121687,28.8271642773134));
#80698=CARTESIAN_POINT('Ctrl Pts',(203.696120343806,12.368370471693,30.3543387894437));
#80699=CARTESIAN_POINT('Ctrl Pts',(203.77477224254,11.0391921283905,31.1126984389437));
#80700=CARTESIAN_POINT('Ctrl Pts',(203.853424141274,9.67474496634252,30.41979990752));
#80701=CARTESIAN_POINT('Ctrl Pts',(203.932076040008,9.5028875627896,28.8991780528276));
#80702=CARTESIAN_POINT('Ctrl Pts',(204.010727938742,10.6782731955722,27.9192335258504));
#80703=CARTESIAN_POINT('Ctrl Pts',(204.089379837476,12.1431793499329,28.361809976924));
#80704=CARTESIAN_POINT('Ctrl Pts',(204.16803173621,12.5793440037285,29.8286415518901));
#80705=CARTESIAN_POINT('Ctrl Pts',(204.246683634945,11.5942672233815,30.999721666654));
#80706=CARTESIAN_POINT('Ctrl Pts',(204.325335533679,10.0744095373885,30.8212286870288));
#80707=CARTESIAN_POINT('Ctrl Pts',(204.403987432413,9.38749205757757,29.4537316819261));
#80708=CARTESIAN_POINT('Ctrl Pts',(204.482639331147,10.1516481446564,28.1279493567164));
#80709=CARTESIAN_POINT('Ctrl Pts',(204.561291229882,11.6792592086998,28.0367058488809));
#80710=CARTESIAN_POINT('Ctrl Pts',(204.639943128615,12.595550969606,29.262608717785));
#80711=CARTESIAN_POINT('Ctrl Pts',(204.71859502735,12.0761353999678,30.7014418696708));
#80712=CARTESIAN_POINT('Ctrl Pts',(204.797246926084,10.5880695234343,31.0605579689034));
#80713=CARTESIAN_POINT('Ctrl Pts',(204.875898824818,9.47126482242333,30.0123540117334));
#80714=CARTESIAN_POINT('Ctrl Pts',(204.928333423974,9.64393086530558,29.0114221333333));
#80715=CARTESIAN_POINT('Ctrl Pts',(204.954550723552,9.92191304981385,28.6562395924064));
#80716=CARTESIAN_POINT('Ctrl Pts',(198.796674365751,11.5513381149266,30.6470489627113));
#80717=CARTESIAN_POINT('Ctrl Pts',(198.82289166533,11.1734356043053,30.8286907797611));
#80718=CARTESIAN_POINT('Ctrl Pts',(198.875326264485,10.2301638806838,30.7860346344513));
#80719=CARTESIAN_POINT('Ctrl Pts',(198.953978163219,9.50090142725805,29.5630927699211));
#80720=CARTESIAN_POINT('Ctrl Pts',(199.032630061953,10.1234907465883,28.2834533166888));
#80721=CARTESIAN_POINT('Ctrl Pts',(199.111281960687,11.5334775550196,28.0985075627251));
#80722=CARTESIAN_POINT('Ctrl Pts',(199.189933859421,12.4640475313945,29.1747868363253));
#80723=CARTESIAN_POINT('Ctrl Pts',(199.268585758156,12.0768125824308,30.5437090660394));
#80724=CARTESIAN_POINT('Ctrl Pts',(199.34723765689,10.7207125626412,30.9734102784528));
#80725=CARTESIAN_POINT('Ctrl Pts',(199.425889555624,9.61586819565963,30.0771943517418));
#80726=CARTESIAN_POINT('Ctrl Pts',(199.504541454358,9.7566318484702,28.6615660464927));
#80727=CARTESIAN_POINT('Ctrl Pts',(199.583193353092,11.0162785323393,28.0004390358545));
#80728=CARTESIAN_POINT('Ctrl Pts',(199.661845251827,12.26128449475,28.688759023795));
#80729=CARTESIAN_POINT('Ctrl Pts',(199.740497150561,12.3712635422058,30.1071100985642));
#80730=CARTESIAN_POINT('Ctrl Pts',(199.819149049295,11.2472520243861,30.9791262402378));
#80731=CARTESIAN_POINT('Ctrl Pts',(199.897800948029,9.90073885401307,30.5200848141488));
#80732=CARTESIAN_POINT('Ctrl Pts',(199.976452846763,9.54344515589176,29.1430747243298));
#80733=CARTESIAN_POINT('Ctrl Pts',(200.055104745497,10.4968968941699,28.0872597067857));
#80734=CARTESIAN_POINT('Ctrl Pts',(200.133756644232,11.903088439063,28.3027618727239));
#80735=CARTESIAN_POINT('Ctrl Pts',(200.212408542966,12.4965956410471,29.5956520075113));
#80736=CARTESIAN_POINT('Ctrl Pts',(200.2910604417,11.7433247244359,30.8024654307069));
#80737=CARTESIAN_POINT('Ctrl Pts',(200.369712340434,10.3211399866139,30.8371974136864));
#80738=CARTESIAN_POINT('Ctrl Pts',(200.448364239168,9.50985762696159,29.6685928377888));
#80739=CARTESIAN_POINT('Ctrl Pts',(200.527016137902,10.0395461470315,28.3482724992014));
#80740=CARTESIAN_POINT('Ctrl Pts',(200.605668036637,11.4335417802784,28.0643853706729));
#80741=CARTESIAN_POINT('Ctrl Pts',(200.684319935371,12.4373955619059,29.0723999094493));
#80742=CARTESIAN_POINT('Ctrl Pts',(200.762971834105,12.1477450251203,30.4652094055));
#80743=CARTESIAN_POINT('Ctrl Pts',(200.841623732839,10.8252450860336,30.9894322942343));
#80744=CARTESIAN_POINT('Ctrl Pts',(200.920275631573,9.66000612786511,30.1733232965494));
#80745=CARTESIAN_POINT('Ctrl Pts',(200.998927530308,9.7006202462919,28.7512943871423));
#80746=CARTESIAN_POINT('Ctrl Pts',(201.077579429042,10.9105390207496,28.0030215191092));
#80747=CARTESIAN_POINT('Ctrl Pts',(201.156231327776,12.2009632357919,28.601871309147));
#80748=CARTESIAN_POINT('Ctrl Pts',(201.23488322651,12.4106472751453,30.0089421422772));
#80749=CARTESIAN_POINT('Ctrl Pts',(201.313535125244,11.3508976311457,30.958018755543));
#80750=CARTESIAN_POINT('Ctrl Pts',(201.392187023979,9.97537714901258,30.5950323521675));
#80751=CARTESIAN_POINT('Ctrl Pts',(201.470838922713,9.52190910528247,29.2466323895747));
#80752=CARTESIAN_POINT('Ctrl Pts',(201.549490821447,10.3985668852571,28.1262365387192));
#80753=CARTESIAN_POINT('Ctrl Pts',(201.628142720181,11.8164509998297,28.2420828310512));
#80754=CARTESIAN_POINT('Ctrl Pts',(201.706794618915,12.4996153738612,29.4899218286219));
#80755=CARTESIAN_POINT('Ctrl Pts',(201.785446517649,11.8332841644169,30.746830116893));
#80756=CARTESIAN_POINT('Ctrl Pts',(201.864098416384,10.417085142691,30.8817228767694));
#80757=CARTESIAN_POINT('Ctrl Pts',(201.942750315118,9.52544797808693,29.7732108594681));
#80758=CARTESIAN_POINT('Ctrl Pts',(202.021402213852,9.96075202511736,28.4188379003305));
#80759=CARTESIAN_POINT('Ctrl Pts',(202.100054112586,11.3312695786813,28.0373967368765));
#80760=CARTESIAN_POINT('Ctrl Pts',(202.17870601132,12.4036794699991,28.9721441630876));
#80761=CARTESIAN_POINT('Ctrl Pts',(202.257357910054,12.2129259672911,30.3819061383901));
#80762=CARTESIAN_POINT('Ctrl Pts',(202.336009808789,10.9306670929571,30.9980456558665));
#80763=CARTESIAN_POINT('Ctrl Pts',(202.414661707523,9.71080051832528,30.2661021704112));
#80764=CARTESIAN_POINT('Ctrl Pts',(202.493313606257,9.65107742919254,28.8447475776273));
#80765=CARTESIAN_POINT('Ctrl Pts',(202.571965504991,10.8052423032571,28.0130510168065));
#80766=CARTESIAN_POINT('Ctrl Pts',(202.650617403725,12.1346685517936,28.5194516245347));
#80767=CARTESIAN_POINT('Ctrl Pts',(202.729269302459,12.4430128442209,29.9082422938307));
#80768=CARTESIAN_POINT('Ctrl Pts',(202.807921201195,11.4527978566356,30.9296579801117));
#80769=CARTESIAN_POINT('Ctrl Pts',(202.886573099928,10.0551125814128,30.6645323547376));
#80770=CARTESIAN_POINT('Ctrl Pts',(202.965224998662,9.50772626983257,29.3514505021364));
#80771=CARTESIAN_POINT('Ctrl Pts',(203.043876897396,10.3032288371725,28.1720475212547));
#80772=CARTESIAN_POINT('Ctrl Pts',(203.12252879613,11.7257519214275,28.1876616338116));
#80773=CARTESIAN_POINT('Ctrl Pts',(203.201180694865,12.495174864366,29.384241785808));
#80774=CARTESIAN_POINT('Ctrl Pts',(203.279832593599,11.9190982136657,30.6849921153385));
#80775=CARTESIAN_POINT('Ctrl Pts',(203.358484492333,10.5159301624556,30.9193745908879));
#80776=CARTESIAN_POINT('Ctrl Pts',(203.437136391067,9.54837388114503,29.876469722557));
#80777=CARTESIAN_POINT('Ctrl Pts',(203.515788289801,9.88712791901166,28.4947818269146));
#80778=CARTESIAN_POINT('Ctrl Pts',(203.594440188536,11.2273493874618,28.0176842187432));
#80779=CARTESIAN_POINT('Ctrl Pts',(203.67309208727,12.3629804032347,28.8745143626181));
#80780=CARTESIAN_POINT('Ctrl Pts',(203.751743986004,12.2720728816894,30.2942156223834));
#80781=CARTESIAN_POINT('Ctrl Pts',(203.830395884738,11.0364340248,30.9992065328513));
#80782=CARTESIAN_POINT('Ctrl Pts',(203.909047783472,9.76800835408834,30.3550699851692));
#80783=CARTESIAN_POINT('Ctrl Pts',(203.987699682206,9.60824522918933,28.9414602466712));
#80784=CARTESIAN_POINT('Ctrl Pts',(204.06635158094,10.7009143710046,28.0304782545025));
#80785=CARTESIAN_POINT('Ctrl Pts',(204.145003479675,12.0627293412418,28.4419088671411));
#80786=CARTESIAN_POINT('Ctrl Pts',(204.223655378409,12.4681993798916,29.8055137585938));
#80787=CARTESIAN_POINT('Ctrl Pts',(204.302307277143,11.5524463111259,30.894180378558));
#80788=CARTESIAN_POINT('Ctrl Pts',(204.380959175877,10.1395469637827,30.7282486490664));
#80789=CARTESIAN_POINT('Ctrl Pts',(204.459611074611,9.50097055768355,29.456987764702));
#80790=CARTESIAN_POINT('Ctrl Pts',(204.538262973346,10.2113499877134,28.2245059348102));
#80791=CARTESIAN_POINT('Ctrl Pts',(204.61691487208,11.6314570775236,28.1396835900221));
#80792=CARTESIAN_POINT('Ctrl Pts',(204.695566770814,12.4832657980976,29.2793148721768));
#80793=CARTESIAN_POINT('Ctrl Pts',(204.774218669548,12.0004035366468,30.6168916992512));
#80794=CARTESIAN_POINT('Ctrl Pts',(204.852870568282,10.6170586846029,30.950735391922));
#80795=CARTESIAN_POINT('Ctrl Pts',(204.931522467016,9.57884790492899,29.9762976530357));
#80796=CARTESIAN_POINT('Ctrl Pts',(204.983957066173,9.73936276204029,29.0458052715714));
#80797=CARTESIAN_POINT('Ctrl Pts',(205.010174365751,9.99778225136778,28.7156183173004));
#80798=CARTESIAN_POINT('Ctrl Pts',(198.85229800795,11.5096010945807,30.5602158477891));
#80799=CARTESIAN_POINT('Ctrl Pts',(198.878515307528,11.1603063009802,30.7281071404171));
#80800=CARTESIAN_POINT('Ctrl Pts',(198.930949906684,10.2884414873013,30.6886801214029));
#80801=CARTESIAN_POINT('Ctrl Pts',(199.009601805418,9.61438516062817,29.5583165642669));
#80802=CARTESIAN_POINT('Ctrl Pts',(199.088253704153,10.189843649739,28.3755475004547));
#80803=CARTESIAN_POINT('Ctrl Pts',(199.166905602887,11.4930926025464,28.2046023832819));
#80804=CARTESIAN_POINT('Ctrl Pts',(199.245557501621,12.3532172079488,29.1994059004922));
#80805=CARTESIAN_POINT('Ctrl Pts',(199.324209400355,11.9952964538612,30.4646989171939));
#80806=CARTESIAN_POINT('Ctrl Pts',(199.402861299089,10.7418549889306,30.8618711827422));
#80807=CARTESIAN_POINT('Ctrl Pts',(199.481513197823,9.72064879347285,30.0334999802663));
#80808=CARTESIAN_POINT('Ctrl Pts',(199.560165096557,9.85075645265219,28.7250365993692));
#80809=CARTESIAN_POINT('Ctrl Pts',(199.638816995292,11.0150462260339,28.113957772862));
#80810=CARTESIAN_POINT('Ctrl Pts',(199.717468894026,12.165803599825,28.7501710325291));
#80811=CARTESIAN_POINT('Ctrl Pts',(199.79612079276,12.2674570887587,30.061151065713));
#80812=CARTESIAN_POINT('Ctrl Pts',(199.874772691494,11.2285347209873,30.8671544387032));
#80813=CARTESIAN_POINT('Ctrl Pts',(199.953424590228,9.98395436836523,30.4428630522389));
#80814=CARTESIAN_POINT('Ctrl Pts',(200.032076488963,9.65370827305649,29.1700944370783));
#80815=CARTESIAN_POINT('Ctrl Pts',(200.110728387697,10.5349824608951,28.1942060048287));
#80816=CARTESIAN_POINT('Ctrl Pts',(200.189380286431,11.834723456605,28.3933943734058));
#80817=CARTESIAN_POINT('Ctrl Pts',(200.268032185165,12.3833013828978,29.588411024754));
#80818=CARTESIAN_POINT('Ctrl Pts',(200.346684083899,11.687054065275,30.7038670847745));
#80819=CARTESIAN_POINT('Ctrl Pts',(200.425335982633,10.3725305823729,30.7359698109675));
#80820=CARTESIAN_POINT('Ctrl Pts',(200.503987881368,9.62266336423614,29.6558301382575));
#80821=CARTESIAN_POINT('Ctrl Pts',(200.582639780102,10.1122537667614,28.4354597856095));
#80822=CARTESIAN_POINT('Ctrl Pts',(200.661291678836,11.4007220973753,28.173063286041));
#80823=CARTESIAN_POINT('Ctrl Pts',(200.73994357757,12.3285828275996,29.1047697986263));
#80824=CARTESIAN_POINT('Ctrl Pts',(200.818595476304,12.0608592173582,30.3921417841895));
#80825=CARTESIAN_POINT('Ctrl Pts',(200.897247375038,10.8384742628351,30.8766803108589));
#80826=CARTESIAN_POINT('Ctrl Pts',(200.975899273773,9.7614454261661,30.122351837536));
#80827=CARTESIAN_POINT('Ctrl Pts',(201.054551172507,9.79898500241771,28.8079723866329));
#80828=CARTESIAN_POINT('Ctrl Pts',(201.133203071241,10.9173113345259,28.1163447587381));
#80829=CARTESIAN_POINT('Ctrl Pts',(201.211854969975,12.1100487394965,28.6698608321431));
#80830=CARTESIAN_POINT('Ctrl Pts',(201.290506868709,12.3038594213226,29.9704145528143));
#80831=CARTESIAN_POINT('Ctrl Pts',(201.369158767444,11.3243342190144,30.8476448183576));
#80832=CARTESIAN_POINT('Ctrl Pts',(201.447810666178,10.052942446279,30.5121369630686));
#80833=CARTESIAN_POINT('Ctrl Pts',(201.526462564912,9.63380252979966,29.2658126508791));
#80834=CARTESIAN_POINT('Ctrl Pts',(201.605114463646,10.4440961629675,28.2302322393278));
#80835=CARTESIAN_POINT('Ctrl Pts',(201.68376636238,11.7546445854556,28.3373088149847));
#80836=CARTESIAN_POINT('Ctrl Pts',(201.762418261114,12.3860925179668,29.4906847594487));
#80837=CARTESIAN_POINT('Ctrl Pts',(201.841070159849,11.7702034573468,30.6524434373803));
#80838=CARTESIAN_POINT('Ctrl Pts',(201.919722058583,10.4612125639608,30.7771246379412));
#80839=CARTESIAN_POINT('Ctrl Pts',(201.998373957317,9.63707350527895,29.7525284381161));
#80840=CARTESIAN_POINT('Ctrl Pts',(202.077025856051,10.0394244634956,28.5006832930751));
#80841=CARTESIAN_POINT('Ctrl Pts',(202.155677754785,11.3061920359338,28.1481177273148));
#80842=CARTESIAN_POINT('Ctrl Pts',(202.23432965352,12.2974190881889,29.0121035441072));
#80843=CARTESIAN_POINT('Ctrl Pts',(202.312981552254,12.1211058764895,30.3151446839492));
#80844=CARTESIAN_POINT('Ctrl Pts',(202.391633450988,10.9359156851976,30.8846416296885));
#80845=CARTESIAN_POINT('Ctrl Pts',(202.470285349722,9.80839461447045,30.2081072286361));
#80846=CARTESIAN_POINT('Ctrl Pts',(202.548937248456,9.75319264172485,28.8943510477011));
#80847=CARTESIAN_POINT('Ctrl Pts',(202.62758914719,10.8199857170198,28.1256150102703));
#80848=CARTESIAN_POINT('Ctrl Pts',(202.706241045925,12.0487726502588,28.5936804260432));
#80849=CARTESIAN_POINT('Ctrl Pts',(202.784892944659,12.3337748742563,29.8773378153221));
#80850=CARTESIAN_POINT('Ctrl Pts',(202.863544843393,11.4185204634293,30.8214309909227));
#80851=CARTESIAN_POINT('Ctrl Pts',(202.942196742127,10.1266418015891,30.576375724047));
#80852=CARTESIAN_POINT('Ctrl Pts',(203.020848640861,9.62069335364468,29.362695894477));
#80853=CARTESIAN_POINT('Ctrl Pts',(203.099500539595,10.3559753304986,28.2725752702408));
#80854=CARTESIAN_POINT('Ctrl Pts',(203.17815243833,11.6708115465637,28.2870073739437));
#80855=CARTESIAN_POINT('Ctrl Pts',(203.256804337064,12.3819881608799,29.393004834852));
#80856=CARTESIAN_POINT('Ctrl Pts',(203.335456235798,11.8495212702164,30.5952866538646));
#80857=CARTESIAN_POINT('Ctrl Pts',(203.414108134532,10.5525748857415,30.8119260677863));
#80858=CARTESIAN_POINT('Ctrl Pts',(203.492760033266,9.65826388732648,29.8479704694768));
#80859=CARTESIAN_POINT('Ctrl Pts',(203.571411932001,9.97137379904272,28.5708781645454));
#80860=CARTESIAN_POINT('Ctrl Pts',(203.650063830735,11.2101387398515,28.1298974727275));
#80861=CARTESIAN_POINT('Ctrl Pts',(203.728715729469,12.2598009943006,28.9218644479227));
#80862=CARTESIAN_POINT('Ctrl Pts',(203.807367628203,12.1757752916857,30.234092455323));
#80863=CARTESIAN_POINT('Ctrl Pts',(203.886019526937,11.0336759212094,30.885714626759));
#80864=CARTESIAN_POINT('Ctrl Pts',(203.964671425671,9.86127174183416,30.2903400628184));
#80865=CARTESIAN_POINT('Ctrl Pts',(204.043323324406,9.71360289558907,28.9837424405148));
#80866=CARTESIAN_POINT('Ctrl Pts',(204.12197522314,10.7235555464368,28.1417229831548));
#80867=CARTESIAN_POINT('Ctrl Pts',(204.200627121874,11.9822793325505,28.5220077573582));
#80868=CARTESIAN_POINT('Ctrl Pts',(204.279279020608,12.3570547560548,29.7823859652975));
#80869=CARTESIAN_POINT('Ctrl Pts',(204.357930919342,11.5106253988703,30.7886390904618));
#80870=CARTESIAN_POINT('Ctrl Pts',(204.436582818076,10.2046843901768,30.635268611104));
#80871=CARTESIAN_POINT('Ctrl Pts',(204.515234716811,9.61444905778955,29.4602438474781));
#80872=CARTESIAN_POINT('Ctrl Pts',(204.593886615545,10.2710518307703,28.321062512904));
#80873=CARTESIAN_POINT('Ctrl Pts',(204.672538514279,11.5836549463473,28.2426613311632));
#80874=CARTESIAN_POINT('Ctrl Pts',(204.751190413013,12.3709806265892,29.2960210265685));
#80875=CARTESIAN_POINT('Ctrl Pts',(204.829842311747,11.924671673326,30.5323415288316));
#80876=CARTESIAN_POINT('Ctrl Pts',(204.908494210482,10.6460478457716,30.8409128149407));
#80877=CARTESIAN_POINT('Ctrl Pts',(204.987146109216,9.68643098743465,29.9402412943381));
#80878=CARTESIAN_POINT('Ctrl Pts',(205.039580708372,9.834794658775,29.0801884098095));
#80879=CARTESIAN_POINT('Ctrl Pts',(205.06579800795,10.0736514529217,28.7749970421944));
#80880=CARTESIAN_POINT('Ctrl Pts',(198.6865,11.6340070945751,30.8190402776367));
#80881=CARTESIAN_POINT('Ctrl Pts',(198.710737126766,11.4537103993182,30.8788097556703));
#80882=CARTESIAN_POINT('Ctrl Pts',(198.731653684349,11.2655768472979,30.9058979865679));
#80883=CARTESIAN_POINT('Ctrl Pts',(198.776140325335,10.9248764665845,30.8800560222072));
#80884=CARTESIAN_POINT('Ctrl Pts',(198.797718346184,10.7784026223058,30.8423706540008));
#80885=CARTESIAN_POINT('Ctrl Pts',(198.832593474394,10.5724822918099,30.7483060524685));
#80886=CARTESIAN_POINT('Ctrl Pts',(198.844351974729,10.5073488774618,30.71140036245));
#80887=CARTESIAN_POINT('Ctrl Pts',(198.865327041601,10.3947405990162,30.6347745027527));
#80888=CARTESIAN_POINT('Ctrl Pts',(198.874645877699,10.3456915364658,30.5963661489365));
#80889=CARTESIAN_POINT('Ctrl Pts',(198.898468331836,10.220730616038,30.4849982515005));
#80890=CARTESIAN_POINT('Ctrl Pts',(198.912523247939,10.1497701747385,30.405322048357));
#80891=CARTESIAN_POINT('Ctrl Pts',(198.940905585237,10.0375577642678,30.2378655455178));
#80892=CARTESIAN_POINT('Ctrl Pts',(198.954811357476,9.99489876194716,30.1534283775981));
#80893=CARTESIAN_POINT('Ctrl Pts',(198.970000790184,9.96359235009872,30.0641429946324));
#80894=CARTESIAN_POINT('Origin',(204.9,11.,29.5));
#80895=CARTESIAN_POINT('',(205.,11.,31.0635));
#80896=CARTESIAN_POINT('Origin',(205.,11.,29.5));
#80897=CARTESIAN_POINT('Origin',(204.9,11.,31.0635));
#80898=CARTESIAN_POINT('Origin',(205.,13.75,29.5));
#80899=CARTESIAN_POINT('',(205.,8.25,29.5));
#80900=CARTESIAN_POINT('Origin',(205.,11.,29.5));
#80901=CARTESIAN_POINT('Origin',(206.15,11.,29.5));
#80902=CARTESIAN_POINT('',(206.15,8.27924642791744,29.1));
#80903=CARTESIAN_POINT('',(206.15,8.25,29.5));
#80904=CARTESIAN_POINT('Origin',(206.15,11.,29.5));
#80905=CARTESIAN_POINT('',(206.15,13.7207535720826,29.1));
#80906=CARTESIAN_POINT('',(206.15,7.75,29.1));
#80907=CARTESIAN_POINT('',(206.15,13.7207535720826,29.9));
#80908=CARTESIAN_POINT('Origin',(206.15,11.,29.5));
#80909=CARTESIAN_POINT('',(206.15,8.27924642791744,29.9));
#80910=CARTESIAN_POINT('',(206.15,14.25,29.9));
#80911=CARTESIAN_POINT('Origin',(206.15,11.,29.5));
#80912=CARTESIAN_POINT('Origin',(207.,7.75,29.9));
#80913=CARTESIAN_POINT('',(206.6,8.27924642791744,29.9));
#80914=CARTESIAN_POINT('',(205.8,8.27924642791744,29.9));
#80915=CARTESIAN_POINT('',(206.6,13.7207535720826,29.9));
#80916=CARTESIAN_POINT('',(205.8,13.7207535720826,29.9));
#80917=CARTESIAN_POINT('',(207.,13.3157072353818,29.9));
#80918=CARTESIAN_POINT('Ctrl Pts',(207.,13.3157072353819,29.9));
#80919=CARTESIAN_POINT('Ctrl Pts',(206.816084562245,13.5023462336636,29.9));
#80920=CARTESIAN_POINT('Ctrl Pts',(206.6,13.7207535720826,29.9));
#80921=CARTESIAN_POINT('',(207.,8.68429276461816,29.9));
#80922=CARTESIAN_POINT('',(207.,9.375,29.9));
#80923=CARTESIAN_POINT('Ctrl Pts',(206.6,8.27924642791744,29.9));
#80924=CARTESIAN_POINT('Ctrl Pts',(206.816084562245,8.4976537663367,29.9));
#80925=CARTESIAN_POINT('Ctrl Pts',(207.,8.68429276461812,29.9));
#80926=CARTESIAN_POINT('Origin',(207.,14.25,29.1));
#80927=CARTESIAN_POINT('',(206.6,8.27924642791744,29.1));
#80928=CARTESIAN_POINT('',(205.8,8.27924642791744,29.1));
#80929=CARTESIAN_POINT('',(207.,8.68429276461816,29.1));
#80930=CARTESIAN_POINT('Ctrl Pts',(207.,8.68429276461812,29.1));
#80931=CARTESIAN_POINT('Ctrl Pts',(206.816084562245,8.4976537663364,29.1));
#80932=CARTESIAN_POINT('Ctrl Pts',(206.6,8.27924642791744,29.1));
#80933=CARTESIAN_POINT('',(207.,13.3157072353818,29.1));
#80934=CARTESIAN_POINT('',(207.,12.625,29.1));
#80935=CARTESIAN_POINT('',(206.6,13.7207535720826,29.1));
#80936=CARTESIAN_POINT('Ctrl Pts',(206.6,13.7207535720826,29.1));
#80937=CARTESIAN_POINT('Ctrl Pts',(206.816084562245,13.5023462336636,29.1));
#80938=CARTESIAN_POINT('Ctrl Pts',(207.,13.3157072353819,29.1));
#80939=CARTESIAN_POINT('',(205.8,13.7207535720826,29.1));
#80940=CARTESIAN_POINT('Origin',(205.8,11.,29.5));
#80941=CARTESIAN_POINT('',(205.8,8.25,29.5));
#80942=CARTESIAN_POINT('Origin',(206.6,11.,29.5));
#80943=CARTESIAN_POINT('Origin',(206.6,11.,29.5));
#80944=CARTESIAN_POINT('Origin',(207.,11.,29.5));
#80945=CARTESIAN_POINT('Origin',(207.,11.,29.5));
#80946=CARTESIAN_POINT('Origin',(207.,11.,29.5));
#80947=CARTESIAN_POINT('Origin',(207.,11.,29.5));
#80948=CARTESIAN_POINT('Origin',(206.8,11.,29.5));
#80949=CARTESIAN_POINT('Origin',(199.,12.15,29.5));
#80950=CARTESIAN_POINT('',(199.,9.85,29.5));
#80951=CARTESIAN_POINT('Origin',(199.,11.,29.5));
#80952=CARTESIAN_POINT('Origin',(198.825,11.,29.5));
#80953=CARTESIAN_POINT('',(198.825,9.675,29.5));
#80954=CARTESIAN_POINT('Origin',(206.8,11.,29.5));
#81027=UNCERTAINTY_MEASURE_WITH_UNIT(LENGTH_MEASURE(0.01),#81041,
'DISTANCE_ACCURACY_VALUE',
'Maximum model space distance between geometric entities at asserted c
onnectivities');
#81028=UNCERTAINTY_MEASURE_WITH_UNIT(LENGTH_MEASURE(0.01),#81041,
'DISTANCE_ACCURACY_VALUE',
'Maximum model space distance between geometric entities at asserted c
onnectivities');
#81039=(
GEOMETRIC_REPRESENTATION_CONTEXT(3)
GLOBAL_UNCERTAINTY_ASSIGNED_CONTEXT((#81027))
GLOBAL_UNIT_ASSIGNED_CONTEXT((#81041,#81043,#81044))
REPRESENTATION_CONTEXT('','3D')
);
#81040=(
GEOMETRIC_REPRESENTATION_CONTEXT(3)
GLOBAL_UNCERTAINTY_ASSIGNED_CONTEXT((#81028))
GLOBAL_UNIT_ASSIGNED_CONTEXT((#81041,#81043,#81044))
REPRESENTATION_CONTEXT('','3D')
);
#81041=(
LENGTH_UNIT()
NAMED_UNIT(*)
SI_UNIT(.MILLI.,.METRE.)
);
#81043=(
NAMED_UNIT(*)
PLANE_ANGLE_UNIT()
SI_UNIT($,.RADIAN.)
);
#81044=(
NAMED_UNIT(*)
SI_UNIT($,.STERADIAN.)
SOLID_ANGLE_UNIT()
);
#81055=SHAPE_DEFINITION_REPRESENTATION(#81066,#81139);
#81066=PRODUCT_DEFINITION_SHAPE('',$,#81151);
#81139=SHAPE_REPRESENTATION('',(#16512),#81039);
#81140=PRODUCT_DEFINITION_CONTEXT('part definition',#81175,'design');
#81151=PRODUCT_DEFINITION('ISO 1207 - M3 x 6 - 4.8',
'ISO 1207 - M3 x 6 - 4.8',#81162,#81140);
#81162=PRODUCT_DEFINITION_FORMATION('',$,#81187);
#81175=APPLICATION_CONTEXT(
'Core Data for Automotive Mechanical Design Process');
#81176=PRODUCT_CONTEXT('part definition',#81175,'mechanical');
#81187=PRODUCT('ISO 1207 - M3 x 6 - 4.8','ISO 1207 - M3 x 6 - 4.8',$,(#81176));
#81198=PRESENTATION_STYLE_ASSIGNMENT((#81209));
#81209=SURFACE_STYLE_USAGE(.BOTH.,#81220);
#81220=SURFACE_SIDE_STYLE('',(#81231));
#81231=SURFACE_STYLE_FILL_AREA(#81242);
#81242=FILL_AREA_STYLE('Opaque(205,209,215)',(#81253));
#81253=FILL_AREA_STYLE_COLOUR('Opaque(205,209,215)',#81264);
#81264=COLOUR_RGB('Opaque(205,209,215)', 0.40784314, 0.44705882, 0.49803922);
ENDSEC;
END-ISO-10303-21;
